ISO-10303-21;
HEADER;
FILE_DESCRIPTION (('STEP AP214'),
    '1' );
FILE_NAME ('7 mm Screw.step',
    '2026-10-25T21:42:00',
    ( '' ),
    ( '' ),
    'SwSTEP 2.0',
    'SolidWorks 2025',
    '' );
FILE_SCHEMA (( 'AUTOMOTIVE_DESIGN' ));
ENDSEC;

DATA;
#2=CARTESIAN_POINT ( 'NONE',  ( 0.9468279798049143992, -42.43229166714461087, 27.28240155936039812 ) ) ;
#3=CARTESIAN_POINT ( 'NONE',  ( 0.9468279798049125118, -42.80312500047794799, 29.19375250200204164 ) ) ;
#10=CARTESIAN_POINT ( 'NONE',  ( 0.9468279798049132889, -44.39062500047794657, 29.19375250200204164 ) ) ;
#20=EDGE_LOOP ( 'NONE', ( #28188, #12369, #422, #8859 ) ) ;
#39=CARTESIAN_POINT ( 'NONE',  ( 4.257385064927798446, -48.31875000421112532, 25.69375250200204519 ) ) ;
#42=CARTESIAN_POINT ( 'NONE',  ( 7.567941867304905479, -50.01145833381128369, 27.28240155936039812 ) ) ;
#43=CARTESIAN_POINT ( 'NONE',  ( 4.257384923554915268, -50.12499999999998579, 25.69375250200204519 ) ) ;
#46=CARTESIAN_POINT ( 'NONE',  ( 0.7573849235549138248, -46.04166666666666430, 27.17302655983835180 ) ) ;
#51=CARTESIAN_POINT ( 'NONE',  ( 4.257384923554908163, -48.26562500047794657, 33.01645438728532866 ) ) ;
#55=AXIS2_PLACEMENT_3D ( 'NONE', #31793, #18416, #15652 ) ;
#57=CARTESIAN_POINT ( 'NONE',  ( 6.007384923554907274, -49.16666666666665719, 26.16266358875650866 ) ) ;
#66=CARTESIAN_POINT ( 'NONE',  ( 3.802356695541112774, -48.80793045187983381, 25.72158031941516398 ) ) ;
#69=CARTESIAN_POINT ( 'NONE',  ( 4.257384923554909051, -51.81875000095590877, 25.15230061767466552 ) ) ;
#82=CARTESIAN_POINT ( 'NONE',  ( 3.319562750045980337, -42.60267090063073425, 25.69375250200204519 ) ) ;
#89=CARTESIAN_POINT ( 'NONE',  ( 4.257384923554909051, -52.24999999999999289, 32.69375250200203453 ) ) ;
#94=AXIS2_PLACEMENT_3D ( 'NONE', #31466, #15525, #2334 ) ;
#96=CARTESIAN_POINT ( 'NONE',  ( 7.567941867304904591, -49.14062500047794657, 29.19375250200204164 ) ) ;
#101=CARTESIAN_POINT ( 'NONE',  ( 4.257384923554908163, -51.67812500047794799, 33.01645438728532866 ) ) ;
#108=CARTESIAN_POINT ( 'NONE',  ( 4.257384923554908163, -47.90562499990440415, 33.23520438632941421 ) ) ;
#114=CARTESIAN_POINT ( 'NONE',  ( 6.007384923554907274, -45.36041666762256597, 26.16266358875650866 ) ) ;
#143=CARTESIAN_POINT ( 'NONE',  ( 4.257384923554909939, -41.90485061181026083, 34.69375250200203453 ) ) ;
#150=CARTESIAN_POINT ( 'NONE',  ( 2.602106451679909505, -47.21979166714461229, 32.06077891596451224 ) ) ;
#151=CARTESIAN_POINT ( 'NONE',  ( 3.819759407186210431, -42.40485061181024662, 32.67317255660598363 ) ) ;
#168=CARTESIAN_POINT ( 'NONE',  ( 0.9581295613991068771, -50.72155651497971718, 27.97398363749321604 ) ) ;
#169=AXIS2_PLACEMENT_3D ( 'NONE', #4109, #7736, #14539 ) ;
#172=FACE_OUTER_BOUND ( 'NONE', #32186, .T. ) ;
#175=( BOUNDED_CURVE ( )  B_SPLINE_CURVE ( 2, ( #22467, #3125, #28846, #13319, #12698, #9935, #26304, #9724, #9505 ),
 .UNSPECIFIED., .F., .T. ) 
 B_SPLINE_CURVE_WITH_KNOTS ( ( 3, 2, 2, 2, 3 ),
 ( 0.03749999999999999861, 0.04166666666666666435, 0.05000000000000000278, 0.05833333333333333426, 0.06250000000000000000 ),
 .UNSPECIFIED. ) 
 CURVE ( )  GEOMETRIC_REPRESENTATION_ITEM ( )  RATIONAL_B_SPLINE_CURVE ( ( 0.9330127018922194093, 0.9330127018922194093, 1.000000000000000000, 0.8660254037844387076, 1.000000000000000000, 0.8660254037844387076, 1.000000000000000000, 0.9330127018922194093, 0.9330127018922194093 ) ) 
 REPRESENTATION_ITEM ( '' )  );
#190=LINE ( 'NONE', #13808, #23079 ) ;
#195=ADVANCED_FACE ( 'NONE', ( #38969 ), #25380, .T. ) ;
#207=CARTESIAN_POINT ( 'NONE',  ( 7.567941867304902814, -43.09479166714462650, 31.10510344464368870 ) ) ;
#212=CARTESIAN_POINT ( 'NONE',  ( 7.779211916243011338, -46.95355343573054085, 29.54647484881920150 ) ) ;
#213=CARTESIAN_POINT ( 'NONE',  ( 2.602106451679912169, -45.97395833381128227, 26.32672608803957459 ) ) ;
#219=VERTEX_POINT ( 'NONE', #19196 ) ;
#221=CARTESIAN_POINT ( 'NONE',  ( 7.134063624253377256, -45.99088173149362291, 31.23767365766003579 ) ) ;
#241=CARTESIAN_POINT ( 'NONE',  ( 7.757384923554902834, -44.29166666666665719, 31.21447844416572792 ) ) ;
#245=CARTESIAN_POINT ( 'NONE',  ( 0.9468279798049115126, -51.76145833381127659, 31.10510344464368515 ) ) ;
#249=CARTESIAN_POINT ( 'NONE',  ( 4.257384923554908163, -48.37499999999999289, 33.23520438632941421 ) ) ;
#251=DIRECTION ( 'NONE',  ( 0.000000000000000000, -1.000000000000000000, -0.000000000000000000 ) ) ;
#253=AXIS2_PLACEMENT_3D ( 'NONE', #22912, #22701, #16742 ) ;
#256=CARTESIAN_POINT ( 'NONE',  ( 7.788572856623962259, -43.43930825666139839, 28.96296817063725726 ) ) ;
#257=CARTESIAN_POINT ( 'NONE',  ( 2.602106451679912169, -49.97395833381128227, 26.32672608803957459 ) ) ;
#265=CARTESIAN_POINT ( 'NONE',  ( 0.7573849235549138248, -51.54166666666666430, 27.17302655983835180 ) ) ;
#268=CARTESIAN_POINT ( 'NONE',  ( 4.611008686493843101, -46.56168535230849415, 32.69375256037956490 ) ) ;
#275=CARTESIAN_POINT ( 'NONE',  ( 2.507384923554911715, -48.77708333428924448, 26.16266358875650866 ) ) ;
#277=VECTOR ( 'NONE', #39050, 1000.000000000000000 ) ;
#292=CARTESIAN_POINT ( 'NONE',  ( 2.507384923554909495, -42.61041666762257307, 32.22484141524756751 ) ) ;
#305=CARTESIAN_POINT ( 'NONE',  ( 7.567941867304904591, -44.09895833381128227, 27.28240155936039812 ) ) ;
#309=CARTESIAN_POINT ( 'NONE',  ( 7.567941867304902814, -50.59479166714461940, 31.10510344464368870 ) ) ;
#318=CARTESIAN_POINT ( 'NONE',  ( 0.7573849235549120484, -47.48895833323773275, 31.21447844416572792 ) ) ;
#321=VERTEX_POINT ( 'NONE', #35359 ) ;
#325=CARTESIAN_POINT ( 'NONE',  ( 7.757384923554902834, -44.98541666762258018, 31.21447844416572792 ) ) ;
#326=CARTESIAN_POINT ( 'NONE',  ( 2.507384923554909495, -43.61041666762257307, 32.22484141524756751 ) ) ;
#353=LINE ( 'NONE', #26314, #7101 ) ;
#360=PRODUCT_DEFINITION_FORMATION_WITH_SPECIFIED_SOURCE ( 'ANY', '', #37738, .NOT_KNOWN. ) ;
#365=CARTESIAN_POINT ( 'NONE',  ( 5.912663395429907709, -43.46979166714461940, 26.32672608803957459 ) ) ;
#373=CARTESIAN_POINT ( 'NONE',  ( 4.257384971216501057, -47.81875000207092086, 25.69375250200204519 ) ) ;
#374=CARTESIAN_POINT ( 'NONE',  ( 0.7565246463372455876, -42.40335187990289256, 28.93845584589010755 ) ) ;
#381=ORIENTED_EDGE ( 'NONE', *, *, #27250, .F. ) ;
#383=CARTESIAN_POINT ( 'NONE',  ( 7.757384923554904610, -43.20833333333332860, 27.17302655983835180 ) ) ;
#390=ADVANCED_FACE ( 'NONE', ( #31953 ), #32376, .T. ) ;
#398=CARTESIAN_POINT ( 'NONE',  ( 2.507384923554911715, -52.08333333333332149, 26.16266358875650866 ) ) ;
#406=CARTESIAN_POINT ( 'NONE',  ( 2.507384923554909495, -47.91666666666665719, 32.22484141524756751 ) ) ;
#420=CARTESIAN_POINT ( 'NONE',  ( 4.257384923554909051, -42.42812500047794799, 25.37105061671875106 ) ) ;
#422=ORIENTED_EDGE ( 'NONE', *, *, #12693, .T. ) ;
#426=CIRCLE ( 'NONE', #40519, 5.499999999999994671 ) ;
#432=CARTESIAN_POINT ( 'NONE',  ( 7.022018489332528368, -45.88858045111683737, 27.00065075227327682 ) ) ;
#435=EDGE_LOOP ( 'NONE', ( #4263, #14199, #16671, #20884 ) ) ;
#457=CARTESIAN_POINT ( 'NONE',  ( 2.602106451679909505, -51.71979166714461940, 32.06077891596451224 ) ) ;
#458=CARTESIAN_POINT ( 'NONE',  ( 4.140911557495338791, -47.31612386767535838, 25.69541433326542901 ) ) ;
#461=CARTESIAN_POINT ( 'NONE',  ( 7.757384923554904610, -47.20833333333332860, 27.17302655983835180 ) ) ;
#468=CARTESIAN_POINT ( 'NONE',  ( 4.257384923554908163, -48.76562500047794657, 33.01645438728532866 ) ) ;
#471=B_SPLINE_CURVE_WITH_KNOTS ( 'NONE', 3,
 ( #27386, #15670, #25237, #12252, #28626, #35016, #5247, #18223, #41615, #22041, #8856, #14827, #18432, #12040, #25033, #11621, #18014, #41405, #38202, #8432 ),
 .UNSPECIFIED., .F., .F.,
 ( 4, 2, 2, 2, 2, 2, 2, 2, 2, 4 ),
 ( 0.9522129200431463936, 0.9544189165146044207, 0.9566249129860625589, 0.9588309094575205860, 0.9610369059289787241, 0.9632429024004367513, 0.9643459006361658759, 0.9654488988718948894, 0.9676548953433530276, 0.9698608918148110547 ),
 .UNSPECIFIED. ) ;
#477=CARTESIAN_POINT ( 'NONE',  ( 7.757384923554904610, -49.70833333333332149, 27.17302655983835180 ) ) ;
#478=CARTESIAN_POINT ( 'NONE',  ( 7.567941867304902814, -51.59895833381127517, 27.28240155936039457 ) ) ;
#480=CARTESIAN_POINT ( 'NONE',  ( 3.000402550427474058, -43.59873921524524576, 32.46193631706483984 ) ) ;
#482=CARTESIAN_POINT ( 'NONE',  ( 3.319562750045992328, -46.10267090063073425, 25.69375250200203453 ) ) ;
#488=CARTESIAN_POINT ( 'NONE',  ( 2.507384923554909495, -49.11041666762257307, 32.22484141524756751 ) ) ;
#501=CARTESIAN_POINT ( 'NONE',  ( 4.140911794976756433, -44.81612387057926838, 25.69541432478372656 ) ) ;
#507=( BOUNDED_CURVE ( )  B_SPLINE_CURVE ( 2, ( #22402, #482, #15834, #23027, #29186, #28987, #13453, #22614, #23236 ),
 .UNSPECIFIED., .F., .T. ) 
 B_SPLINE_CURVE_WITH_KNOTS ( ( 3, 2, 2, 2, 3 ),
 ( 0.6124999999999999334, 0.6166666666666666963, 0.6250000000000000000, 0.6333333333333333037, 0.6375000000000000666 ),
 .UNSPECIFIED. ) 
 CURVE ( )  GEOMETRIC_REPRESENTATION_ITEM ( )  RATIONAL_B_SPLINE_CURVE ( ( 0.9330127018922194093, 0.9330127018922185211, 1.000000000000000000, 0.8660254037844387076, 1.000000000000000000, 0.8660254037844387076, 1.000000000000000000, 0.9330127018922185211, 0.9330127018922194093 ) ) 
 REPRESENTATION_ITEM ( '' )  );
#513=CARTESIAN_POINT ( 'NONE',  ( 4.257384923554908163, -44.26562500047795368, 33.01645438728532866 ) ) ;
#518=CARTESIAN_POINT ( 'NONE',  ( 5.912663395429907709, -50.46979166714461940, 26.32672608803957459 ) ) ;
#525=CARTESIAN_POINT ( 'NONE',  ( 0.7573849235549129366, -47.03062499990440415, 29.19375250200204164 ) ) ;
#531=CARTESIAN_POINT ( 'NONE',  ( 0.7573849235549138248, -43.73541666762257307, 27.17302655983835180 ) ) ;
#532=CARTESIAN_POINT ( 'NONE',  ( 4.257384923554909051, -43.81875000095590877, 25.15230061767466552 ) ) ;
#553=CARTESIAN_POINT ( 'NONE',  ( 0.7980551096671941735, -51.68002053973792442, 29.84941435640805096 ) ) ;
#572=CARTESIAN_POINT ( 'NONE',  ( 7.567941867304905479, -43.51145833381128369, 27.28240155936039812 ) ) ;
#573=CARTESIAN_POINT ( 'NONE',  ( 3.389804136281158620, -42.40485061181025372, 32.59157291905037113 ) ) ;
#581=CARTESIAN_POINT ( 'NONE',  ( 4.879030421287430030, -48.55394890265384333, 32.63810574445512458 ) ) ;
#590=CARTESIAN_POINT ( 'NONE',  ( 1.492573714751328495, -50.74676105021354999, 27.04712707065803556 ) ) ;
#591=CARTESIAN_POINT ( 'NONE',  ( 6.007384923554907274, -43.16666666666665719, 26.16266358875650866 ) ) ;
#617=CARTESIAN_POINT ( 'NONE',  ( 4.257384923554909051, -52.75000000000000000, 29.19375250200204164 ) ) ;
#627=CARTESIAN_POINT ( 'NONE',  ( 0.9468279798049125118, -42.30312500047794799, 29.19375250200204164 ) ) ;
#631=VERTEX_POINT ( 'NONE', #21084 ) ;
#636=CARTESIAN_POINT ( 'NONE',  ( 4.257384923554908163, -48.67812500047794089, 33.01645438728532866 ) ) ;
#641=CARTESIAN_POINT ( 'NONE',  ( 6.376638882316896684, -45.86847629457404452, 26.37211172118686520 ) ) ;
#654=CARTESIAN_POINT ( 'NONE',  ( 7.757384923554902834, -45.79166666666667140, 31.21447844416572792 ) ) ;
#662=CARTESIAN_POINT ( 'NONE',  ( 3.319562750045979005, -47.39732909936925154, 32.69375250200202743 ) ) ;
#669=CARTESIAN_POINT ( 'NONE',  ( 7.567941867304905479, -51.01145833381128369, 27.28240155936039812 ) ) ;
#673=CARTESIAN_POINT ( 'NONE',  ( 0.7573849235549120484, -47.95833333333332149, 31.21447844416572792 ) ) ;
#677=CARTESIAN_POINT ( 'NONE',  ( 1.499251777370047778, -49.13834154090844919, 31.42035496242633741 ) ) ;
#679=VERTEX_POINT ( 'NONE', #1730 ) ;
#681=CARTESIAN_POINT ( 'NONE',  ( 5.912663395429907709, -48.05729166714461087, 26.32672608803957459 ) ) ;
#689=ADVANCED_FACE ( 'NONE', ( #24701 ), #1926, .T. ) ;
#691=CARTESIAN_POINT ( 'NONE',  ( 2.507384923554911715, -48.58333333333332860, 26.16266358875650866 ) ) ;
#692=CARTESIAN_POINT ( 'NONE',  ( 7.567941867304902814, -50.18229166714461797, 31.10510344464368870 ) ) ;
#694=VECTOR ( 'NONE', #28183, 1000.000000000000000 ) ;
#702=CARTESIAN_POINT ( 'NONE',  ( 6.007384923554907274, -50.86041666762257307, 26.16266358875650866 ) ) ;
#704=CARTESIAN_POINT ( 'NONE',  ( 7.757384923554905498, -51.24999999999999289, 29.19375250200204164 ) ) ;
#717=CARTESIAN_POINT ( 'NONE',  ( 0.7573849235549120484, -43.15208333428923737, 31.21447844416572792 ) ) ;
#727=ORIENTED_EDGE ( 'NONE', *, *, #8077, .F. ) ;
#730=CARTESIAN_POINT ( 'NONE',  ( 5.912663395429904156, -45.22395833381128227, 32.06077891596451224 ) ) ;
#735=CARTESIAN_POINT ( 'NONE',  ( 7.567941867304905479, -46.55312500047795510, 29.19375250200204164 ) ) ;
#743=CARTESIAN_POINT ( 'NONE',  ( 7.757384923554902834, -45.82229166657107555, 31.21447844416572792 ) ) ;
#749=CARTESIAN_POINT ( 'NONE',  ( 0.7573849235549120484, -43.65208333428924448, 31.21447844416572792 ) ) ;
#766=CARTESIAN_POINT ( 'NONE',  ( 4.558104779508536097, -51.32590786667334726, 25.70589253242968297 ) ) ;
#791=CARTESIAN_POINT ( 'NONE',  ( 2.815360438258434961, -42.21442363818449905, 32.18390116252139421 ) ) ;
#792=DIRECTION ( 'NONE',  ( 0.000000000000000000, 0.000000000000000000, -1.000000000000000000 ) ) ;
#801=CARTESIAN_POINT ( 'NONE',  ( 6.996467676173400818, -42.40388931145210449, 26.99673536543800978 ) ) ;
#805=CARTESIAN_POINT ( 'NONE',  ( 3.928120587378577611, -44.31094111304120986, 25.70856423692994497 ) ) ;
#810=AXIS2_PLACEMENT_3D ( 'NONE', #27651, #17876, #5738 ) ;
#811=CARTESIAN_POINT ( 'NONE',  ( 0.000000000000000000, 3.250000000000000444, 0.000000000000000000 ) ) ;
#812=CARTESIAN_POINT ( 'NONE',  ( 6.007384923554904610, -42.83333333333332149, 32.22484141524757462 ) ) ;
#826=DIRECTION ( 'NONE',  ( -0.000000000000000000, -1.000000000000000000, -0.000000000000000000 ) ) ;
#840=CARTESIAN_POINT ( 'NONE',  ( 4.715534414328271140, -50.05662139172729752, 32.69375242513323343 ) ) ;
#850=ORIENTED_EDGE ( 'NONE', *, *, #28567, .T. ) ;
#851=AXIS2_PLACEMENT_3D ( 'NONE', #19395, #35140, #21955 ) ;
#855=EDGE_LOOP ( 'NONE', ( #30774, #33387, #21883, #12996 ) ) ;
#858=CARTESIAN_POINT ( 'NONE',  ( 0.9468279798049125118, -46.80312500047795510, 29.19375250200204164 ) ) ;
#882=CARTESIAN_POINT ( 'NONE',  ( 2.507384923554909495, -47.41666666666665719, 32.22484141524756751 ) ) ;
#886=CARTESIAN_POINT ( 'NONE',  ( 4.257384923554907274, -44.37499999999999289, 32.69375250200203453 ) ) ;
#889=CARTESIAN_POINT ( 'NONE',  ( 7.567941867304905479, -52.01145833381127659, 27.28240155936039812 ) ) ;
#894=CARTESIAN_POINT ( 'NONE',  ( 7.757384923554902834, -46.29166666666665719, 31.21447844416572792 ) ) ;
#897=CARTESIAN_POINT ( 'NONE',  ( 0.8153229055217173782, -49.20977436168735863, 28.41138067166303216 ) ) ;
#900=CARTESIAN_POINT ( 'NONE',  ( 4.257384923554909051, -49.01562500047793947, 25.37105061671875461 ) ) ;
#907=CARTESIAN_POINT ( 'NONE',  ( 7.757384923554902834, -46.79166666666665009, 31.21447844416572792 ) ) ;
#909=CARTESIAN_POINT ( 'NONE',  ( 0.9468279798049132889, -51.39062500047794657, 29.19375250200204164 ) ) ;
#915=CARTESIAN_POINT ( 'NONE',  ( 4.257384923554909051, -52.75000000000000000, 26.19375250200205230 ) ) ;
#921=CARTESIAN_POINT ( 'NONE',  ( 4.257384923554908163, -50.56875000095590167, 33.23520438632941421 ) ) ;
#946=( BOUNDED_CURVE ( )  B_SPLINE_CURVE ( 2, ( #38403, #41602, #25441, #5021, #18002, #30980, #1836, #27782, #8419, #101, #13490, #16697, #29029, #9907, #22441, #42026, #16089, #32841, #26065, #32635, #16491, #9697, #22863, #6901, #29440, #13082, #35831, #16284, #25857, #3499, #10103, #23067, #29225, #6694, #19663, #309, #6283, #19875, #518, #3708, #9476, #22657, #13291, #26275, #6495, #29653, #39221, #26476, #12877, #38820, #19048, #28819, #35632, #35420, #32229, #36035, #19466, #39432, #15874, #10307, #32434, #3297, #19258, #35205, #6069, #3097, #32017, #2884, #41818, #39022, #12671, #25650, #38611, #7329, #31282, #24498, #15129, #21092, #3921, #28091, #41074, #2142, #5334, #17116, #40647, #10521, #30081, #4131, #21504, #14719, #21301, #5132, #26899, #24289, #954, #37671, #34271, #24709, #27678, #34476, #18111, #40857, #11712, #4921, #11505, #37467, #8322, #36465, #8530, #23280, #18309, #39650, #27882, #10727, #23503, #37261, #39866, #13920, #8115, #31081, #34066, #36245, #7118, #20091, #17902, #30876, #1739, #1934, #33055, #16902, #14914, #29868, #735, #20299, #13709, #26689, #33267, #5549, #25121, #28299, #31491, #25751, #12345, #32122, #15977, #5965, #19359, #15549, #28925, #41704, #6177, #35313, #22336, #41282, #38086, #35528, #2985, #21914, #19151, #28504, #2566, #31906, #41495, #12126, #25331, #37875, #6386, #8734, #8942, #3201, #32334, #41922, #2358, #38717, #21708, #16187, #18939, #34892, #5760, #2775, #29127, #12770, #15758, #9587, #38289, #18736, #31698, #22545, #11924, #28710, #24917, #34683, #12558, #18523, #9155, #15350, #22132, #25545, #35104, #38506, #9371, #36576, #3825, #26806, #12983, #10209, #4250, #20418, #36143, #23617, #17234, #39328, #3609, #19994, #32741, #207, #16601, #6801, #29556, #36366, #7236, #39125, #3, #22967, #32535, #39546, #16805, #23401, #39770, #22762, #35737, #420, #13604, #29767, #627, #25964, #33383, #7015, #23178 ),
 .UNSPECIFIED., .F., .T. ) 
 B_SPLINE_CURVE_WITH_KNOTS ( ( 3, 2, 2, 2, 2, 2, 2, 2, 2, 2, 2, 2, 2, 2, 2, 2, 2, 2, 2, 2, 2, 2, 2, 2, 2, 2, 2, 2, 2, 2, 2, 2, 2, 2, 2, 2, 2, 2, 2, 2, 2, 2, 2, 2, 2, 2, 2, 2, 2, 2, 2, 2, 2, 2, 2, 2, 2, 2, 2, 2, 2, 2, 2, 2, 2, 2, 2, 2, 2, 2, 2, 2, 2, 2, 2, 2, 2, 2, 2, 2, 2, 2, 2, 2, 2, 2, 2, 2, 2, 2, 2, 2, 2, 2, 2, 2, 2, 2, 2, 2, 2, 2, 2, 2, 2, 2, 2, 2, 2, 2, 2, 2, 2, 2, 2, 2, 2, 2, 2, 3 ),
 ( 0.000000000000000000, 0.008333333333333333218, 0.01666666666666666644, 0.02500000000000000139, 0.03333333333333333287, 0.04166666666666666435, 0.05000000000000000278, 0.05833333333333333426, 0.06666666666666666574, 0.07499999999999999722, 0.08333333333333332871, 0.09166666666666666019, 0.1000000000000000056, 0.1083333333333333370, 0.1166666666666666685, 0.1250000000000000000, 0.1333333333333333315, 0.1416666666666666630, 0.1499999999999999944, 0.1583333333333333259, 0.1666666666666666574, 0.1749999999999999889, 0.1833333333333333204, 0.1916666666666666796, 0.2000000000000000111, 0.2083333333333333426, 0.2166666666666666741, 0.2250000000000000056, 0.2333333333333333370, 0.2416666666666666685, 0.2500000000000000000, 0.2583333333333333592, 0.2666666666666666630, 0.2750000000000000222, 0.2833333333333333259, 0.2916666666666666852, 0.2999999999999999889, 0.3083333333333333481, 0.3166666666666666519, 0.3250000000000000111, 0.3333333333333333148, 0.3416666666666666741, 0.3499999999999999778, 0.3583333333333333370, 0.3666666666666666408, 0.3750000000000000555, 0.3833333333333333592, 0.3916666666666666630, 0.4000000000000000222, 0.4083333333333333259, 0.4166666666666666852, 0.4249999999999999889, 0.4333333333333333481, 0.4416666666666666519, 0.4500000000000000111, 0.4583333333333333148, 0.4666666666666666741, 0.4749999999999999778, 0.4833333333333333370, 0.4916666666666666408, 0.5000000000000000000, 0.5083333333333333037, 0.5166666666666667185, 0.5250000000000000222, 0.5333333333333333259, 0.5416666666666666297, 0.5500000000000000444, 0.5583333333333333481, 0.5666666666666666519, 0.5749999999999999556, 0.5833333333333333703, 0.5916666666666666741, 0.5999999999999999778, 0.6083333333333332815, 0.6166666666666666963, 0.6250000000000000000, 0.6333333333333333037, 0.6416666666666667185, 0.6500000000000000222, 0.6583333333333333259, 0.6666666666666666297, 0.6750000000000000444, 0.6833333333333333481, 0.6916666666666666519, 0.6999999999999999556, 0.7083333333333333703, 0.7166666666666666741, 0.7249999999999999778, 0.7333333333333332815, 0.7416666666666666963, 0.7500000000000001110, 0.7583333333333333037, 0.7666666666666667185, 0.7750000000000000222, 0.7833333333333333259, 0.7916666666666666297, 0.8000000000000000444, 0.8083333333333333481, 0.8166666666666666519, 0.8249999999999999556, 0.8333333333333333703, 0.8416666666666666741, 0.8499999999999999778, 0.8583333333333332815, 0.8666666666666666963, 0.8750000000000000000, 0.8833333333333333037, 0.8916666666666667185, 0.9000000000000000222, 0.9083333333333333259, 0.9166666666666666297, 0.9250000000000000444, 0.9333333333333333481, 0.9416666666666666519, 0.9499999999999999556, 0.9583333333333333703, 0.9666666666666666741, 0.9749999999999999778, 0.9833333333333332815, 0.9845487975508080414 ),
 .UNSPECIFIED. ) 
 CURVE ( )  GEOMETRIC_REPRESENTATION_ITEM ( )  RATIONAL_B_SPLINE_CURVE ( ( 1.000000000000000000, 0.8660254037844387076, 1.000000000000000000, 0.8660254037844387076, 1.000000000000000000, 0.8660254037844387076, 1.000000000000000000, 0.8660254037844387076, 1.000000000000000000, 0.8660254037844387076, 1.000000000000000000, 0.8660254037844387076, 1.000000000000000000, 0.8660254037844387076, 1.000000000000000000, 0.8660254037844387076, 1.000000000000000000, 0.8660254037844387076, 1.000000000000000000, 0.8660254037844387076, 1.000000000000000000, 0.8660254037844387076, 1.000000000000000000, 0.8660254037844387076, 1.000000000000000000, 0.8660254037844387076, 1.000000000000000000, 0.8660254037844387076, 1.000000000000000000, 0.8660254037844387076, 1.000000000000000000, 0.8660254037844387076, 1.000000000000000000, 0.8660254037844387076, 1.000000000000000000, 0.8660254037844387076, 1.000000000000000000, 0.8660254037844387076, 1.000000000000000000, 0.8660254037844387076, 1.000000000000000000, 0.8660254037844387076, 1.000000000000000000, 0.8660254037844387076, 1.000000000000000000, 0.8660254037844387076, 1.000000000000000000, 0.8660254037844387076, 1.000000000000000000, 0.8660254037844387076, 1.000000000000000000, 0.8660254037844387076, 1.000000000000000000, 0.8660254037844387076, 1.000000000000000000, 0.8660254037844387076, 1.000000000000000000, 0.8660254037844387076, 1.000000000000000000, 0.8660254037844387076, 1.000000000000000000, 0.8660254037844387076, 1.000000000000000000, 0.8660254037844387076, 1.000000000000000000, 0.8660254037844387076, 1.000000000000000000, 0.8660254037844387076, 1.000000000000000000, 0.8660254037844387076, 1.000000000000000000, 0.8660254037844387076, 1.000000000000000000, 0.8660254037844387076, 1.000000000000000000, 0.8660254037844387076, 1.000000000000000000, 0.8660254037844387076, 1.000000000000000000, 0.8660254037844387076, 1.000000000000000000, 0.8660254037844387076, 1.000000000000000000, 0.8660254037844387076, 1.000000000000000000, 0.8660254037844387076, 1.000000000000000000, 0.8660254037844387076, 1.000000000000000000, 0.8660254037844387076, 1.000000000000000000, 0.8660254037844387076, 1.000000000000000000, 0.8660254037844387076, 1.000000000000000000, 0.8660254037844387076, 1.000000000000000000, 0.8660254037844387076, 1.000000000000000000, 0.8660254037844387076, 1.000000000000000000, 0.8660254037844387076, 1.000000000000000000, 0.8660254037844387076, 1.000000000000000000, 0.8660254037844387076, 1.000000000000000000, 0.8660254037844387076, 1.000000000000000000, 0.8660254037844387076, 1.000000000000000000, 0.8660254037844387076, 1.000000000000000000, 0.8660254037844387076, 1.000000000000000000, 0.8660254037844387076, 1.000000000000000000, 0.8660254037844387076, 1.000000000000000000, 0.8660254037844387076, 1.000000000000000000, 0.8660254037844387076, 1.000000000000000000, 0.8660254037844387076, 1.000000000000000000, 0.8660254037844387076, 1.000000000000000000, 0.8660254037844387076, 1.000000000000000000, 0.8660254037844387076, 1.000000000000000000, 0.8660254037844387076, 1.000000000000000000, 0.8660254037844387076, 1.000000000000000000, 0.8660254037844387076, 1.000000000000000000, 0.8660254037844387076, 1.000000000000000000, 0.8660254037844387076, 1.000000000000000000, 0.8660254037844387076, 1.000000000000000000, 0.8660254037844387076, 1.000000000000000000, 0.8660254037844387076, 1.000000000000000000, 0.8660254037844387076, 1.000000000000000000, 0.8660254037844387076, 1.000000000000000000, 0.8660254037844387076, 1.000000000000000000, 0.8660254037844387076, 1.000000000000000000, 0.8660254037844387076, 1.000000000000000000, 0.8660254037844387076, 1.000000000000000000, 0.8660254037844387076, 1.000000000000000000, 0.8660254037844387076, 1.000000000000000000, 0.8660254037844387076, 1.000000000000000000, 0.8660254037844387076, 1.000000000000000000, 0.8660254037844387076, 1.000000000000000000, 0.8660254037844387076, 1.000000000000000000, 0.8660254037844387076, 1.000000000000000000, 0.8660254037844387076, 1.000000000000000000, 0.8660254037844387076, 1.000000000000000000, 0.8660254037844387076, 1.000000000000000000, 0.8660254037844387076, 1.000000000000000000, 0.8660254037844387076, 1.000000000000000000, 0.8660254037844387076, 1.000000000000000000, 0.8660254037844387076, 1.000000000000000000, 0.8660254037844387076, 1.000000000000000000, 0.8660254037844387076, 1.000000000000000000, 0.8660254037844387076, 1.000000000000000000, 0.8660254037844387076, 1.000000000000000000, 0.8660254037844387076, 1.000000000000000000, 0.8660254037844387076, 1.000000000000000000, 0.8660254037844387076, 1.000000000000000000, 0.8660254037844387076, 1.000000000000000000, 0.8660254037844387076, 1.000000000000000000, 0.8660254037844387076, 1.000000000000000000, 0.8660254037844387076, 1.000000000000000000, 0.8660254037844387076, 1.000000000000000000, 0.8660254037844387076, 1.000000000000000000, 0.8660254037844387076, 1.000000000000000000, 0.8660254037844387076, 1.000000000000000000, 0.8660254037844387076, 1.000000000000000000, 0.8660254037844387076, 1.000000000000000000, 0.8660254037844387076, 1.000000000000000000, 0.8660254037844387076, 1.000000000000000000, 0.8660254037844387076, 1.000000000000000000, 0.8660254037844387076, 1.000000000000000000, 0.8660254037844387076, 1.000000000000000000, 0.8660254037844387076, 1.000000000000000000, 0.8660254037844387076, 1.000000000000000000, 0.8660254037844387076, 1.000000000000000000, 0.9804590406699229543, 0.9666184021816470739 ) ) 
 REPRESENTATION_ITEM ( '' )  );
#950=CARTESIAN_POINT ( 'NONE',  ( 2.602106451679912169, -44.97395833381127517, 26.32672608803957459 ) ) ;
#954=CARTESIAN_POINT ( 'NONE',  ( 5.912663395429905044, -48.13645833381128369, 32.06077891596451224 ) ) ;
#960=CARTESIAN_POINT ( 'NONE',  ( 0.7573849235549129366, -46.03062499990440415, 29.19375250200204164 ) ) ;
#963=ORIENTED_EDGE ( 'NONE', *, *, #1923, .T. ) ;
#966=CARTESIAN_POINT ( 'NONE',  ( 0.7573849235549129366, -43.19375000095590167, 29.19375250200204164 ) ) ;
#975=VECTOR ( 'NONE', #19045, 1000.000000000000114 ) ;
#983=EDGE_CURVE ( 'NONE', #5445, #22238, #32854, .T. ) ;
#985=EDGE_CURVE ( 'NONE', #10374, #13809, #16848, .T. ) ;
#997=CARTESIAN_POINT ( 'NONE',  ( 7.262703625583482037, -50.90085599904792701, 27.39607937939682358 ) ) ;
#1008=CARTESIAN_POINT ( 'NONE',  ( 4.257384923554909051, -44.42812500047794799, 25.37105061671875461 ) ) ;
#1016=CARTESIAN_POINT ( 'NONE',  ( 4.334160784610809003, -42.40468115105387170, 25.68300921981454721 ) ) ;
#1018=ORIENTED_EDGE ( 'NONE', *, *, #37998, .T. ) ;
#1019=CIRCLE ( 'NONE', #6439, 10.16127960363519200 ) ;
#1021=CARTESIAN_POINT ( 'NONE',  ( 1.296509284301159415, -44.23832384044276012, 27.27887260493179156 ) ) ;
#1022=CARTESIAN_POINT ( 'NONE',  ( 0.9157898350030243551, -50.17036160625526975, 30.23696554908891443 ) ) ;
#1028=CARTESIAN_POINT ( 'NONE',  ( 7.757384923554905498, -50.94375000095590167, 29.19375250200204164 ) ) ;
#1033=VECTOR ( 'NONE', #30327, 1000.000000000000000 ) ;
#1052=CARTESIAN_POINT ( 'NONE',  ( 2.492184380352688855, -47.60993350042300420, 32.25065013957770788 ) ) ;
#1055=CARTESIAN_POINT ( 'NONE',  ( 5.195207097063841317, -49.35267090063072004, 32.69375250200202743 ) ) ;
#1066=DIRECTION ( 'NONE',  ( 0.000000000000000000, 0.000000000000000000, -1.000000000000000000 ) ) ;
#1071=EDGE_LOOP ( 'NONE', ( #40402, #21040, #17866, #5697 ) ) ;
#1077=CARTESIAN_POINT ( 'NONE',  ( 0.9468279798049134000, -47.34479166714461940, 27.28240155936039457 ) ) ;
#1080=CARTESIAN_POINT ( 'NONE',  ( 4.257384923554909051, -51.62499999999999289, 25.15230061767466552 ) ) ;
#1081=CARTESIAN_POINT ( 'NONE',  ( 0.7573849235549138248, -47.04166666666665719, 27.17302655983835180 ) ) ;
#1083=EDGE_CURVE ( 'NONE', #40134, #15555, #16767, .T. ) ;
#1107=CARTESIAN_POINT ( 'NONE',  ( 0.9468279798049115126, -48.76145833381128369, 31.10510344464368515 ) ) ;
#1111=CARTESIAN_POINT ( 'NONE',  ( 6.007384923554904610, -43.83333333333332149, 32.22484141524757462 ) ) ;
#1113=CARTESIAN_POINT ( 'NONE',  ( 5.171512903780173254, -49.54615306638036998, 32.60305723588238180 ) ) ;
#1117=CARTESIAN_POINT ( 'NONE',  ( 7.567941867304904591, -46.09895833381127517, 27.28240155936039812 ) ) ;
#1123=CARTESIAN_POINT ( 'NONE',  ( 4.257384923554908163, -47.87499999999999289, 33.23520438632941421 ) ) ;
#1124=CARTESIAN_POINT ( 'NONE',  ( 7.567941867304902814, -50.68229166714461797, 31.10510344464368870 ) ) ;
#1127=CARTESIAN_POINT ( 'NONE',  ( 1.546849826716359066, -43.13869041197474985, 31.40817622872517489 ) ) ;
#1134=CARTESIAN_POINT ( 'NONE',  ( 0.7573849235549129366, -48.69375000095590167, 29.19375250200204164 ) ) ;
#1136=LINE ( 'NONE', #4319, #13234 ) ;
#1149=CARTESIAN_POINT ( 'NONE',  ( 7.757384923554905498, -42.94375000095590167, 29.19375250200204164 ) ) ;
#1161=CARTESIAN_POINT ( 'NONE',  ( 0.9468279798049124008, -44.84895833381128227, 31.10510344464368515 ) ) ;
#1169=CARTESIAN_POINT ( 'NONE',  ( 4.257384923554908163, -45.90562499990440415, 33.23520438632941421 ) ) ;
#1171=ADVANCED_FACE ( 'NONE', ( #42067 ), #29705, .F. ) ;
#1177=CARTESIAN_POINT ( 'NONE',  ( 2.507384923554911715, -42.77708333428924448, 26.16266358875650866 ) ) ;
#1189=B_SPLINE_CURVE_WITH_KNOTS ( 'NONE', 3,
 ( #33112, #7180, #22922, #10369, #3977, #26122, #32489, #6751, #19520, #29081 ),
 .UNSPECIFIED., .F., .F.,
 ( 4, 2, 2, 2, 4 ),
 ( 0.000000000000000000, 0.003174066542862672043, 0.006348133085725344085, 0.009522199628588016995, 0.01269626617145068817 ),
 .UNSPECIFIED. ) ;
#1191=CARTESIAN_POINT ( 'NONE',  ( 7.757390661421029066, -51.45010600855616190, 29.50199576836617865 ) ) ;
#1199=CARTESIAN_POINT ( 'NONE',  ( 4.257384923554909051, -52.75000000000000000, 32.69375250200203453 ) ) ;
#1204=DIRECTION ( 'NONE',  ( -0.000000000000000000, -1.000000000000000000, -0.000000000000000000 ) ) ;
#1214=CARTESIAN_POINT ( 'NONE',  ( 5.912663395429907709, -42.46979166714461940, 26.32672608803957459 ) ) ;
#1222=CARTESIAN_POINT ( 'NONE',  ( 4.821117960794319757, -48.55532725896756574, 32.64833370828896619 ) ) ;
#1235=CARTESIAN_POINT ( 'NONE',  ( 2.507384923554909495, -49.11041666762257307, 32.22484141524756751 ) ) ;
#1260=CARTESIAN_POINT ( 'NONE',  ( 0.7562705821891613223, -47.68342873967699092, 29.64403518322449926 ) ) ;
#1283=CARTESIAN_POINT ( 'NONE',  ( 0.9468279798049115126, -45.76145833381128369, 31.10510344464368515 ) ) ;
#1296=CARTESIAN_POINT ( 'NONE',  ( 2.783277039523302410, -46.10390887767790957, 32.37987024324076657 ) ) ;
#1312=CARTESIAN_POINT ( 'NONE',  ( 5.912663395429907709, -48.96979166714461940, 26.32672608803957459 ) ) ;
#1316=CARTESIAN_POINT ( 'NONE',  ( 0.7573849235549120484, -44.95833333333332149, 31.21447844416572792 ) ) ;
#1324=CARTESIAN_POINT ( 'NONE',  ( 5.912663395429904156, -47.22395833381128227, 32.06077891596451224 ) ) ;
#1327=ORIENTED_EDGE ( 'NONE', *, *, #11016, .T. ) ;
#1331=CARTESIAN_POINT ( 'NONE',  ( 7.757384923554902834, -47.29166666666665719, 31.21447844416572792 ) ) ;
#1332=CARTESIAN_POINT ( 'NONE',  ( 7.567941867304904591, -51.14062500047794657, 29.19375250200204164 ) ) ;
#1335=CARTESIAN_POINT ( 'NONE',  ( 0.9180208126477865660, -43.22160567301123990, 28.03124139943347615 ) ) ;
#1342=CARTESIAN_POINT ( 'NONE',  ( 2.507384923554911715, -47.77708333428923737, 26.16266358875650866 ) ) ;
#1368=CARTESIAN_POINT ( 'NONE',  ( 2.602106451679912169, -42.97395833381127517, 26.32672608803957459 ) ) ;
#1375=CARTESIAN_POINT ( 'NONE',  ( 7.757384923554905498, -45.78062499990440415, 29.19375250200204164 ) ) ;
#1383=CARTESIAN_POINT ( 'NONE',  ( 5.912663395429905044, -51.13645833381127659, 32.06077891596451224 ) ) ;
#1401=CARTESIAN_POINT ( 'NONE',  ( 9.216391464164017222, 3.250000000000000444, 25.89968016835878828 ) ) ;
#1409=CYLINDRICAL_SURFACE ( 'NONE', #11558, 3.499999999999996003 ) ;
#1410=CARTESIAN_POINT ( 'NONE',  ( 7.436871778188120174, -50.90975612242779391, 27.73019409324238538 ) ) ;
#1417=VERTEX_POINT ( 'NONE', #29811 ) ;
#1418=AXIS2_PLACEMENT_3D ( 'NONE', #15413, #40712, #15618 ) ;
#1420=CARTESIAN_POINT ( 'NONE',  ( 7.567941867304904591, -49.64062500047794657, 29.19375250200204164 ) ) ;
#1423=CARTESIAN_POINT ( 'NONE',  ( 0.8510322481285291785, -45.21500081289355677, 28.26783748059364498 ) ) ;
#1427=DIRECTION ( 'NONE',  ( -0.000000000000000000, -1.000000000000000000, -0.000000000000000000 ) ) ;
#1432=CARTESIAN_POINT ( 'NONE',  ( 9.589638516698011372, 7.250000000000000000, 31.84134197688108614 ) ) ;
#1441=CARTESIAN_POINT ( 'NONE',  ( 2.507384923554909495, -50.11041666762257307, 32.22484141524756751 ) ) ;
#1468=ORIENTED_EDGE ( 'NONE', *, *, #23246, .T. ) ;
#1472=CARTESIAN_POINT ( 'NONE',  ( 3.044481415175603889, -42.20865620537255580, 32.27411812269912161 ) ) ;
#1479=CARTESIAN_POINT ( 'NONE',  ( 4.257384923554909051, -52.75000000000000000, 29.19375250200204164 ) ) ;
#1480=ORIENTED_EDGE ( 'NONE', *, *, #7710, .F. ) ;
#1486=CARTESIAN_POINT ( 'NONE',  ( 7.567941867304904591, -47.09479166714461940, 31.10510344464368870 ) ) ;
#1520=CARTESIAN_POINT ( 'NONE',  ( 4.257384923554908163, -49.67812500047794799, 33.01645438728532866 ) ) ;
#1524=CARTESIAN_POINT ( 'NONE',  ( 2.507384923554911715, -43.58333333333332149, 26.16266358875650866 ) ) ;
#1526=CARTESIAN_POINT ( 'NONE',  ( 7.758145088196113370, -49.43856291864983632, 28.97712966651067035 ) ) ;
#1527=CARTESIAN_POINT ( 'NONE',  ( 4.005449014497274085, -49.31275154288346130, 25.69375972451559775 ) ) ;
#1530=CARTESIAN_POINT ( 'NONE',  ( 0.9468279798049124008, -45.84895833381127517, 31.10510344464368515 ) ) ;
#1533=ORIENTED_EDGE ( 'NONE', *, *, #16772, .T. ) ;
#1536=CARTESIAN_POINT ( 'NONE',  ( 0.7573849235549138248, -48.04166666666665719, 27.17302655983835180 ) ) ;
#1537=CARTESIAN_POINT ( 'NONE',  ( 7.567941867304902814, -47.59895833381128227, 27.28240155936039457 ) ) ;
#1550=CARTESIAN_POINT ( 'NONE',  ( 0.7573849235549138248, -46.73541666762257307, 27.17302655983835180 ) ) ;
#1556=ADVANCED_FACE ( 'NONE', ( #6844 ), #16434, .T. ) ;
#1577=CARTESIAN_POINT ( 'NONE',  ( 6.125319626624167846, -43.86454229931417359, 26.21514642412573437 ) ) ;
#1580=CARTESIAN_POINT ( 'NONE',  ( 4.257384923554909051, -42.51562500047793947, 25.37105061671875461 ) ) ;
#1584=CARTESIAN_POINT ( 'NONE',  ( 5.430196717779790738, -44.34665582036524256, 25.88055882389310725 ) ) ;
#1586=EDGE_LOOP ( 'NONE', ( #24463, #9634, #20948, #21464, #13249, #41038 ) ) ;
#1587=CARTESIAN_POINT ( 'NONE',  ( 4.257384923554909051, -45.65562499990440415, 25.15230061767466552 ) ) ;
#1593=CARTESIAN_POINT ( 'NONE',  ( 4.257384923554909051, -42.31875000095590167, 25.15230061767466552 ) ) ;
#1625=CARTESIAN_POINT ( 'NONE',  ( 2.602106451679909505, -49.80729166714461087, 32.06077891596451224 ) ) ;
#1629=CARTESIAN_POINT ( 'NONE',  ( 5.195207097063835988, -46.35267090063073425, 32.69375250200204164 ) ) ;
#1631=EDGE_LOOP ( 'NONE', ( #21821, #22394, #31414, #40600 ) ) ;
#1642=DIRECTION ( 'NONE',  ( 0.000000000000000000, -0.000000000000000000, 1.000000000000000000 ) ) ;
#1643=CARTESIAN_POINT ( 'NONE',  ( 7.757384923554905498, -48.94375000095590167, 29.19375250200204164 ) ) ;
#1656=AXIS2_PLACEMENT_3D ( 'NONE', #19284, #42052, #13318 ) ;
#1664=CARTESIAN_POINT ( 'NONE',  ( 7.705332930860770091, -42.95677857963937640, 29.79556752327468416 ) ) ;
#1694=CARTESIAN_POINT ( 'NONE',  ( 7.567941867304904591, -45.59479166714461229, 31.10510344464368870 ) ) ;
#1717=EDGE_CURVE ( 'NONE', #36911, #29977, #41710, .T. ) ;
#1726=CARTESIAN_POINT ( 'NONE',  ( 4.257384923554908163, -47.67812500047795510, 33.01645438728532866 ) ) ;
#1730=CARTESIAN_POINT ( 'NONE',  ( 4.257461754300457812, -46.31875183025808695, 25.69375250284532441 ) ) ;
#1731=CARTESIAN_POINT ( 'NONE',  ( 7.757384923554902834, -44.79166666666666430, 31.21447844416572792 ) ) ;
#1737=CARTESIAN_POINT ( 'NONE',  ( 5.912663395429907709, -47.05729166714461087, 26.32672608803957459 ) ) ;
#1739=CARTESIAN_POINT ( 'NONE',  ( 0.9468279798049125118, -46.80312500047795510, 29.19375250200204164 ) ) ;
#1742=CARTESIAN_POINT ( 'NONE',  ( -0.7016216170541935693, 3.250000000000000444, 32.48782483564529855 ) ) ;
#1745=CARTESIAN_POINT ( 'NONE',  ( 7.757384923554905498, -43.74999999999999289, 29.19375250200204164 ) ) ;
#1746=CARTESIAN_POINT ( 'NONE',  ( 4.257384923554909051, -48.51562500047794657, 25.37105061671875106 ) ) ;
#1747=EDGE_CURVE ( 'NONE', #11963, #3413, #27387, .T. ) ;
#1758=CARTESIAN_POINT ( 'NONE',  ( 2.507384923554909495, -47.61041666762257307, 32.22484141524756751 ) ) ;
#1789=AXIS2_PLACEMENT_3D ( 'NONE', #8648, #38000, #41409 ) ;
#1791=ORIENTED_EDGE ( 'NONE', *, *, #31748, .F. ) ;
#1792=CARTESIAN_POINT ( 'NONE',  ( 4.965282557631612192, -42.38877029433117372, 33.23404929009055309 ) ) ;
#1795=ORIENTED_EDGE ( 'NONE', *, *, #17608, .F. ) ;
#1798=CARTESIAN_POINT ( 'NONE',  ( 0.7573849235549120484, -42.65208333428924448, 31.21447844416572792 ) ) ;
#1819=ADVANCED_FACE ( 'NONE', ( #15342 ), #39663, .T. ) ;
#1829=ORIENTED_EDGE ( 'NONE', *, *, #13265, .T. ) ;
#1831=CARTESIAN_POINT ( 'NONE',  ( 0.9468279798049132889, -50.39062500047794657, 29.19375250200204164 ) ) ;
#1836=CARTESIAN_POINT ( 'NONE',  ( 0.9468279798049125118, -51.80312500047794799, 29.19375250200204164 ) ) ;
#1842=CARTESIAN_POINT ( 'NONE',  ( 2.728101031522838671, -50.28437517702589332, 26.01938517402391682 ) ) ;
#1849=CARTESIAN_POINT ( 'NONE',  ( 6.007384923554907274, -49.36041666762257307, 26.16266358875650866 ) ) ;
#1850=CARTESIAN_POINT ( 'NONE',  ( 7.567941867304904591, -43.14062500047794657, 29.19375250200204164 ) ) ;
#1865=LINE ( 'NONE', #27814, #20701 ) ;
#1869=CARTESIAN_POINT ( 'NONE',  ( 7.656741415129464379, -42.96220386570389138, 30.03251987822094549 ) ) ;
#1880=CARTESIAN_POINT ( 'NONE',  ( 5.442628577851887250, -49.04202465591859550, 32.54506058780780364 ) ) ;
#1886=ORIENTED_EDGE ( 'NONE', *, *, #17548, .T. ) ;
#1893=CARTESIAN_POINT ( 'NONE',  ( 2.602106451679909505, -42.21979166714461940, 32.06077891596451224 ) ) ;
#1894=CARTESIAN_POINT ( 'NONE',  ( 4.257384923554910827, 0.8500000000000013101, 19.03247289836684786 ) ) ;
#1896=CYLINDRICAL_SURFACE ( 'NONE', #10533, 3.499999999999996003 ) ;
#1907=CARTESIAN_POINT ( 'NONE',  ( 7.757384923554905498, -45.74999999999999289, 29.19375250200204164 ) ) ;
#1921=CARTESIAN_POINT ( 'NONE',  ( 7.567941867304904591, -47.59479166714461940, 31.10510344464368870 ) ) ;
#1923=EDGE_CURVE ( 'NONE', #34443, #19251, #23848, .T. ) ;
#1926=CYLINDRICAL_SURFACE ( 'NONE', #29456, 3.499999999999996003 ) ;
#1927=CARTESIAN_POINT ( 'NONE',  ( 0.7573849235549129366, -43.99999999999999289, 29.19375250200204164 ) ) ;
#1933=CARTESIAN_POINT ( 'NONE',  ( 5.912663395429907709, -45.55729166714461797, 26.32672608803957459 ) ) ;
#1934=CARTESIAN_POINT ( 'NONE',  ( 0.9468279798049117346, -46.76145833381129080, 31.10510344464368515 ) ) ;
#1936=ORIENTED_EDGE ( 'NONE', *, *, #30169, .T. ) ;
#1942=CARTESIAN_POINT ( 'NONE',  ( 2.507384923554909495, -45.41666666666665719, 32.22484141524756751 ) ) ;
#1943=CARTESIAN_POINT ( 'NONE',  ( 0.9468279798049124008, -48.34895833381128227, 31.10510344464368515 ) ) ;
#1951=ORIENTED_EDGE ( 'NONE', *, *, #25909, .T. ) ;
#1955=CARTESIAN_POINT ( 'NONE',  ( 0.7573849235549120484, -46.65208333428924448, 31.21447844416572792 ) ) ;
#1964=AXIS2_PLACEMENT_3D ( 'NONE', #7496, #4085, #16650 ) ;
#1978=ORIENTED_EDGE ( 'NONE', *, *, #28194, .F. ) ;
#1982=CARTESIAN_POINT ( 'NONE',  ( 6.007384923554907274, -52.16666666666665719, 26.16266358875650866 ) ) ;
#1985=CARTESIAN_POINT ( 'NONE',  ( 7.567941867304902814, -42.68229166714461797, 31.10510344464368870 ) ) ;
#1989=CARTESIAN_POINT ( 'NONE',  ( 4.624072753243583023, -44.56205984194657788, 32.69375259985920934 ) ) ;
#1993=CARTESIAN_POINT ( 'NONE',  ( 0.7573849235549138248, -44.07229166657106845, 27.17302655983835180 ) ) ;
#1999=CARTESIAN_POINT ( 'NONE',  ( 2.380045031808905698, -43.77242317320209253, 26.19950162479453226 ) ) ;
#2001=CARTESIAN_POINT ( 'NONE',  ( 7.567941867304905479, -51.55312500047794799, 29.19375250200204164 ) ) ;
#2028=AXIS2_PLACEMENT_3D ( 'NONE', #12182, #25174, #18785 ) ;
#2032=EDGE_LOOP ( 'NONE', ( #10951, #11409, #20085, #32440 ) ) ;
#2035=CARTESIAN_POINT ( 'NONE',  ( 5.912663395429907709, -50.55729166714461797, 26.32672608803957459 ) ) ;
#2038=CYLINDRICAL_SURFACE ( 'NONE', #19826, 3.499999999999996003 ) ;
#2046=CARTESIAN_POINT ( 'NONE',  ( 4.257384923554908163, -49.90562499990439704, 33.23520438632941421 ) ) ;
#2049=EDGE_LOOP ( 'NONE', ( #40201, #850, #7875, #33124, #26495, #2875 ) ) ;
#2052=CARTESIAN_POINT ( 'NONE',  ( 4.257384923554909051, -49.62499999999998579, 25.69375250200204519 ) ) ;
#2053=CARTESIAN_POINT ( 'NONE',  ( 6.007384923554904610, -47.02708333428923737, 32.22484141524757462 ) ) ;
#2055=ORIENTED_EDGE ( 'NONE', *, *, #26968, .T. ) ;
#2059=CARTESIAN_POINT ( 'NONE',  ( 0.9220621800903404663, -46.66572407051145177, 30.40549418696603468 ) ) ;
#2066=VECTOR ( 'NONE', #21161, 1000.000000000000000 ) ;
#2085=CARTESIAN_POINT ( 'NONE',  ( 7.757384923554905498, -49.24999999999998579, 29.19375250200204164 ) ) ;
#2088=CARTESIAN_POINT ( 'NONE',  ( 4.839185499523360079, -49.05546107154852109, 32.69375246874288621 ) ) ;
#2092=VECTOR ( 'NONE', #21291, 1000.000000000000114 ) ;
#2093=DIRECTION ( 'NONE',  ( 0.000000000000000000, 0.000000000000000000, -1.000000000000000000 ) ) ;
#2096=DIRECTION ( 'NONE',  ( -0.000000000000000000, 1.000000000000000000, -0.000000000000000000 ) ) ;
#2099=ORIENTED_EDGE ( 'NONE', *, *, #42091, .T. ) ;
#2103=CARTESIAN_POINT ( 'NONE',  ( 2.602106451679909505, -44.21979166714461940, 32.06077891596451224 ) ) ;
#2107=DIRECTION ( 'NONE',  ( 0.000000000000000000, 0.000000000000000000, -1.000000000000000000 ) ) ;
#2126=CARTESIAN_POINT ( 'NONE',  ( 6.229482922732664463, -45.52162552700547593, 32.08667129827552600 ) ) ;
#2133=CARTESIAN_POINT ( 'NONE',  ( 0.9468279798049125118, -45.30312500047794799, 29.19375250200204164 ) ) ;
#2140=ORIENTED_EDGE ( 'NONE', *, *, #34915, .F. ) ;
#2141=CARTESIAN_POINT ( 'NONE',  ( 7.567941867304902814, -43.68229166714461797, 31.10510344464368870 ) ) ;
#2142=CARTESIAN_POINT ( 'NONE',  ( 4.257384923554908163, -48.67812500047794799, 33.01645438728532866 ) ) ;
#2144=ORIENTED_EDGE ( 'NONE', *, *, #1083, .F. ) ;
#2149=CARTESIAN_POINT ( 'NONE',  ( 6.007384923554907274, -45.66666666666666430, 26.16266358875650866 ) ) ;
#2150=CARTESIAN_POINT ( 'NONE',  ( 0.9468279798049124008, -48.84895833381128227, 31.10510344464368515 ) ) ;
#2163=CARTESIAN_POINT ( 'NONE',  ( 0.7573849235549138248, -46.23541666762256597, 27.17302655983835180 ) ) ;
#2165=( BOUNDED_CURVE ( )  B_SPLINE_CURVE ( 2, ( #4259, #23626, #26388, #1081, #36377, #7453, #27025, #39340, #36807 ),
 .UNSPECIFIED., .F., .F. ) 
 B_SPLINE_CURVE_WITH_KNOTS ( ( 3, 2, 2, 2, 3 ),
 ( 0.5124999999999999556, 0.5166666666666667185, 0.5250000000000000222, 0.5333333333333333259, 0.5374999999999999778 ),
 .UNSPECIFIED. ) 
 CURVE ( )  GEOMETRIC_REPRESENTATION_ITEM ( )  RATIONAL_B_SPLINE_CURVE ( ( 0.9330127018922194093, 0.9330127018922185211, 1.000000000000000000, 0.8660254037844387076, 1.000000000000000000, 0.8660254037844387076, 1.000000000000000000, 0.9330127018922194093, 0.9330127018922194093 ) ) 
 REPRESENTATION_ITEM ( '' )  );
#2184=CARTESIAN_POINT ( 'NONE',  ( 5.974550946483529579, -51.02784515227923379, 32.24395051825254654 ) ) ;
#2190=EDGE_CURVE ( 'NONE', #15360, #34443, #27012, .T. ) ;
#2197=CARTESIAN_POINT ( 'NONE',  ( 2.602106451679909505, -43.80729166714461797, 32.06077891596451224 ) ) ;
#2205=CARTESIAN_POINT ( 'NONE',  ( 0.7573849235549138248, -42.57229166657106845, 27.17302655983835180 ) ) ;
#2214=CARTESIAN_POINT ( 'NONE',  ( 6.007384923554907274, -42.36041666762257307, 26.16266358875650866 ) ) ;
#2236=VECTOR ( 'NONE', #29752, 1000.000000000000000 ) ;
#2248=CARTESIAN_POINT ( 'NONE',  ( 7.567941867304902814, -50.18229166714461797, 31.10510344464368870 ) ) ;
#2260=VERTEX_POINT ( 'NONE', #3326 ) ;
#2261=CARTESIAN_POINT ( 'NONE',  ( 6.007384923554907274, -52.19729166657106845, 26.16266358875650866 ) ) ;
#2265=CARTESIAN_POINT ( 'NONE',  ( 4.257384923554909051, -52.24999999999999289, 29.19375250200204164 ) ) ;
#2267=CARTESIAN_POINT ( 'NONE',  ( 4.257384923554909051, -46.81875000095590877, 25.15230061767466552 ) ) ;
#2276=EDGE_CURVE ( 'NONE', #3504, #22457, #32874, .T. ) ;
#2290=CARTESIAN_POINT ( 'NONE',  ( 6.007384923554904610, -42.83333333333332149, 32.22484141524757462 ) ) ;
#2295=CARTESIAN_POINT ( 'NONE',  ( 0.8068856798407963993, -48.20862872111767672, 28.57227212758943580 ) ) ;
#2298=CARTESIAN_POINT ( 'NONE',  ( 2.494517222039486004, -46.27575957839410137, 26.13536210233941759 ) ) ;
#2319=CARTESIAN_POINT ( 'NONE',  ( 4.257384923554909051, -43.42812500047794799, 25.37105061671875461 ) ) ;
#2320=DIRECTION ( 'NONE',  ( 0.8956692225370903593, 0.000000000000000000, 0.4447208605404113779 ) ) ;
#2321=ADVANCED_FACE ( 'NONE', ( #36277 ), #22684, .F. ) ;
#2323=CARTESIAN_POINT ( 'NONE',  ( 4.257384923554933032, -43.62499999999999289, 25.69375250200204519 ) ) ;
#2334=DIRECTION ( 'NONE',  ( -0.06269504844767276319, 0.000000000000000000, -0.9980327303751835855 ) ) ;
#2345=CARTESIAN_POINT ( 'NONE',  ( 3.170325152817199843, -45.79317935478493951, 25.85978506093603713 ) ) ;
#2354=CARTESIAN_POINT ( 'NONE',  ( 4.257420362424698901, -42.81875084473693249, 25.69375250218146078 ) ) ;
#2357=CARTESIAN_POINT ( 'NONE',  ( 0.9468279798049132889, -43.89062500047794657, 29.19375250200204164 ) ) ;
#2358=CARTESIAN_POINT ( 'NONE',  ( 2.602106451679911281, -44.88645833381128369, 26.32672608803957459 ) ) ;
#2368=CARTESIAN_POINT ( 'NONE',  ( 6.007384923554904610, -44.83333333333332149, 32.22484141524757462 ) ) ;
#2369=CARTESIAN_POINT ( 'NONE',  ( 0.9468279798049143992, -48.93229166714461087, 27.28240155936039457 ) ) ;
#2382=CARTESIAN_POINT ( 'NONE',  ( 2.507384923554909495, -45.61041666762256597, 32.22484141524756751 ) ) ;
#2400=CARTESIAN_POINT ( 'NONE',  ( 7.566614879033199514, -50.97369423425535473, 30.42082090999991806 ) ) ;
#2406=CARTESIAN_POINT ( 'NONE',  ( 0.7573849235549120484, -50.95833333333332860, 31.21447844416572792 ) ) ;
#2412=CARTESIAN_POINT ( 'NONE',  ( 7.755074336822840309, -50.43152286027196141, 28.71967905532235221 ) ) ;
#2418=CARTESIAN_POINT ( 'NONE',  ( 2.507384923554911715, -43.11395833323773275, 26.16266358875650866 ) ) ;
#2420=VERTEX_POINT ( 'NONE', #13162 ) ;
#2425=CARTESIAN_POINT ( 'NONE',  ( 2.602106451679909505, -48.21979166714461229, 32.06077891596451224 ) ) ;
#2434=CARTESIAN_POINT ( 'NONE',  ( 2.507384923554909495, -44.91666666666665719, 32.22484141524756751 ) ) ;
#2458=CARTESIAN_POINT ( 'NONE',  ( 4.257384923554908163, -47.76562500047794657, 33.01645438728532866 ) ) ;
#2471=CARTESIAN_POINT ( 'NONE',  ( 7.757384923554905498, -50.28062499990439704, 29.19375250200204164 ) ) ;
#2476=DIRECTION ( 'NONE',  ( -0.000000000000000000, -1.000000000000000000, -0.000000000000000000 ) ) ;
#2477=CARTESIAN_POINT ( 'NONE',  ( 7.757384923554904610, -45.90208333428923737, 27.17302655983835180 ) ) ;
#2505=CARTESIAN_POINT ( 'NONE',  ( 1.556814259774676801, -48.24719997713471997, 26.92547815095636565 ) ) ;
#2509=CARTESIAN_POINT ( 'NONE',  ( 6.007384923554907274, -48.66666666666665719, 26.16266358875650866 ) ) ;
#2513=ADVANCED_FACE ( 'NONE', ( #23374 ), #19540, .T. ) ;
#2521=CARTESIAN_POINT ( 'NONE',  ( 4.257384923554909051, -44.12499999999999289, 25.69375250200204519 ) ) ;
#2524=ORIENTED_EDGE ( 'NONE', *, *, #39671, .F. ) ;
#2526=CARTESIAN_POINT ( 'NONE',  ( 4.257384923554908163, -44.67812500047794799, 33.01645438728532866 ) ) ;
#2546=( BOUNDED_SURFACE ( )  B_SPLINE_SURFACE ( 1, 2, ( 
 ( #15602, #35366, #19204, #6018, #18995, #12185, #5814, #19411, #22186, #25178, #2617, #2830, #41972, #9423, #15817, #28762, #35155, #31746, #38556, #3040, #16033, #12614, #25596, #22388, #6228, #38138, #12820, #32384, #38768, #21971, #32177, #28560, #9638, #3246, #41129, #11976, #24970, #8793, #31543, #13032, #23224, #26223, #35783, #23016, #23667, #29604, #26012, #20468, #4081, #36191, #23452, #3657, #257, #10052, #36415, #39820, #7063, #17062, #38977, #16854, #30030, #16646, #7282, #20252, #10257, #36630, #19821, #33215, #3875, #10471, #39596, #26635, #3448, #29387, #10683, #900, #39173, #13871, #32788, #6850, #26851, #468, #7492, #33433, #20043, #16233, #13441, #32583, #33007, #13241, #29174, #35982, #6645, #51, #29818, #9856, #26424, #16438, #681, #22813, #19609, #39381, #4920, #21503, #24497, #14298, #11504, #20885, #37063, #40646, #7917, #27677, #37466, #8114, #8320, #4717, #20681, #21091, #1324, #8528, #27275, #36845, #1737, #34064, #21300, #17493, #33658, #40450, #11306, #17900, #30874, #14718, #4298, #24706, #24288, #14508, #4511, #17280, #34269, #30454, #30245, #5131, #14912, #40238, #11108, #1117, #37260, #24092, #11710, #18109, #37669, #1530, #27061, #40856, #23879, #33856, #31079, #30664, #1933, #27880, #14089, #40026, #27481, #10897, #7705, #28503, #21706, #8941, #9154, #6176, #15757, #12343, #22131, #15548, #25120, #2774, #9370, #22334, #41494, #35103, #5963, #18938, #5547, #19150, #41921, #32121, #8732, #38505, #21913, #34682, #34891, #38084, #12124, #5759, #28709, #31696, #31281, #25330, #2357, #11923, #41281, #12769, #18735, #2141, #38715, #35312, #38288, #41703, #2565, #18522, #28297, #12557, #15976, #31905, #2984, #15128, #25544, #28924, #25750, #9586, #34475, #5333, #18308, #28090, #41071, #24915, #37874, #31489, #15347, #6385, #19358, #25962, #38926, #2, #12981, #16186, #22544, #35527, #32333 ),
 ( #3200, #19752, #16369, #3582, #398, #32935, #18667, #31835, #18871, #11992, #15195, #31144, #11781, #20747, #24777, #1080, #30833, #4679, #20641, #5509, #40310, #38788, #3266, #26245, #704, #37902, #28136, #9204, #8991, #21756, #41329, #2406, #5597, #28345, #34729, #28968, #41542, #18569, #18782, #25381, #12395, #31537, #22595, #31954, #12813, #41123, #38341, #32377, #6434, #22179, #9633, #3240, #35149, #31740, #6011, #2610, #12178, #15595, #34939, #28554, #22381, #35360, #18988, #41965, #38550, #25796, #5808, #2824, #11971, #15393, #25169, #32169, #15809, #3033, #28756, #35571, #8783, #16026, #41752, #12608, #38133, #25590, #24965, #21964, #9417, #6223, #19197, #37924, #38762, #19405, #7486, #16845, #33208, #249, #33000, #3868, #29808, #38970, #39814, #10045, #13432, #10677, #23008, #673, #3441, #35977, #39164, #13863, #7055, #13647, #39589, #19814, #16638, #6842, #30022, #32574, #20246, #3649, #16432, #29597, #32781, #461, #26417, #10463, #39372, #13026, #23217, #26217, #35777, #10248, #23661, #36184, #26006, #20460, #4072, #20035, #23443, #26628, #13231, #36408, #7274, #36622, #17056, #894, #9848, #26843, #33427, #16224, #29168, #46, #22805, #6637, #19601, #29380, #34059, #40641, #27671, #14713, #33651, #17486, #27875, #24491, #14290, #11498, #20879, #37053, #37460, #7911, #8315, #21295, #8108, #34264, #4710, #20673, #21085, #1316, #8521, #27269, #36838, #1731, #4915, #5125, #30447, #4505, #40440, #11299, #17896, #30869, #18104, #21498, #24702, #24282, #14502, #40232, #4292, #31074, #11101, #17273, #1927, #14906, #24085, #33850, #1111, #37254, #17690, #11705, #40851, #37664, #1524, #27055, #30236, #23874, #30658, #14083, #27473, #40020, #10889, #7699, #25325, #18517, #41276, #28919, #28496, #21700, #8936, #9149, #6170, #15753, #12338, #22125, #15543, #25114, #2768, #9365, #22330, #41489, #35097, #5959, #18932 ) ),
 .UNSPECIFIED., .F., .F., .T. ) 
 B_SPLINE_SURFACE_WITH_KNOTS ( ( 2, 2 ),
 ( 3, 2, 2, 2, 2, 2, 2, 2, 2, 2, 2, 2, 2, 2, 2, 2, 2, 2, 2, 2, 2, 2, 2, 2, 2, 2, 2, 2, 2, 2, 2, 2, 2, 2, 2, 2, 2, 2, 2, 2, 2, 2, 2, 2, 2, 2, 2, 2, 2, 2, 2, 2, 2, 2, 2, 2, 2, 2, 2, 2, 2, 2, 2, 2, 2, 2, 2, 2, 2, 2, 2, 2, 2, 2, 2, 2, 2, 2, 2, 2, 2, 2, 2, 2, 2, 2, 2, 2, 2, 2, 2, 2, 2, 2, 2, 2, 2, 2, 2, 2, 2, 2, 2, 2, 2, 2, 2, 2, 2, 2, 2, 2, 2, 2, 2, 2, 2, 2, 2, 3 ),
 ( 0.000000000000000000, 1.000000000000000000 ),
 ( 0.000000000000000000, 0.008333333333333333218, 0.01666666666666666644, 0.02500000000000000139, 0.03333333333333333287, 0.04166666666666666435, 0.05000000000000000278, 0.05833333333333333426, 0.06666666666666666574, 0.07499999999999999722, 0.08333333333333332871, 0.09166666666666666019, 0.1000000000000000056, 0.1083333333333333370, 0.1166666666666666685, 0.1250000000000000000, 0.1333333333333333315, 0.1416666666666666630, 0.1499999999999999944, 0.1583333333333333259, 0.1666666666666666574, 0.1749999999999999889, 0.1833333333333333204, 0.1916666666666666796, 0.2000000000000000111, 0.2083333333333333426, 0.2166666666666666741, 0.2250000000000000056, 0.2333333333333333370, 0.2416666666666666685, 0.2500000000000000000, 0.2583333333333333592, 0.2666666666666666630, 0.2750000000000000222, 0.2833333333333333259, 0.2916666666666666852, 0.2999999999999999889, 0.3083333333333333481, 0.3166666666666666519, 0.3250000000000000111, 0.3333333333333333148, 0.3416666666666666741, 0.3499999999999999778, 0.3583333333333333370, 0.3666666666666666408, 0.3750000000000000000, 0.3833333333333333592, 0.3916666666666666630, 0.4000000000000000222, 0.4083333333333333259, 0.4166666666666666852, 0.4249999999999999889, 0.4333333333333333481, 0.4416666666666666519, 0.4500000000000000111, 0.4583333333333333148, 0.4666666666666666741, 0.4749999999999999778, 0.4833333333333333370, 0.4916666666666666408, 0.5000000000000000000, 0.5083333333333333037, 0.5166666666666667185, 0.5250000000000000222, 0.5333333333333333259, 0.5416666666666666297, 0.5500000000000000444, 0.5583333333333333481, 0.5666666666666666519, 0.5749999999999999556, 0.5833333333333333703, 0.5916666666666666741, 0.5999999999999999778, 0.6083333333333332815, 0.6166666666666666963, 0.6250000000000000000, 0.6333333333333333037, 0.6416666666666667185, 0.6500000000000000222, 0.6583333333333333259, 0.6666666666666666297, 0.6750000000000000444, 0.6833333333333333481, 0.6916666666666666519, 0.6999999999999999556, 0.7083333333333333703, 0.7166666666666666741, 0.7249999999999999778, 0.7333333333333332815, 0.7416666666666666963, 0.7500000000000000000, 0.7583333333333333037, 0.7666666666666667185, 0.7750000000000000222, 0.7833333333333333259, 0.7916666666666666297, 0.8000000000000000444, 0.8083333333333333481, 0.8166666666666666519, 0.8249999999999999556, 0.8333333333333333703, 0.8416666666666666741, 0.8499999999999999778, 0.8583333333333332815, 0.8666666666666666963, 0.8750000000000000000, 0.8833333333333333037, 0.8916666666666667185, 0.9000000000000000222, 0.9083333333333333259, 0.9166666666666666297, 0.9250000000000000444, 0.9333333333333333481, 0.9416666666666666519, 0.9499999999999999556, 0.9583333333333333703, 0.9666666666666666741, 0.9749999999999999778, 0.9833333333333332815, 0.9845488016436918510 ),
 .UNSPECIFIED. ) 
 GEOMETRIC_REPRESENTATION_ITEM ( )  RATIONAL_B_SPLINE_SURFACE ( (
 ( 1.000000000000000000, 0.8660254037844387076, 1.000000000000000000, 0.8660254037844387076, 1.000000000000000000, 0.8660254037844387076, 1.000000000000000000, 0.8660254037844387076, 1.000000000000000000, 0.8660254037844387076, 1.000000000000000000, 0.8660254037844387076, 1.000000000000000000, 0.8660254037844387076, 1.000000000000000000, 0.8660254037844387076, 1.000000000000000000, 0.8660254037844387076, 1.000000000000000000, 0.8660254037844387076, 1.000000000000000000, 0.8660254037844387076, 1.000000000000000000, 0.8660254037844387076, 1.000000000000000000, 0.8660254037844387076, 1.000000000000000000, 0.8660254037844387076, 1.000000000000000000, 0.8660254037844387076, 1.000000000000000000, 0.8660254037844387076, 1.000000000000000000, 0.8660254037844387076, 1.000000000000000000, 0.8660254037844387076, 1.000000000000000000, 0.8660254037844387076, 1.000000000000000000, 0.8660254037844387076, 1.000000000000000000, 0.8660254037844387076, 1.000000000000000000, 0.8660254037844387076, 1.000000000000000000, 0.8660254037844387076, 1.000000000000000000, 0.8660254037844387076, 1.000000000000000000, 0.8660254037844387076, 1.000000000000000000, 0.8660254037844387076, 1.000000000000000000, 0.8660254037844387076, 1.000000000000000000, 0.8660254037844387076, 1.000000000000000000, 0.8660254037844387076, 1.000000000000000000, 0.8660254037844387076, 1.000000000000000000, 0.8660254037844387076, 1.000000000000000000, 0.8660254037844387076, 1.000000000000000000, 0.8660254037844387076, 1.000000000000000000, 0.8660254037844387076, 1.000000000000000000, 0.8660254037844387076, 1.000000000000000000, 0.8660254037844387076, 1.000000000000000000, 0.8660254037844387076, 1.000000000000000000, 0.8660254037844387076, 1.000000000000000000, 0.8660254037844387076, 1.000000000000000000, 0.8660254037844387076, 1.000000000000000000, 0.8660254037844387076, 1.000000000000000000, 0.8660254037844387076, 1.000000000000000000, 0.8660254037844387076, 1.000000000000000000, 0.8660254037844387076, 1.000000000000000000, 0.8660254037844387076, 1.000000000000000000, 0.8660254037844387076, 1.000000000000000000, 0.8660254037844387076, 1.000000000000000000, 0.8660254037844387076, 1.000000000000000000, 0.8660254037844387076, 1.000000000000000000, 0.8660254037844387076, 1.000000000000000000, 0.8660254037844387076, 1.000000000000000000, 0.8660254037844387076, 1.000000000000000000, 0.8660254037844387076, 1.000000000000000000, 0.8660254037844387076, 1.000000000000000000, 0.8660254037844387076, 1.000000000000000000, 0.8660254037844387076, 1.000000000000000000, 0.8660254037844387076, 1.000000000000000000, 0.8660254037844387076, 1.000000000000000000, 0.8660254037844387076, 1.000000000000000000, 0.8660254037844387076, 1.000000000000000000, 0.8660254037844387076, 1.000000000000000000, 0.8660254037844387076, 1.000000000000000000, 0.8660254037844387076, 1.000000000000000000, 0.8660254037844387076, 1.000000000000000000, 0.8660254037844387076, 1.000000000000000000, 0.8660254037844387076, 1.000000000000000000, 0.8660254037844387076, 1.000000000000000000, 0.8660254037844387076, 1.000000000000000000, 0.8660254037844387076, 1.000000000000000000, 0.8660254037844387076, 1.000000000000000000, 0.8660254037844387076, 1.000000000000000000, 0.8660254037844387076, 1.000000000000000000, 0.8660254037844387076, 1.000000000000000000, 0.8660254037844387076, 1.000000000000000000, 0.8660254037844387076, 1.000000000000000000, 0.8660254037844387076, 1.000000000000000000, 0.8660254037844387076, 1.000000000000000000, 0.8660254037844387076, 1.000000000000000000, 0.8660254037844387076, 1.000000000000000000, 0.8660254037844387076, 1.000000000000000000, 0.8660254037844387076, 1.000000000000000000, 0.8660254037844387076, 1.000000000000000000, 0.8660254037844387076, 1.000000000000000000, 0.8660254037844387076, 1.000000000000000000, 0.8660254037844387076, 1.000000000000000000, 0.8660254037844387076, 1.000000000000000000, 0.8660254037844387076, 1.000000000000000000, 0.8660254037844387076, 1.000000000000000000, 0.8660254037844387076, 1.000000000000000000, 0.8660254037844387076, 1.000000000000000000, 0.8660254037844387076, 1.000000000000000000, 0.8660254037844387076, 1.000000000000000000, 0.8660254037844387076, 1.000000000000000000, 0.8660254037844387076, 1.000000000000000000, 0.8660254037844387076, 1.000000000000000000, 0.8660254037844387076, 1.000000000000000000, 0.8660254037844387076, 1.000000000000000000, 0.8660254037844387076, 1.000000000000000000, 0.8660254037844387076, 1.000000000000000000, 0.8660254037844387076, 1.000000000000000000, 0.8660254037844387076, 1.000000000000000000, 0.8660254037844387076, 1.000000000000000000, 0.8660254037844387076, 1.000000000000000000, 0.8660254037844387076, 1.000000000000000000, 0.8660254037844387076, 1.000000000000000000, 0.8660254037844387076, 1.000000000000000000, 0.8660254037844387076, 1.000000000000000000, 0.8660254037844387076, 1.000000000000000000, 0.8660254037844387076, 1.000000000000000000, 0.8660254037844387076, 1.000000000000000000, 0.8660254037844387076, 1.000000000000000000, 0.8660254037844387076, 1.000000000000000000, 0.8660254037844387076, 1.000000000000000000, 0.8660254037844387076, 1.000000000000000000, 0.8660254037844387076, 1.000000000000000000, 0.8660254037844387076, 1.000000000000000000, 0.8660254037844387076, 1.000000000000000000, 0.8660254037844387076, 1.000000000000000000, 0.9804589748688282702, 0.9666183089693827224),
 ( 1.000000000000000000, 0.8660254037844387076, 1.000000000000000000, 0.8660254037844387076, 1.000000000000000000, 0.8660254037844387076, 1.000000000000000000, 0.8660254037844387076, 1.000000000000000000, 0.8660254037844387076, 1.000000000000000000, 0.8660254037844387076, 1.000000000000000000, 0.8660254037844387076, 1.000000000000000000, 0.8660254037844387076, 1.000000000000000000, 0.8660254037844387076, 1.000000000000000000, 0.8660254037844387076, 1.000000000000000000, 0.8660254037844387076, 1.000000000000000000, 0.8660254037844387076, 1.000000000000000000, 0.8660254037844387076, 1.000000000000000000, 0.8660254037844387076, 1.000000000000000000, 0.8660254037844387076, 1.000000000000000000, 0.8660254037844387076, 1.000000000000000000, 0.8660254037844387076, 1.000000000000000000, 0.8660254037844387076, 1.000000000000000000, 0.8660254037844387076, 1.000000000000000000, 0.8660254037844387076, 1.000000000000000000, 0.8660254037844387076, 1.000000000000000000, 0.8660254037844387076, 1.000000000000000000, 0.8660254037844387076, 1.000000000000000000, 0.8660254037844387076, 1.000000000000000000, 0.8660254037844387076, 1.000000000000000000, 0.8660254037844387076, 1.000000000000000000, 0.8660254037844387076, 1.000000000000000000, 0.8660254037844387076, 1.000000000000000000, 0.8660254037844387076, 1.000000000000000000, 0.8660254037844387076, 1.000000000000000000, 0.8660254037844387076, 1.000000000000000000, 0.8660254037844387076, 1.000000000000000000, 0.8660254037844387076, 1.000000000000000000, 0.8660254037844387076, 1.000000000000000000, 0.8660254037844387076, 1.000000000000000000, 0.8660254037844387076, 1.000000000000000000, 0.8660254037844387076, 1.000000000000000000, 0.8660254037844387076, 1.000000000000000000, 0.8660254037844387076, 1.000000000000000000, 0.8660254037844387076, 1.000000000000000000, 0.8660254037844387076, 1.000000000000000000, 0.8660254037844387076, 1.000000000000000000, 0.8660254037844387076, 1.000000000000000000, 0.8660254037844387076, 1.000000000000000000, 0.8660254037844387076, 1.000000000000000000, 0.8660254037844387076, 1.000000000000000000, 0.8660254037844387076, 1.000000000000000000, 0.8660254037844387076, 1.000000000000000000, 0.8660254037844387076, 1.000000000000000000, 0.8660254037844387076, 1.000000000000000000, 0.8660254037844387076, 1.000000000000000000, 0.8660254037844387076, 1.000000000000000000, 0.8660254037844387076, 1.000000000000000000, 0.8660254037844387076, 1.000000000000000000, 0.8660254037844387076, 1.000000000000000000, 0.8660254037844387076, 1.000000000000000000, 0.8660254037844387076, 1.000000000000000000, 0.8660254037844387076, 1.000000000000000000, 0.8660254037844387076, 1.000000000000000000, 0.8660254037844387076, 1.000000000000000000, 0.8660254037844387076, 1.000000000000000000, 0.8660254037844387076, 1.000000000000000000, 0.8660254037844387076, 1.000000000000000000, 0.8660254037844387076, 1.000000000000000000, 0.8660254037844387076, 1.000000000000000000, 0.8660254037844387076, 1.000000000000000000, 0.8660254037844387076, 1.000000000000000000, 0.8660254037844387076, 1.000000000000000000, 0.8660254037844387076, 1.000000000000000000, 0.8660254037844387076, 1.000000000000000000, 0.8660254037844387076, 1.000000000000000000, 0.8660254037844387076, 1.000000000000000000, 0.8660254037844387076, 1.000000000000000000, 0.8660254037844387076, 1.000000000000000000, 0.8660254037844387076, 1.000000000000000000, 0.8660254037844387076, 1.000000000000000000, 0.8660254037844387076, 1.000000000000000000, 0.8660254037844387076, 1.000000000000000000, 0.8660254037844387076, 1.000000000000000000, 0.8660254037844387076, 1.000000000000000000, 0.8660254037844387076, 1.000000000000000000, 0.8660254037844387076, 1.000000000000000000, 0.8660254037844387076, 1.000000000000000000, 0.8660254037844387076, 1.000000000000000000, 0.8660254037844387076, 1.000000000000000000, 0.8660254037844387076, 1.000000000000000000, 0.8660254037844387076, 1.000000000000000000, 0.8660254037844387076, 1.000000000000000000, 0.8660254037844387076, 1.000000000000000000, 0.8660254037844387076, 1.000000000000000000, 0.8660254037844387076, 1.000000000000000000, 0.8660254037844387076, 1.000000000000000000, 0.8660254037844387076, 1.000000000000000000, 0.8660254037844387076, 1.000000000000000000, 0.8660254037844387076, 1.000000000000000000, 0.8660254037844387076, 1.000000000000000000, 0.8660254037844387076, 1.000000000000000000, 0.8660254037844387076, 1.000000000000000000, 0.8660254037844387076, 1.000000000000000000, 0.8660254037844387076, 1.000000000000000000, 0.8660254037844387076, 1.000000000000000000, 0.8660254037844387076, 1.000000000000000000, 0.8660254037844387076, 1.000000000000000000, 0.8660254037844387076, 1.000000000000000000, 0.8660254037844387076, 1.000000000000000000, 0.8660254037844387076, 1.000000000000000000, 0.8660254037844387076, 1.000000000000000000, 0.8660254037844387076, 1.000000000000000000, 0.8660254037844387076, 1.000000000000000000, 0.8660254037844387076, 1.000000000000000000, 0.8660254037844387076, 1.000000000000000000, 0.8660254037844387076, 1.000000000000000000, 0.8660254037844387076, 1.000000000000000000, 0.8660254037844387076, 1.000000000000000000, 0.8660254037844387076, 1.000000000000000000, 0.8660254037844387076, 1.000000000000000000, 0.8660254037844387076, 1.000000000000000000, 0.8660254037844387076, 1.000000000000000000, 0.9804589748688282702, 0.9666183089693827224) ) ) 
 REPRESENTATION_ITEM ( '' )  SURFACE ( )  );
#2548=CARTESIAN_POINT ( 'NONE',  ( 6.009348476549478235, -45.52703728045461418, 32.22392412845276510 ) ) ;
#2552=CARTESIAN_POINT ( 'NONE',  ( 1.132195812467071461, -45.65678379089349193, 30.77036467654158258 ) ) ;
#2562=CARTESIAN_POINT ( 'NONE',  ( 7.341567464759685357, -49.40455516506535361, 27.48546486168072533 ) ) ;
#2565=CARTESIAN_POINT ( 'NONE',  ( 2.602106451679912169, -43.47395833381127517, 26.32672608803957459 ) ) ;
#2566=CARTESIAN_POINT ( 'NONE',  ( 2.602106451679911281, -45.38645833381128369, 26.32672608803957459 ) ) ;
#2573=CARTESIAN_POINT ( 'NONE',  ( 5.647996821765916664, -47.03809886738047652, 32.42459398907978141 ) ) ;
#2574=CARTESIAN_POINT ( 'NONE',  ( 0.7573849235549129366, -43.99999999999999289, 29.19375250200204164 ) ) ;
#2575=CARTESIAN_POINT ( 'NONE',  ( 5.912663395429907709, -45.05729166714461797, 26.32672608803957459 ) ) ;
#2580=CARTESIAN_POINT ( 'NONE',  ( 2.507384923554909495, -51.91666666666665719, 32.22484141524756751 ) ) ;
#2610=CARTESIAN_POINT ( 'NONE',  ( 0.7573849235549120484, -49.95833333333332860, 31.21447844416572792 ) ) ;
#2617=CARTESIAN_POINT ( 'NONE',  ( 5.912663395429904156, -51.72395833381127517, 32.06077891596451224 ) ) ;
#2621=CARTESIAN_POINT ( 'NONE',  ( 3.776403311941112229, -51.07899062695563686, 32.67001192764423223 ) ) ;
#2624=CARTESIAN_POINT ( 'NONE',  ( 0.7573849235549129366, -43.53062499990439704, 29.19375250200204164 ) ) ;
#2626=ORIENTED_EDGE ( 'NONE', *, *, #14685, .F. ) ;
#2628=CARTESIAN_POINT ( 'NONE',  ( 4.242209996576106867, -43.81838871691699921, 25.69378328369220199 ) ) ;
#2630=CARTESIAN_POINT ( 'NONE',  ( 7.567941867304904591, -47.59479166714461940, 31.10510344464368870 ) ) ;
#2632=CARTESIAN_POINT ( 'NONE',  ( 0.7925744004279580146, -48.68303981060392260, 29.69411625405754762 ) ) ;
#2634=CARTESIAN_POINT ( 'NONE',  ( 0.7573849235549120484, -51.15208333428923737, 31.21447844416572792 ) ) ;
#2664=CARTESIAN_POINT ( 'NONE',  ( 5.912663395429907709, -49.05729166714461087, 26.32672608803957459 ) ) ;
#2672=CARTESIAN_POINT ( 'NONE',  ( 7.757384923554905498, -51.94375000095590877, 29.19375250200204164 ) ) ;
#2679=CARTESIAN_POINT ( 'NONE',  ( 2.507384923554909495, -49.94729166657106845, 32.22484141524756751 ) ) ;
#2686=CARTESIAN_POINT ( 'NONE',  ( 4.257384923554909051, -45.81875000095590877, 25.15230061767466552 ) ) ;
#2701=DIRECTION ( 'NONE',  ( -0.000000000000000000, -1.000000000000000000, -0.000000000000000000 ) ) ;
#2714=CARTESIAN_POINT ( 'NONE',  ( 4.257384923554907274, -45.37499999999999289, 32.69375250200203453 ) ) ;
#2726=CARTESIAN_POINT ( 'NONE',  ( 6.047313250368883786, -48.02612826763341047, 32.20173675254635981 ) ) ;
#2736=CARTESIAN_POINT ( 'NONE',  ( 2.602106451679911281, -44.38645833381128369, 26.32672608803957459 ) ) ;
#2737=CARTESIAN_POINT ( 'NONE',  ( 6.837589543544248194, -42.38018344428898132, 26.64198244958982897 ) ) ;
#2768=CARTESIAN_POINT ( 'NONE',  ( 2.507384923554911715, -42.58333333333332149, 26.16266358875650866 ) ) ;
#2774=CARTESIAN_POINT ( 'NONE',  ( 0.9468279798049124008, -44.84895833381128227, 31.10510344464368515 ) ) ;
#2775=CARTESIAN_POINT ( 'NONE',  ( 7.567941867304902814, -44.59479166714461940, 31.10510344464368870 ) ) ;
#2780=ORIENTED_EDGE ( 'NONE', *, *, #23267, .F. ) ;
#2785=EDGE_CURVE ( 'NONE', #15067, #29243, #1865, .T. ) ;
#2786=CARTESIAN_POINT ( 'NONE',  ( 0.7573849235549138248, -51.23541666762257307, 27.17302655983835180 ) ) ;
#2787=CARTESIAN_POINT ( 'NONE',  ( 2.602106451679912169, -44.47395833381127517, 26.32672608803957459 ) ) ;
#2793=DIRECTION ( 'NONE',  ( 0.000000000000000000, 0.000000000000000000, 1.000000000000000000 ) ) ;
#2802=EDGE_CURVE ( 'NONE', #16017, #3008, #25046, .T. ) ;
#2822=CARTESIAN_POINT ( 'NONE',  ( 7.666287271702439732, -47.46382790796208440, 30.10987722856529558 ) ) ;
#2824=CARTESIAN_POINT ( 'NONE',  ( 0.7573849235549120484, -49.45833333333332860, 31.21447844416572792 ) ) ;
#2827=CARTESIAN_POINT ( 'NONE',  ( 4.257384923554909051, -52.12499999999999289, 25.69375250200204519 ) ) ;
#2830=CARTESIAN_POINT ( 'NONE',  ( 7.567941867304902814, -51.68229166714461797, 31.10510344464368870 ) ) ;
#2834=AXIS2_PLACEMENT_3D ( 'NONE', #19497, #3531, #22690 ) ;
#2838=CARTESIAN_POINT ( 'NONE',  ( 7.757384923554902834, -50.29166666666665719, 31.21447844416572792 ) ) ;
#2840=CARTESIAN_POINT ( 'NONE',  ( 0.7268877558064784639, -43.69438581936281452, 29.06119947735034259 ) ) ;
#2842=CARTESIAN_POINT ( 'NONE',  ( 7.567941867304905479, -47.51145833381127659, 27.28240155936039812 ) ) ;
#2862=CARTESIAN_POINT ( 'NONE',  ( 6.007384923554907274, -46.66666666666665719, 26.16266358875650866 ) ) ;
#2875=ORIENTED_EDGE ( 'NONE', *, *, #32343, .T. ) ;
#2877=CARTESIAN_POINT ( 'NONE',  ( 7.567941867304904591, -48.64062500047794657, 29.19375250200204164 ) ) ;
#2884=CARTESIAN_POINT ( 'NONE',  ( 0.9468279798049117346, -49.26145833381128369, 31.10510344464368515 ) ) ;
#2889=VERTEX_POINT ( 'NONE', #5475 ) ;
#2890=CARTESIAN_POINT ( 'NONE',  ( 7.757384923554902834, -50.82229166657106845, 31.21447844416572792 ) ) ;
#2892=ORIENTED_EDGE ( 'NONE', *, *, #27234, .F. ) ;
#2896=CARTESIAN_POINT ( 'NONE',  ( 0.7573849235549120484, -46.65208333428924448, 31.21447844416572792 ) ) ;
#2902=LINE ( 'NONE', #12689, #15598 ) ;
#2927=CARTESIAN_POINT ( 'NONE',  ( 4.148859949529951407, -48.31637102562046948, 25.69375249836358321 ) ) ;
#2932=CARTESIAN_POINT ( 'NONE',  ( 7.567941867304905479, -47.01145833381128369, 27.28240155936039812 ) ) ;
#2940=CARTESIAN_POINT ( 'NONE',  ( 7.339640309704016374, -47.90455601427180454, 27.53361210857719499 ) ) ;
#2951=CARTESIAN_POINT ( 'NONE',  ( 2.507384923554909495, -42.11041666762257307, 32.22484141524756751 ) ) ;
#2974=CARTESIAN_POINT ( 'NONE',  ( 0.9528598946248513224, -45.66750498230493349, 30.35411025554243380 ) ) ;
#2982=CARTESIAN_POINT ( 'NONE',  ( 1.021869656056290321, -42.66324832057951966, 30.58238150993415161 ) ) ;
#2984=CARTESIAN_POINT ( 'NONE',  ( 5.912663395429904156, -43.22395833381127517, 32.06077891596451224 ) ) ;
#2985=CARTESIAN_POINT ( 'NONE',  ( 7.567941867304905479, -45.55312500047794799, 29.19375250200204164 ) ) ;
#2991=VERTEX_POINT ( 'NONE', #12704 ) ;
#2996=CARTESIAN_POINT ( 'NONE',  ( 0.9468279798049132889, -46.39062500047794657, 29.19375250200204164 ) ) ;
#3008=VERTEX_POINT ( 'NONE', #12489 ) ;
#3030=CARTESIAN_POINT ( 'NONE',  ( 1.014226666565541057, -47.22696855243463432, 27.79397413955463847 ) ) ;
#3033=CARTESIAN_POINT ( 'NONE',  ( 7.757384923554904610, -49.20833333333333570, 27.17302655983835180 ) ) ;
#3034=VERTEX_POINT ( 'NONE', #35239 ) ;
#3039=CARTESIAN_POINT ( 'NONE',  ( 4.445535741605620039, -43.32283183689707329, 25.69808885611207927 ) ) ;
#3040=CARTESIAN_POINT ( 'NONE',  ( 0.9468279798049124008, -51.34895833381127517, 31.10510344464368515 ) ) ;
#3048=CARTESIAN_POINT ( 'NONE',  ( 7.757384923554904610, -50.70833333333332860, 27.17302655983835180 ) ) ;
#3051=CARTESIAN_POINT ( 'NONE',  ( 4.257363451562580003, -43.56959840651998661, 32.69375250187801640 ) ) ;
#3054=CARTESIAN_POINT ( 'NONE',  ( 4.257384923554908163, -49.17812500047794799, 33.01645438728532866 ) ) ;
#3057=CARTESIAN_POINT ( 'NONE',  ( 0.7623779362210003629, -48.68963102019149147, 29.39103142152722725 ) ) ;
#3075=CARTESIAN_POINT ( 'NONE',  ( 0.7573849235549120484, -42.45833333333332860, 31.21447844416572792 ) ) ;
#3091=CARTESIAN_POINT ( 'NONE',  ( 4.257384923554909051, -47.01562500047794657, 25.37105061671875461 ) ) ;
#3097=CARTESIAN_POINT ( 'NONE',  ( 0.9468279798049134000, -49.34479166714461940, 27.28240155936039102 ) ) ;
#3105=CARTESIAN_POINT ( 'NONE',  ( 0.7573849235549120484, -48.98895833323773275, 31.21447844416572792 ) ) ;
#3111=CARTESIAN_POINT ( 'NONE',  ( 2.507384923554911715, -45.27708333428923737, 26.16266358875650866 ) ) ;
#3114=CARTESIAN_POINT ( 'NONE',  ( 2.507384923554909495, -42.91666666666665719, 32.22484141524756751 ) ) ;
#3125=CARTESIAN_POINT ( 'NONE',  ( 5.195207097063835988, -51.85267090063072715, 32.69375250200204164 ) ) ;
#3128=CARTESIAN_POINT ( 'NONE',  ( 3.083769392894965211, -51.59668766289245667, 32.53393153047227315 ) ) ;
#3138=EDGE_CURVE ( 'NONE', #34951, #25326, #6939, .T. ) ;
#3145=CARTESIAN_POINT ( 'NONE',  ( 0.7675909832832559232, -46.18811830847105426, 29.46102386014162988 ) ) ;
#3146=CARTESIAN_POINT ( 'NONE',  ( 5.912663395429907709, -45.46979166714461229, 26.32672608803957459 ) ) ;
#3162=CARTESIAN_POINT ( 'NONE',  ( 4.222636998834624400, -50.81798717800577947, 25.69391422978443984 ) ) ;
#3171=( BOUNDED_CURVE ( )  B_SPLINE_CURVE ( 2, ( #32210, #82, #25418, #38383, #25836, #3075, #35813, #22844, #10084 ),
 .UNSPECIFIED., .F., .F. ) 
 B_SPLINE_CURVE_WITH_KNOTS ( ( 3, 2, 2, 2, 3 ),
 ( 0.9625000000000000222, 0.9666666666666666741, 0.9749999999999999778, 0.9833333333333332815, 0.9845488016436918510 ),
 .UNSPECIFIED. ) 
 CURVE ( )  GEOMETRIC_REPRESENTATION_ITEM ( )  RATIONAL_B_SPLINE_CURVE ( ( 0.9330127018922194093, 0.9330127018922194093, 1.000000000000000000, 0.8660254037844387076, 1.000000000000000000, 0.8660254037844387076, 1.000000000000000000, 0.9804589748688282702, 0.9666183089693827224 ) ) 
 REPRESENTATION_ITEM ( '' )  );
#3189=CARTESIAN_POINT ( 'NONE',  ( 0.7573849235549120484, -50.95833333333332860, 31.21447844416572792 ) ) ;
#3195=CARTESIAN_POINT ( 'NONE',  ( 4.257384923554909051, 0.8500000000000035305, 29.19375250200204164 ) ) ;
#3197=CARTESIAN_POINT ( 'NONE',  ( 0.7573865785542123197, -42.68739215929544883, 29.50208360792847628 ) ) ;
#3200=CARTESIAN_POINT ( 'NONE',  ( 7.757384923554905498, -52.24999999999999289, 29.19375250200204164 ) ) ;
#3201=CARTESIAN_POINT ( 'NONE',  ( 7.567941867304905479, -45.01145833381128369, 27.28240155936039457 ) ) ;
#3207=CARTESIAN_POINT ( 'NONE',  ( 4.257364757503538932, -47.06955867894671286, 32.69375250189110460 ) ) ;
#3208=CARTESIAN_POINT ( 'NONE',  ( 2.602106451679912169, -44.97395833381127517, 26.32672608803957459 ) ) ;
#3216=ORIENTED_EDGE ( 'NONE', *, *, #32343, .F. ) ;
#3226=CARTESIAN_POINT ( 'NONE',  ( 4.257337177015303453, -43.31874891592651977, 25.69375250232772245 ) ) ;
#3237=CARTESIAN_POINT ( 'NONE',  ( 4.715551244148891818, -47.32907896923704527, 25.69375487964306259 ) ) ;
#3240=CARTESIAN_POINT ( 'NONE',  ( 4.257384923554909051, -50.12499999999999289, 25.15230061767466552 ) ) ;
#3245=CARTESIAN_POINT ( 'NONE',  ( 4.351448419358070474, -43.32078794482188044, 25.69483579731370426 ) ) ;
#3246=CARTESIAN_POINT ( 'NONE',  ( 4.257384923554908163, -50.76562500047794657, 33.01645438728532866 ) ) ;
#3250=EDGE_CURVE ( 'NONE', #8274, #8243, #16321, .T. ) ;
#3255=CARTESIAN_POINT ( 'NONE',  ( 7.757384923554904610, -49.20833333333333570, 27.17302655983835180 ) ) ;
#3256=CARTESIAN_POINT ( 'NONE',  ( 5.195207097063835988, -45.35267090063072715, 32.69375250200204164 ) ) ;
#3262=CARTESIAN_POINT ( 'NONE',  ( 4.058124613621689747, -48.81401115383377487, 25.69861542568218127 ) ) ;
#3265=CARTESIAN_POINT ( 'NONE',  ( 7.757384923554904610, -51.90208333428923737, 27.17302655983835180 ) ) ;
#3266=CARTESIAN_POINT ( 'NONE',  ( 6.007384923554904610, -51.33333333333332149, 32.22484141524757462 ) ) ;
#3280=CARTESIAN_POINT ( 'NONE',  ( 7.757384923554904610, -46.70833333333332149, 27.17302655983835180 ) ) ;
#3293=CARTESIAN_POINT ( 'NONE',  ( 7.567941867304904591, -46.64062500047794657, 29.19375250200204164 ) ) ;
#3297=CARTESIAN_POINT ( 'NONE',  ( 7.567941867304905479, -49.51145833381128369, 27.28240155936039457 ) ) ;
#3304=CARTESIAN_POINT ( 'NONE',  ( 2.507384923554911715, -48.11395833323773275, 26.16266358875650866 ) ) ;
#3306=B_SPLINE_CURVE_WITH_KNOTS ( 'NONE', 3,
 ( #16747, #22917, #151, #573, #13133, #26116 ),
 .UNSPECIFIED., .F., .F.,
 ( 4, 2, 4 ),
 ( 0.5000000000000000000, 0.5298504205087859464, 0.5597008410175718929 ),
 .UNSPECIFIED. ) ;
#3311=EDGE_CURVE ( 'NONE', #5487, #7185, #7363, .T. ) ;
#3313=CARTESIAN_POINT ( 'NONE',  ( 0.7573849235549129366, -43.69375000095590877, 29.19375250200204164 ) ) ;
#3315=EDGE_CURVE ( 'NONE', #27430, #27686, #7794, .T. ) ;
#3326=CARTESIAN_POINT ( 'NONE',  ( 4.257384923554907274, -50.37499999999998579, 32.69375250200203453 ) ) ;
#3348=CARTESIAN_POINT ( 'NONE',  ( 0.9468279798049125118, -46.30312500047794799, 29.19375250200204164 ) ) ;
#3366=EDGE_LOOP ( 'NONE', ( #37221, #18265, #31741, #20842 ) ) ;
#3367=CARTESIAN_POINT ( 'NONE',  ( 1.411003818924247089, -50.74352958133138713, 27.15693724216819405 ) ) ;
#3408=CARTESIAN_POINT ( 'NONE',  ( 4.257384923554909051, -45.51562500047795368, 25.37105061671875106 ) ) ;
#3413=VERTEX_POINT ( 'NONE', #25987 ) ;
#3437=CARTESIAN_POINT ( 'NONE',  ( 7.567941867304905479, -51.55312500047794799, 29.19375250200204164 ) ) ;
#3438=CARTESIAN_POINT ( 'NONE',  ( 1.240397744902267840, -47.23794492404785217, 27.35160661698481377 ) ) ;
#3441=CARTESIAN_POINT ( 'NONE',  ( 2.507384923554909495, -47.91666666666665719, 32.22484141524756751 ) ) ;
#3446=ORIENTED_EDGE ( 'NONE', *, *, #33733, .T. ) ;
#3448=CARTESIAN_POINT ( 'NONE',  ( 7.567941867304904591, -49.14062500047794657, 29.19375250200204164 ) ) ;
#3455=CARTESIAN_POINT ( 'NONE',  ( 0.7573849235549120484, -50.95833333333332860, 31.21447844416572792 ) ) ;
#3459=CARTESIAN_POINT ( 'NONE',  ( 3.869754523475995800, -43.57908220961675028, 32.69375235852697159 ) ) ;
#3463=CARTESIAN_POINT ( 'NONE',  ( 0.8629060653032183392, -48.67477004852683820, 30.06361894639907106 ) ) ;
#3466=CARTESIAN_POINT ( 'NONE',  ( 7.757384923554905498, -51.44375000095590877, 29.19375250200204164 ) ) ;
#3495=CARTESIAN_POINT ( 'NONE',  ( 5.912663395429904156, -44.22395833381127517, 32.06077891596451224 ) ) ;
#3499=CARTESIAN_POINT ( 'NONE',  ( 0.9468279798049134000, -50.84479166714461940, 27.28240155936039102 ) ) ;
#3504=VERTEX_POINT ( 'NONE', #38116 ) ;
#3506=CARTESIAN_POINT ( 'NONE',  ( 0.7573849235549138248, -47.57229166657106134, 27.17302655983835180 ) ) ;
#3513=CARTESIAN_POINT ( 'NONE',  ( 0.7573849235549129366, -44.19375000095590877, 29.19375250200204164 ) ) ;
#3514=CARTESIAN_POINT ( 'NONE',  ( 6.007384923554907274, -43.86041666762257307, 26.16266358875650866 ) ) ;
#3531=DIRECTION ( 'NONE',  ( 0.000000000000000000, 1.000000000000000000, 0.000000000000000000 ) ) ;
#3545=VERTEX_POINT ( 'NONE', #34921 ) ;
#3549=CARTESIAN_POINT ( 'NONE',  ( 0.9468279798049125118, -43.80312500047794799, 29.19375250200204164 ) ) ;
#3559=ORIENTED_EDGE ( 'NONE', *, *, #16803, .F. ) ;
#3567=ADVANCED_FACE ( 'NONE', ( #36602 ), #33407, .T. ) ;
#3568=CARTESIAN_POINT ( 'NONE',  ( 7.757384923554904610, -51.40208333428923027, 27.17302655983835180 ) ) ;
#3582=CARTESIAN_POINT ( 'NONE',  ( 4.257384923554909051, -52.12499999999999289, 25.15230061767466552 ) ) ;
#3591=CARTESIAN_POINT ( 'NONE',  ( 6.007384923554904610, -47.33333333333332149, 32.22484141524757462 ) ) ;
#3596=CARTESIAN_POINT ( 'NONE',  ( 7.056219122567421564, -49.99366238037033838, 31.34466569045931550 ) ) ;
#3597=AXIS2_PLACEMENT_3D ( 'NONE', #12270, #2701, #19701 ) ;
#3609=CARTESIAN_POINT ( 'NONE',  ( 2.602106451679909505, -43.21979166714461940, 32.06077891596451224 ) ) ;
#3621=CARTESIAN_POINT ( 'NONE',  ( 4.821113816375371286, -46.05532735902576036, 32.64833438017230094 ) ) ;
#3642=CARTESIAN_POINT ( 'NONE',  ( 4.257384923554909051, -41.90485061181026083, 23.69375250200204519 ) ) ;
#3646=CARTESIAN_POINT ( 'NONE',  ( 0.7275300099533476006, -47.19487547329910626, 29.18866630973243659 ) ) ;
#3649=CARTESIAN_POINT ( 'NONE',  ( 4.257384923554908163, -47.37499999999999289, 33.23520438632941421 ) ) ;
#3656=CARTESIAN_POINT ( 'NONE',  ( 6.911370815035220438, -43.38662813956295849, 26.91196816919017820 ) ) ;
#3657=CARTESIAN_POINT ( 'NONE',  ( 4.257384923554909051, -50.01562500047793947, 25.37105061671875461 ) ) ;
#3666=CARTESIAN_POINT ( 'NONE',  ( 0.7573849235549129366, -48.99999999999998579, 29.19375250200204164 ) ) ;
#3673=CARTESIAN_POINT ( 'NONE',  ( 4.257384923554909051, 0.8500000000000035305, 29.19375250200204164 ) ) ;
#3677=CARTESIAN_POINT ( 'NONE',  ( 0.7573849235549138248, -49.23541666762258018, 27.17302655983835180 ) ) ;
#3691=CARTESIAN_POINT ( 'NONE',  ( 4.024745194044820451, -44.81350275326456511, 25.70038836304057739 ) ) ;
#3693=CARTESIAN_POINT ( 'NONE',  ( 2.507384923554911715, -42.77708333428924448, 26.16266358875650866 ) ) ;
#3704=CARTESIAN_POINT ( 'NONE',  ( 0.9468279798049124008, -45.34895833381127517, 31.10510344464368515 ) ) ;
#3708=CARTESIAN_POINT ( 'NONE',  ( 4.257384923554909051, -50.42812500047796220, 25.37105061671875106 ) ) ;
#3711=ORIENTED_EDGE ( 'NONE', *, *, #35309, .F. ) ;
#3714=CARTESIAN_POINT ( 'NONE',  ( 2.507384923554911715, -47.11395833323773275, 26.16266358875650866 ) ) ;
#3722=CARTESIAN_POINT ( 'NONE',  ( 7.757384923554902834, -43.98541666762258018, 31.21447844416572792 ) ) ;
#3723=CARTESIAN_POINT ( 'NONE',  ( 2.507384923554909495, -44.11041666762257307, 32.22484141524756751 ) ) ;
#3733=DIRECTION ( 'NONE',  ( 0.000000000000000000, 0.7071067811865474617, 0.7071067811865474617 ) ) ;
#3762=CARTESIAN_POINT ( 'NONE',  ( 0.9468279798049134000, -43.84479166714461940, 27.28240155936039457 ) ) ;
#3771=CARTESIAN_POINT ( 'NONE',  ( 0.9145871159158894814, -42.40311593909473231, 28.11954587812425288 ) ) ;
#3782=CARTESIAN_POINT ( 'NONE',  ( 4.250209806777895061, -50.81859248301203991, 25.69375249668682315 ) ) ;
#3784=CARTESIAN_POINT ( 'NONE',  ( 0.7573849235549129366, -43.49999999999999289, 29.19375250200204164 ) ) ;
#3806=CARTESIAN_POINT ( 'NONE',  ( 4.257384971216501057, -47.81875000207092086, 25.69375250200204519 ) ) ;
#3809=CARTESIAN_POINT ( 'NONE',  ( 3.884137871020911792, 3.250000000000000444, 23.25209069347974022 ) ) ;
#3825=CARTESIAN_POINT ( 'NONE',  ( 5.912663395429905044, -43.63645833381128369, 32.06077891596451224 ) ) ;
#3831=CARTESIAN_POINT ( 'NONE',  ( 0.9468279798049125118, -49.80312500047794799, 29.19375250200204164 ) ) ;
#3832=CARTESIAN_POINT ( 'NONE',  ( 4.257363451562580003, -43.56959840651998661, 32.69375250187801640 ) ) ;
#3836=CARTESIAN_POINT ( 'NONE',  ( 4.257387320252103535, -45.81875005579910720, 25.69375250200286587 ) ) ;
#3839=ORIENTED_EDGE ( 'NONE', *, *, #6870, .T. ) ;
#3863=CARTESIAN_POINT ( 'NONE',  ( 4.257384923554909051, -51.42812500047794799, 25.37105061671875461 ) ) ;
#3868=CARTESIAN_POINT ( 'NONE',  ( 7.757384923554902834, -48.29166666666665009, 31.21447844416572792 ) ) ;
#3875=CARTESIAN_POINT ( 'NONE',  ( 2.602106451679909505, -49.30729166714461087, 32.06077891596451224 ) ) ;
#3878=ORIENTED_EDGE ( 'NONE', *, *, #14685, .T. ) ;
#3881=CARTESIAN_POINT ( 'NONE',  ( 6.007384923554907274, -46.66666666666665719, 26.16266358875650866 ) ) ;
#3882=CARTESIAN_POINT ( 'NONE',  ( 7.567941867304902814, -50.59895833381128227, 27.28240155936039457 ) ) ;
#3883=EDGE_LOOP ( 'NONE', ( #11411, #34127, #5448, #2140 ) ) ;
#3885=CARTESIAN_POINT ( 'NONE',  ( 1.575122801020536700, -43.13765301630450466, 31.44219004874084789 ) ) ;
#3890=CARTESIAN_POINT ( 'NONE',  ( 0.7573849235549138248, -49.73541666762256597, 27.17302655983835180 ) ) ;
#3895=ADVANCED_FACE ( 'NONE', ( #12748 ), #19356, .T. ) ;
#3905=CARTESIAN_POINT ( 'NONE',  ( 4.257384923554909051, -42.81875000095590167, 25.15230061767466552 ) ) ;
#3917=CARTESIAN_POINT ( 'NONE',  ( 0.9468279798049132889, -44.89062500047794657, 29.19375250200204164 ) ) ;
#3921=CARTESIAN_POINT ( 'NONE',  ( 0.9468279798049125118, -48.80312500047794799, 29.19375250200204164 ) ) ;
#3928=CARTESIAN_POINT ( 'NONE',  ( 2.507384923554911715, -49.11395833323773275, 26.16266358875650866 ) ) ;
#3933=CARTESIAN_POINT ( 'NONE',  ( 4.257384923554915268, -50.62499999999999289, 25.69375250200204519 ) ) ;
#3934=CARTESIAN_POINT ( 'NONE',  ( 0.7573849235549138248, -43.23541666762256597, 27.17302655983835180 ) ) ;
#3947=EDGE_CURVE ( 'NONE', #41285, #27540, #32310, .T. ) ;
#3950=CARTESIAN_POINT ( 'NONE',  ( 6.372162063493702178, -51.37157995136612243, 26.35440564930307517 ) ) ;
#3957=CARTESIAN_POINT ( 'NONE',  ( 9.589638516698011372, 3.250000000000000444, 31.84134197688108614 ) ) ;
#3972=CARTESIAN_POINT ( 'NONE',  ( 0.9468279798049134000, -43.34479166714461229, 27.28240155936039457 ) ) ;
#3974=CARTESIAN_POINT ( 'NONE',  ( 5.529031075589441180, -43.84911176810921063, 25.91591933264947656 ) ) ;
#3977=CARTESIAN_POINT ( 'NONE',  ( 7.308746397194781252, -51.90384855769124073, 27.41918393531257792 ) ) ;
#3981=CARTESIAN_POINT ( 'NONE',  ( 4.257385064927798446, -48.31875000421112532, 25.69375250200204519 ) ) ;
#3985=CARTESIAN_POINT ( 'NONE',  ( 3.119353925537964312, -44.29165189067819597, 25.86936841105205787 ) ) ;
#3990=CARTESIAN_POINT ( 'NONE',  ( 3.099070733870683547, -50.59634381480474730, 32.49740361561892854 ) ) ;
#3991=CARTESIAN_POINT ( 'NONE',  ( 2.507384923554909495, -51.61041666762257307, 32.22484141524756751 ) ) ;
#4011=CARTESIAN_POINT ( 'NONE',  ( 0.7573849235549120484, -44.45833333333332149, 31.21447844416572792 ) ) ;
#4039=CARTESIAN_POINT ( 'NONE',  ( 2.602106451679911281, -44.88645833381128369, 26.32672608803957459 ) ) ;
#4043=CARTESIAN_POINT ( 'NONE',  ( 7.283179133313935516, -45.89867704182979224, 27.37786058950996448 ) ) ;
#4068=CARTESIAN_POINT ( 'NONE',  ( 0.9468279798049134000, -50.84479166714461940, 27.28240155936039457 ) ) ;
#4072=CARTESIAN_POINT ( 'NONE',  ( 6.007384923554907274, -46.66666666666665719, 26.16266358875650866 ) ) ;
#4081=CARTESIAN_POINT ( 'NONE',  ( 7.567941867304904591, -50.14062500047794657, 29.19375250200204164 ) ) ;
#4085=DIRECTION ( 'NONE',  ( -0.000000000000000000, -1.000000000000000000, -0.000000000000000000 ) ) ;
#4087=CARTESIAN_POINT ( 'NONE',  ( 2.507384923554909495, -46.91666666666665719, 32.22484141524756751 ) ) ;
#4088=CARTESIAN_POINT ( 'NONE',  ( 4.257384923554908163, -49.76562500047794657, 33.01645438728532866 ) ) ;
#4089=ORIENTED_EDGE ( 'NONE', *, *, #29003, .T. ) ;
#4099=CARTESIAN_POINT ( 'NONE',  ( 7.757384923554905498, -50.44375000095590167, 29.19375250200204164 ) ) ;
#4109=CARTESIAN_POINT ( 'NONE',  ( 4.257384923554909051, -52.75000000000000000, 29.19375250200204164 ) ) ;
#4127=CARTESIAN_POINT ( 'NONE',  ( 4.257384923554909051, -46.01562500047794657, 25.37105061671875461 ) ) ;
#4131=CARTESIAN_POINT ( 'NONE',  ( 4.257384923554909051, -48.42812500047795510, 25.37105061671875106 ) ) ;
#4137=ORIENTED_EDGE ( 'NONE', *, *, #28802, .T. ) ;
#4138=CARTESIAN_POINT ( 'NONE',  ( 4.257384923554908163, -44.40562499990440415, 33.23520438632941421 ) ) ;
#4145=CARTESIAN_POINT ( 'NONE',  ( 4.257384923554908163, -43.06875000095590167, 33.23520438632941421 ) ) ;
#4161=CARTESIAN_POINT ( 'NONE',  ( 5.666266341680390894, -51.35291013971912122, 25.97877250594521570 ) ) ;
#4165=CARTESIAN_POINT ( 'NONE',  ( 5.195207097063835988, -48.35267090063072715, 32.69375250200204164 ) ) ;
#4175=B_SPLINE_CURVE_WITH_KNOTS ( 'NONE', 3,
 ( #6813, #13203, #36590, #17243, #3621, #17025, #26598, #13833, #16610, #39139, #39988, #7027, #30205, #10434, #20217, #23412, #221, #35949, #29570, #33177, #39782, #10855, #4043, #432, #641, #29989, #39557, #20005, #3836 ),
 .UNSPECIFIED., .F., .F.,
 ( 4, 2, 1, 2, 2, 1, 1, 2, 2, 2, 2, 2, 2, 2, 2, 4 ),
 ( 0.5971170540015400263, 0.5978981798657179159, 0.5980934613317624438, 0.5981178715150179404, 0.5981422816982735480, 0.5981911020647846522, 0.5982887427978068606, 0.5986793057298958054, 0.6002415574582516955, 0.6033660609149633647, 0.6064905643716750339, 0.6096150678283867030, 0.6127395712850984832, 0.6158640747418101524, 0.6189885781985218216, 0.6221130816552334908 ),
 .UNSPECIFIED. ) ;
#4186=CARTESIAN_POINT ( 'NONE',  ( 7.567941867304905479, -44.05312500047794799, 29.19375250200204164 ) ) ;
#4195=CARTESIAN_POINT ( 'NONE',  ( 4.986184314846762611, -48.55139264123500453, 32.61764107056806949 ) ) ;
#4199=CARTESIAN_POINT ( 'NONE',  ( 4.145640014138216145, -44.31609344832823894, 25.69527481516433198 ) ) ;
#4200=CARTESIAN_POINT ( 'NONE',  ( 4.257372105343447011, -50.31874971046479317, 25.69375250202551797 ) ) ;
#4201=EDGE_CURVE ( 'NONE', #26379, #27384, #32719, .T. ) ;
#4208=CARTESIAN_POINT ( 'NONE',  ( 7.757384923554905498, -51.94375000095590877, 29.19375250200204164 ) ) ;
#4227=CARTESIAN_POINT ( 'NONE',  ( 7.628735456095878220, -42.96462280839229919, 30.13667607713240315 ) ) ;
#4250=CARTESIAN_POINT ( 'NONE',  ( 5.912663395429907709, -43.46979166714461940, 26.32672608803957459 ) ) ;
#4255=CARTESIAN_POINT ( 'NONE',  ( 0.9468279798049134000, -45.84479166714461229, 27.28240155936039457 ) ) ;
#4259=CARTESIAN_POINT ( 'NONE',  ( 4.257384923554933032, -47.12499999999998579, 25.69375250200204519 ) ) ;
#4263=ORIENTED_EDGE ( 'NONE', *, *, #19848, .F. ) ;
#4287=CARTESIAN_POINT ( 'NONE',  ( 4.257384923554909051, -48.42812500047795510, 25.37105061671875461 ) ) ;
#4292=CARTESIAN_POINT ( 'NONE',  ( 6.007384923554907274, -44.16666666666665719, 26.16266358875650866 ) ) ;
#4298=CARTESIAN_POINT ( 'NONE',  ( 7.567941867304904591, -46.64062500047794657, 29.19375250200204164 ) ) ;
#4302=CYLINDRICAL_SURFACE ( 'NONE', #1964, 3.499999999999996003 ) ;
#4304=CARTESIAN_POINT ( 'NONE',  ( 6.007384923554907274, -48.16666666666665719, 26.16266358875650866 ) ) ;
#4306=CARTESIAN_POINT ( 'NONE',  ( 2.602106451679912169, -50.97395833381128227, 26.32672608803957459 ) ) ;
#4310=CARTESIAN_POINT ( 'NONE',  ( 3.319562750045990107, -43.39732909936924443, 32.69375250200203453 ) ) ;
#4317=CARTESIAN_POINT ( 'NONE',  ( 6.007384923554904610, -50.52708333428924448, 32.22484141524757462 ) ) ;
#4319=CARTESIAN_POINT ( 'NONE',  ( 4.257384923554909051, -52.75000000000000000, 32.69375250200203453 ) ) ;
#4326=CARTESIAN_POINT ( 'NONE',  ( 4.257403298629887978, -44.81875042683200405, 25.69375250205027683 ) ) ;
#4344=FACE_OUTER_BOUND ( 'NONE', #38835, .T. ) ;
#4346=CARTESIAN_POINT ( 'NONE',  ( 7.567941867304902814, -44.68229166714461087, 31.10510344464368870 ) ) ;
#4355=CARTESIAN_POINT ( 'NONE',  ( 4.257384923554908163, -46.40562499990440415, 33.23520438632941421 ) ) ;
#4358=B_SPLINE_CURVE_WITH_KNOTS ( 'NONE', 3,
 ( #32911, #20579, #33121, #29722, #10376, #20160, #4199, #33331, #805, #14196, #30143, #3985, #16967, #29933, #27172, #1021, #10591, #13990, #39929, #23572, #7393, #26965, #10791, #22634, #38798, #13469, #6672, #13270, #39201, #19443, #16263, #35610, #29633, #26253, #16676 ),
 .UNSPECIFIED., .F., .F.,
 ( 4, 2, 1, 1, 1, 1, 2, 2, 2, 2, 2, 2, 2, 2, 1, 2, 2, 2, 2, 4 ),
 ( 0.7744659764373558186, 0.7745067754929308990, 0.7745475745485059793, 0.7746291726596560290, 0.7747923688819562393, 0.7751187613265566601, 0.7757715462157575015, 0.7770771159941591844, 0.7796882555509624391, 0.7822993951077658048, 0.7849105346645691705, 0.7855633195537700120, 0.7856449176649200616, 0.7857265157760702223, 0.7858897119983704327, 0.7862161044429707424, 0.7875216742213724253, 0.7901328137781757910, 0.7927439533349790457, 0.7953550928917824114 ),
 .UNSPECIFIED. ) ;
#4362=CARTESIAN_POINT ( 'NONE',  ( 4.257384923554909051, -43.81875000095590877, 25.15230061767466552 ) ) ;
#4368=DIRECTION ( 'NONE',  ( 0.000000000000000000, 0.000000000000000000, -1.000000000000000000 ) ) ;
#4370=ADVANCED_FACE ( 'NONE', ( #23523, #30519 ), #10544, .T. ) ;
#4374=ADVANCED_FACE ( 'NONE', ( #23304 ), #30310, .T. ) ;
#4403=CARTESIAN_POINT ( 'NONE',  ( 0.9468279798049115126, -42.76145833381128369, 31.10510344464368515 ) ) ;
#4411=CARTESIAN_POINT ( 'NONE',  ( 4.414209988176128086, -48.56491322716216530, 32.69375250041858294 ) ) ;
#4417=DIRECTION ( 'NONE',  ( -0.06269504844767276319, 0.000000000000000000, -0.9980327303751835855 ) ) ;
#4422=CARTESIAN_POINT ( 'NONE',  ( 4.257384923554908163, -48.06875000095591588, 33.23520438632941421 ) ) ;
#4423=CARTESIAN_POINT ( 'NONE',  ( 5.912663395429907709, -43.05729166714461797, 26.32672608803957459 ) ) ;
#4425=DIRECTION ( 'NONE',  ( 0.000000000000000000, 0.000000000000000000, -1.000000000000000000 ) ) ;
#4427=CARTESIAN_POINT ( 'NONE',  ( 4.257384923554919709, -48.87499999999998579, 32.69375250200203453 ) ) ;
#4446=CARTESIAN_POINT ( 'NONE',  ( 4.257386979189129228, -48.56866505152967761, 32.69375250200084793 ) ) ;
#4451=CARTESIAN_POINT ( 'NONE',  ( 0.7573849235549138248, -49.04166666666666430, 27.17302655983835180 ) ) ;
#4473=CARTESIAN_POINT ( 'NONE',  ( 7.567941867304905479, -46.55312500047795510, 29.19375250200204164 ) ) ;
#4485=CARTESIAN_POINT ( 'NONE',  ( 3.623384818797003692, -46.08340060954702722, 32.64873813253547041 ) ) ;
#4501=CARTESIAN_POINT ( 'NONE',  ( 7.567941867304904591, -49.59479166714461940, 31.10510344464368870 ) ) ;
#4505=CARTESIAN_POINT ( 'NONE',  ( 4.257384923554909051, -44.62499999999999289, 25.15230061767466552 ) ) ;
#4510=ORIENTED_EDGE ( 'NONE', *, *, #28101, .T. ) ;
#4511=CARTESIAN_POINT ( 'NONE',  ( 2.602106451679912169, -46.47395833381128227, 26.32672608803957459 ) ) ;
#4516=CARTESIAN_POINT ( 'NONE',  ( 0.7573849235549138248, -46.54166666666665009, 27.17302655983835180 ) ) ;
#4517=CARTESIAN_POINT ( 'NONE',  ( 5.912663395429904156, -50.22395833381128227, 32.06077891596451224 ) ) ;
#4528=CARTESIAN_POINT ( 'NONE',  ( 7.757384923554905498, -50.94375000095590167, 29.19375250200204164 ) ) ;
#4561=CARTESIAN_POINT ( 'NONE',  ( 3.044482980331683741, -42.29615616597446603, 32.27411873898371653 ) ) ;
#4564=CARTESIAN_POINT ( 'NONE',  ( 7.757384923554905498, -44.78062499990439704, 29.19375250200204164 ) ) ;
#4570=CARTESIAN_POINT ( 'NONE',  ( 7.757384923554905498, -42.44375000095590167, 29.19375250200204164 ) ) ;
#4576=DIRECTION ( 'NONE',  ( 0.000000000000000000, -0.000000000000000000, 1.000000000000000000 ) ) ;
#4577=CARTESIAN_POINT ( 'NONE',  ( 4.257384923554909051, -52.75000000000000000, 25.69375250200204519 ) ) ;
#4605=ORIENTED_EDGE ( 'NONE', *, *, #10638, .F. ) ;
#4607=CARTESIAN_POINT ( 'NONE',  ( 0.9468279798049124008, -49.34895833381128938, 31.10510344464368515 ) ) ;
#4615=CARTESIAN_POINT ( 'NONE',  ( 3.884137871020911792, 7.250000000000000000, 23.25209069347974022 ) ) ;
#4621=CARTESIAN_POINT ( 'NONE',  ( 1.010296970832578189, -50.16380869402242837, 30.50036738254013713 ) ) ;
#4628=CARTESIAN_POINT ( 'NONE',  ( 2.507384923554911715, -50.27708333428924448, 26.16266358875650866 ) ) ;
#4629=CARTESIAN_POINT ( 'NONE',  ( 2.602106451679912169, -43.97395833381127517, 26.32672608803957459 ) ) ;
#4649=CARTESIAN_POINT ( 'NONE',  ( 7.694381580818771660, -42.95813609088305896, 29.85510387239071761 ) ) ;
#4676=CARTESIAN_POINT ( 'NONE',  ( 0.9468279798049125118, -47.30312500047795510, 29.19375250200204164 ) ) ;
#4679=CARTESIAN_POINT ( 'NONE',  ( 0.7573849235549138248, -51.54166666666666430, 27.17302655983835180 ) ) ;
#4680=CARTESIAN_POINT ( 'NONE',  ( 4.257384923554909051, -52.75000000000000000, 29.19375250200204164 ) ) ;
#4706=CARTESIAN_POINT ( 'NONE',  ( 4.257384923554908163, -48.17812500047794799, 33.01645438728532866 ) ) ;
#4710=CARTESIAN_POINT ( 'NONE',  ( 2.507384923554911715, -45.08333333333332149, 26.16266358875650866 ) ) ;
#4714=CARTESIAN_POINT ( 'NONE',  ( 2.209765167820375353, -49.26791102901238162, 26.33311073051439877 ) ) ;
#4717=CARTESIAN_POINT ( 'NONE',  ( 0.9468279798049124008, -47.34895833381128227, 31.10510344464368515 ) ) ;
#4723=CARTESIAN_POINT ( 'NONE',  ( 2.507384923554911715, -47.08333333333332149, 26.16266358875650866 ) ) ;
#4724=CARTESIAN_POINT ( 'NONE',  ( 0.9468279798049143992, -46.93229166714461087, 27.28240155936039457 ) ) ;
#4726=ORIENTED_EDGE ( 'NONE', *, *, #23502, .T. ) ;
#4728=CARTESIAN_POINT ( 'NONE',  ( 2.565898679282433648, -43.10738233019596066, 32.28576886232022503 ) ) ;
#4735=CARTESIAN_POINT ( 'NONE',  ( 2.507384923554911715, -46.27708333428923737, 26.16266358875650866 ) ) ;
#4737=CIRCLE ( 'NONE', #15614, 10.16127960363519200 ) ;
#4762=CARTESIAN_POINT ( 'NONE',  ( 0.9468279798049132889, -42.89062500047794657, 29.19375250200204164 ) ) ;
#4767=CARTESIAN_POINT ( 'NONE',  ( 6.317825176521873587, -44.36968050724386359, 26.33785153070475005 ) ) ;
#4770=CARTESIAN_POINT ( 'NONE',  ( 2.507384923554911715, -44.61395833323773275, 26.16266358875650866 ) ) ;
#4777=CARTESIAN_POINT ( 'NONE',  ( 2.602106451679909505, -51.71979166714461940, 32.06077891596451224 ) ) ;
#4793=CARTESIAN_POINT ( 'NONE',  ( 7.757379184476259404, -51.43739130682193661, 28.88537894627425473 ) ) ;
#4798=CARTESIAN_POINT ( 'NONE',  ( 2.507384923554909495, -46.41666666666666430, 32.22484141524756751 ) ) ;
#4804=CARTESIAN_POINT ( 'NONE',  ( 0.7573849235549129366, -49.49999999999998579, 29.19375250200204164 ) ) ;
#4813=CARTESIAN_POINT ( 'NONE',  ( 0.9468279798049143992, -49.93229166714461087, 27.28240155936039812 ) ) ;
#4819=CARTESIAN_POINT ( 'NONE',  ( 4.257384923554907274, -46.37499999999999289, 32.69375250200203453 ) ) ;
#4826=CARTESIAN_POINT ( 'NONE',  ( 2.492052225596140147, -50.10964413702874509, 32.25057942998105176 ) ) ;
#4833=CARTESIAN_POINT ( 'NONE',  ( 2.507384923554911715, -49.27708333428924448, 26.16266358875650866 ) ) ;
#4834=CARTESIAN_POINT ( 'NONE',  ( 2.602106451679909505, -43.30729166714461797, 32.06077891596451224 ) ) ;
#4835=VERTEX_POINT ( 'NONE', #41777 ) ;
#4852=CARTESIAN_POINT ( 'NONE',  ( 4.679285540522276854, -43.05761502611878910, 32.69375240742491684 ) ) ;
#4859=ORIENTED_EDGE ( 'NONE', *, *, #26998, .F. ) ;
#4861=CARTESIAN_POINT ( 'NONE',  ( 4.858564497732468013, -42.40485061181026083, 32.69375250200203453 ) ) ;
#4864=CARTESIAN_POINT ( 'NONE',  ( 6.437564807956788648, -49.01592712452269751, 31.93207029468803171 ) ) ;
#4879=CARTESIAN_POINT ( 'NONE',  ( 5.912663395429907709, -45.46979166714461229, 26.32672608803957459 ) ) ;
#4911=CARTESIAN_POINT ( 'NONE',  ( 0.9468279798049115126, -47.76145833381128369, 31.10510344464368515 ) ) ;
#4915=CARTESIAN_POINT ( 'NONE',  ( 7.757384923554905498, -44.74999999999999289, 29.19375250200204164 ) ) ;
#4920=CARTESIAN_POINT ( 'NONE',  ( 0.9468279798049132889, -47.89062500047795368, 29.19375250200204164 ) ) ;
#4921=CARTESIAN_POINT ( 'NONE',  ( 0.9468279798049117346, -47.76145833381128369, 31.10510344464368515 ) ) ;
#4927=CARTESIAN_POINT ( 'NONE',  ( 4.257384923554909051, -44.12499999999999289, 25.15230061767466552 ) ) ;
#4928=CARTESIAN_POINT ( 'NONE',  ( 4.257384923554908163, -48.26562500047794657, 33.01645438728532866 ) ) ;
#4935=ADVANCED_FACE ( 'NONE', ( #38366 ), #34852, .T. ) ;
#4942=CARTESIAN_POINT ( 'NONE',  ( 0.7573849235549120484, -48.15208333428924448, 31.21447844416572792 ) ) ;
#4955=CARTESIAN_POINT ( 'NONE',  ( 1.457022454045862281, -49.74697066505729026, 27.04475518746730955 ) ) ;
#4961=CARTESIAN_POINT ( 'NONE',  ( 4.257393644456948678, -47.56839819610503639, 32.69375250198117300 ) ) ;
#4968=CARTESIAN_POINT ( 'NONE',  ( 0.9468279798049143992, -43.43229166714461797, 27.28240155936039812 ) ) ;
#4977=CARTESIAN_POINT ( 'NONE',  ( 0.7573849235549138248, -44.57229166657106845, 27.17302655983835180 ) ) ;
#4984=CARTESIAN_POINT ( 'NONE',  ( 2.602106451679909505, -50.71979166714461940, 32.06077891596451224 ) ) ;
#5016=CARTESIAN_POINT ( 'NONE',  ( 7.567941867304904591, -51.59895833381127517, 27.28240155936039812 ) ) ;
#5019=CARTESIAN_POINT ( 'NONE',  ( 0.8465264847932635339, -45.17291499507261676, 30.10292899036398140 ) ) ;
#5021=CARTESIAN_POINT ( 'NONE',  ( 4.257384923554909051, -51.92812500047794799, 25.37105061671875106 ) ) ;
#5024=ORIENTED_EDGE ( 'NONE', *, *, #33401, .T. ) ;
#5026=ORIENTED_EDGE ( 'NONE', *, *, #16057, .F. ) ;
#5033=( BOUNDED_CURVE ( )  B_SPLINE_CURVE ( 2, ( #5215, #25002, #8196, #18399, #7995, #20966, #4798, #8613, #8398 ),
 .UNSPECIFIED., .F., .T. ) 
 B_SPLINE_CURVE_WITH_KNOTS ( ( 3, 2, 2, 2, 3 ),
 ( 0.5625000000000000000, 0.5666666666666666519, 0.5749999999999999556, 0.5833333333333333703, 0.5875000000000000222 ),
 .UNSPECIFIED. ) 
 CURVE ( )  GEOMETRIC_REPRESENTATION_ITEM ( )  RATIONAL_B_SPLINE_CURVE ( ( 0.9330127018922194093, 0.9330127018922194093, 1.000000000000000000, 0.8660254037844387076, 1.000000000000000000, 0.8660254037844387076, 1.000000000000000000, 0.9330127018922194093, 0.9330127018922194093 ) ) 
 REPRESENTATION_ITEM ( '' )  );
#5034=CARTESIAN_POINT ( 'NONE',  ( 6.007384923554907274, -50.16666666666665719, 26.16266358875650866 ) ) ;
#5035=CARTESIAN_POINT ( 'NONE',  ( 4.257373630597665937, -44.06920056960389331, 32.69375250196740978 ) ) ;
#5036=CARTESIAN_POINT ( 'NONE',  ( 4.257384923554908163, -48.56875000095589456, 33.23520438632941421 ) ) ;
#5037=CARTESIAN_POINT ( 'NONE',  ( 0.9468279798049143992, -42.93229166714461797, 27.28240155936039457 ) ) ;
#5047=VERTEX_POINT ( 'NONE', #19116 ) ;
#5087=CARTESIAN_POINT ( 'NONE',  ( 0.9468279798049115126, -42.26145833381129080, 31.10510344464368515 ) ) ;
#5110=AXIS2_PLACEMENT_3D ( 'NONE', #13943, #20751, #4368 ) ;
#5116=CARTESIAN_POINT ( 'NONE',  ( 4.257384923554909051, -51.62499999999999289, 25.69375250200204519 ) ) ;
#5120=CARTESIAN_POINT ( 'NONE',  ( 5.912663395429907709, -48.46979166714461229, 26.32672608803957459 ) ) ;
#5125=CARTESIAN_POINT ( 'NONE',  ( 7.757384923554904610, -44.70833333333332860, 27.17302655983835180 ) ) ;
#5131=CARTESIAN_POINT ( 'NONE',  ( 4.257384923554908163, -46.26562500047795368, 33.01645438728532866 ) ) ;
#5132=CARTESIAN_POINT ( 'NONE',  ( 0.9468279798049117346, -48.26145833381127659, 31.10510344464368515 ) ) ;
#5141=CARTESIAN_POINT ( 'NONE',  ( 0.7573849235549129366, -44.49999999999999289, 29.19375250200204164 ) ) ;
#5142=CARTESIAN_POINT ( 'NONE',  ( 4.257384923554908163, -48.76562500047794657, 33.01645438728532866 ) ) ;
#5154=CARTESIAN_POINT ( 'NONE',  ( 0.7573849235549129366, -46.69375000095590877, 29.19375250200204164 ) ) ;
#5188=CARTESIAN_POINT ( 'NONE',  ( 7.166761538707229207, -44.39730182767009126, 27.19489640936335206 ) ) ;
#5192=CARTESIAN_POINT ( 'NONE',  ( 0.7573849235549129366, -44.03062499990439704, 29.19375250200204164 ) ) ;
#5198=CARTESIAN_POINT ( 'NONE',  ( 6.007384923554904610, -42.52708333428924448, 32.22484141524757462 ) ) ;
#5200=EDGE_CURVE ( 'NONE', #1417, #18063, #42085, .T. ) ;
#5215=CARTESIAN_POINT ( 'NONE',  ( 4.257384923554909051, -46.62499999999999289, 25.69375250200204519 ) ) ;
#5229=CARTESIAN_POINT ( 'NONE',  ( 2.602106451679909505, -51.30729166714461797, 32.06077891596451224 ) ) ;
#5230=CARTESIAN_POINT ( 'NONE',  ( 0.7573849235549138248, -48.54166666666665719, 27.17302655983835180 ) ) ;
#5232=CARTESIAN_POINT ( 'NONE',  ( 2.492180318239951564, -45.10993369123420393, 32.25064796597265371 ) ) ;
#5242=CARTESIAN_POINT ( 'NONE',  ( 7.757384923554902834, -51.82229166657106845, 31.21447844416572792 ) ) ;
#5244=VERTEX_POINT ( 'NONE', #22927 ) ;
#5247=CARTESIAN_POINT ( 'NONE',  ( 6.914815212038112335, -42.49855590526476590, 31.49302548487920106 ) ) ;
#5248=CARTESIAN_POINT ( 'NONE',  ( 6.007384923554907274, -48.36041666762257307, 26.16266358875650866 ) ) ;
#5254=CARTESIAN_POINT ( 'NONE',  ( 0.8135782343053009624, -46.70730349460165343, 28.56889790815325725 ) ) ;
#5276=CARTESIAN_POINT ( 'NONE',  ( 1.082415802611938149, -48.22757325400807815, 27.71980849637871813 ) ) ;
#5279=CARTESIAN_POINT ( 'NONE',  ( 4.250460976167463656, -46.31858515239463259, 25.69375754101168141 ) ) ;
#5290=CARTESIAN_POINT ( 'NONE',  ( 4.257384923554909051, -52.75000000000000000, 29.19375250200204164 ) ) ;
#5293=EDGE_LOOP ( 'NONE', ( #6597, #13563 ) ) ;
#5296=CARTESIAN_POINT ( 'NONE',  ( 7.567941867304905479, -44.01145833381129080, 27.28240155936039812 ) ) ;
#5298=VERTEX_POINT ( 'NONE', #30355 ) ;
#5311=LINE ( 'NONE', #18284, #38143 ) ;
#5324=CARTESIAN_POINT ( 'NONE',  ( 0.9468279798049115126, -44.76145833381128369, 31.10510344464368515 ) ) ;
#5333=CARTESIAN_POINT ( 'NONE',  ( 0.9468279798049143992, -42.93229166714461797, 27.28240155936039812 ) ) ;
#5334=CARTESIAN_POINT ( 'NONE',  ( 5.912663395429905044, -48.63645833381128369, 32.06077891596451224 ) ) ;
#5340=EDGE_CURVE ( 'NONE', #5298, #37054, #4358, .T. ) ;
#5343=CARTESIAN_POINT ( 'NONE',  ( 2.507384923554909495, -44.41666666666665719, 32.22484141524756751 ) ) ;
#5344=CARTESIAN_POINT ( 'NONE',  ( 4.257384923554909051, -47.51562500047794657, 25.37105061671875106 ) ) ;
#5355=CARTESIAN_POINT ( 'NONE',  ( 7.757384923554904610, -47.40208333428923737, 27.17302655983835180 ) ) ;
#5370=CARTESIAN_POINT ( 'NONE',  ( 3.344147214146980129, -49.58827736583224777, 32.60323618271737445 ) ) ;
#5373=CARTESIAN_POINT ( 'NONE',  ( 6.047639609933945337, -50.86036776996892428, 26.15038353619980782 ) ) ;
#5376=CARTESIAN_POINT ( 'NONE',  ( 2.507384923554909495, -50.41666666666665719, 32.22484141524756751 ) ) ;
#5380=EDGE_LOOP ( 'NONE', ( #17246, #22606, #10597, #4859 ) ) ;
#5386=CARTESIAN_POINT ( 'NONE',  ( 0.9468279798049143992, -42.43229166714461087, 27.28240155936039812 ) ) ;
#5395=CARTESIAN_POINT ( 'NONE',  ( 6.007384923554907274, -42.69729166657106845, 26.16266358875650866 ) ) ;
#5398=ORIENTED_EDGE ( 'NONE', *, *, #35302, .T. ) ;
#5402=CARTESIAN_POINT ( 'NONE',  ( 0.9468279798049134000, -50.84479166714461940, 27.28240155936039457 ) ) ;
#5428=CARTESIAN_POINT ( 'NONE',  ( 7.757384923554904610, -49.70833333333332860, 27.17302655983835180 ) ) ;
#5436=CARTESIAN_POINT ( 'NONE',  ( 0.9468279798049124008, -50.34895833381128227, 31.10510344464368515 ) ) ;
#5437=FACE_OUTER_BOUND ( 'NONE', #20840, .T. ) ;
#5438=CYLINDRICAL_SURFACE ( 'NONE', #21346, 3.499999999999996003 ) ;
#5440=CARTESIAN_POINT ( 'NONE',  ( 1.465983582516957373, -45.24661677427183548, 27.03304990110994055 ) ) ;
#5445=VERTEX_POINT ( 'NONE', #28794 ) ;
#5448=ORIENTED_EDGE ( 'NONE', *, *, #26998, .T. ) ;
#5449=CARTESIAN_POINT ( 'NONE',  ( 0.7573849235549138248, -50.57229166657106134, 27.17302655983835180 ) ) ;
#5455=CARTESIAN_POINT ( 'NONE',  ( 0.7573849235549129366, -46.69375000095590877, 29.19375250200204164 ) ) ;
#5475=CARTESIAN_POINT ( 'NONE',  ( 4.257384923554896616, -47.62499999999999289, 25.69375250200204519 ) ) ;
#5486=CARTESIAN_POINT ( 'NONE',  ( 3.817969832886694892, -48.30888835370557644, 25.71970067155665518 ) ) ;
#5487=VERTEX_POINT ( 'NONE', #6261 ) ;
#5489=CARTESIAN_POINT ( 'NONE',  ( 4.207747386061200245, -46.31756856766628516, 25.69405380546465523 ) ) ;
#5492=CARTESIAN_POINT ( 'NONE',  ( 5.522285150417832078, -48.84912240721714483, 25.91296907892025914 ) ) ;
#5501=CARTESIAN_POINT ( 'NONE',  ( 3.044481415175603889, -42.20865620537255580, 32.27411812269912161 ) ) ;
#5507=CARTESIAN_POINT ( 'NONE',  ( 2.602106451679909505, -44.71979166714461940, 32.06077891596451224 ) ) ;
#5508=LINE ( 'NONE', #21051, #17193 ) ;
#5509=CARTESIAN_POINT ( 'NONE',  ( 0.7573849235549120484, -51.45833333333332860, 31.21447844416572792 ) ) ;
#5516=AXIS2_PLACEMENT_3D ( 'NONE', #37264, #7922, #34274 ) ;
#5529=CONICAL_SURFACE ( 'NONE', #2834, 2.999999999999988898, 0.7853981633974482790 ) ;
#5535=CARTESIAN_POINT ( 'NONE',  ( 3.319562750045979005, -51.39732909936924443, 32.69375250200202743 ) ) ;
#5544=CARTESIAN_POINT ( 'NONE',  ( 4.311547594202736811, -49.32003915391032933, 25.69411134273358499 ) ) ;
#5547=CARTESIAN_POINT ( 'NONE',  ( 5.912663395429907709, -44.55729166714461797, 26.32672608803957459 ) ) ;
#5549=CARTESIAN_POINT ( 'NONE',  ( 0.9468279798049134000, -46.34479166714461229, 27.28240155936039102 ) ) ;
#5555=EDGE_CURVE ( 'NONE', #3504, #29198, #24658, .T. ) ;
#5558=CARTESIAN_POINT ( 'NONE',  ( 7.757384923554905498, -45.24999999999999289, 29.19375250200204164 ) ) ;
#5559=CARTESIAN_POINT ( 'NONE',  ( 7.567941867304902814, -48.59895833381128227, 27.28240155936039457 ) ) ;
#5563=DIRECTION ( 'NONE',  ( 0.000000000000000000, 0.000000000000000000, -1.000000000000000000 ) ) ;
#5570=CARTESIAN_POINT ( 'NONE',  ( 7.757384923554904610, -45.40208333428923737, 27.17302655983835180 ) ) ;
#5578=EDGE_CURVE ( 'NONE', #13392, #20633, #39371, .T. ) ;
#5591=CARTESIAN_POINT ( 'NONE',  ( 5.889103563556269627, -51.02990395803887225, 32.29050263214028149 ) ) ;
#5597=CARTESIAN_POINT ( 'NONE',  ( 2.507384923554909495, -50.91666666666665719, 32.22484141524756751 ) ) ;
#5602=CARTESIAN_POINT ( 'NONE',  ( 5.162048144506971248, -50.33854639181622304, 25.80498743595777000 ) ) ;
#5612=CARTESIAN_POINT ( 'NONE',  ( 7.757384923554905498, -52.24999999999999289, 29.19375250200204164 ) ) ;
#5615=AXIS2_PLACEMENT_3D ( 'NONE', #2265, #19058, #27998 ) ;
#5619=CARTESIAN_POINT ( 'NONE',  ( 5.912663395429905044, -48.13645833381128369, 32.06077891596451224 ) ) ;
#5633=EDGE_CURVE ( 'NONE', #18585, #21757, #13075, .T. ) ;
#5650=EDGE_LOOP ( 'NONE', ( #40247, #39992, #22721, #11829 ) ) ;
#5652=CARTESIAN_POINT ( 'NONE',  ( 7.567941867304902814, -49.18229166714461087, 31.10510344464368870 ) ) ;
#5656=CARTESIAN_POINT ( 'NONE',  ( 4.257384923554933032, -46.12499999999999289, 25.69375250200204519 ) ) ;
#5659=( BOUNDED_CURVE ( )  B_SPLINE_CURVE ( 2, ( #36258, #17547, #30513, #39661, #40088, #33499, #7770, #10534, #3933 ),
 .UNSPECIFIED., .F., .T. ) 
 B_SPLINE_CURVE_WITH_KNOTS ( ( 3, 2, 2, 2, 3 ),
 ( 0.1375000000000000111, 0.1416666666666666630, 0.1499999999999999944, 0.1583333333333333259, 0.1624999999999999778 ),
 .UNSPECIFIED. ) 
 CURVE ( )  GEOMETRIC_REPRESENTATION_ITEM ( )  RATIONAL_B_SPLINE_CURVE ( ( 0.9330127018922194093, 0.9330127018922196314, 1.000000000000000000, 0.8660254037844387076, 1.000000000000000000, 0.8660254037844387076, 1.000000000000000000, 0.9330127018922196314, 0.9330127018922194093 ) ) 
 REPRESENTATION_ITEM ( '' )  );
#5663=CARTESIAN_POINT ( 'NONE',  ( 2.507384923554911715, -51.61395833323773275, 26.16266358875650866 ) ) ;
#5669=CYLINDRICAL_SURFACE ( 'NONE', #21980, 3.499999999999996003 ) ;
#5670=CARTESIAN_POINT ( 'NONE',  ( 0.7573849235549120484, -46.15208333428923737, 31.21447844416572792 ) ) ;
#5678=CARTESIAN_POINT ( 'NONE',  ( 1.062835702788538228, -46.72798980285339354, 27.68305657103001494 ) ) ;
#5685=ORIENTED_EDGE ( 'NONE', *, *, #36844, .T. ) ;
#5690=CARTESIAN_POINT ( 'NONE',  ( 3.044482980331683741, -42.29615616597446603, 32.27411873898371653 ) ) ;
#5697=ORIENTED_EDGE ( 'NONE', *, *, #32176, .T. ) ;
#5700=CARTESIAN_POINT ( 'NONE',  ( 2.192236980596466545, -48.26691354474279905, 26.33485159162115608 ) ) ;
#5703=CARTESIAN_POINT ( 'NONE',  ( 4.257384923554909051, -49.12499999999998579, 25.69375250200204519 ) ) ;
#5720=CARTESIAN_POINT ( 'NONE',  ( 2.602106451679909505, -43.21979166714461940, 32.06077891596451224 ) ) ;
#5724=CARTESIAN_POINT ( 'NONE',  ( 4.257384923554909051, -52.75000000000000000, 32.69375250200203453 ) ) ;
#5738=DIRECTION ( 'NONE',  ( 0.000000000000000000, 0.000000000000000000, -1.000000000000000000 ) ) ;
#5748=CARTESIAN_POINT ( 'NONE',  ( 1.294735043387984730, -45.73774940924044330, 27.28041587168420179 ) ) ;
#5755=CARTESIAN_POINT ( 'NONE',  ( 4.240937408158275801, -42.81835841818395494, 25.69378551711294989 ) ) ;
#5759=CARTESIAN_POINT ( 'NONE',  ( 7.567941867304904591, -44.09895833381128227, 27.28240155936039812 ) ) ;
#5760=CARTESIAN_POINT ( 'NONE',  ( 5.912663395429905044, -44.63645833381128369, 32.06077891596451224 ) ) ;
#5766=CIRCLE ( 'NONE', #27511, 2.999999999999988898 ) ;
#5770=CARTESIAN_POINT ( 'NONE',  ( 4.257384923554908163, -44.87499999999998579, 33.23520438632941421 ) ) ;
#5771=CARTESIAN_POINT ( 'NONE',  ( 7.567941867304902814, -44.09895833381128227, 27.28240155936039457 ) ) ;
#5777=EDGE_LOOP ( 'NONE', ( #1480, #39450, #25451, #14354 ) ) ;
#5808=CARTESIAN_POINT ( 'NONE',  ( 0.7573849235549129366, -49.49999999999998579, 29.19375250200204164 ) ) ;
#5811=CARTESIAN_POINT ( 'NONE',  ( 7.757384923554905498, -52.24999999999999289, 29.19375250200204164 ) ) ;
#5814=CARTESIAN_POINT ( 'NONE',  ( 0.9468279798049132889, -51.89062500047794657, 29.19375250200204164 ) ) ;
#5818=CARTESIAN_POINT ( 'NONE',  ( 3.400352878426299519, -51.08812583147929587, 32.58962158073460103 ) ) ;
#5821=CARTESIAN_POINT ( 'NONE',  ( 6.007384923554904610, -51.83333333333332149, 32.22484141524757462 ) ) ;
#5826=CARTESIAN_POINT ( 'NONE',  ( 0.7793942747566584561, -43.70530211506715546, 28.57069476044211243 ) ) ;
#5828=CARTESIAN_POINT ( 'NONE',  ( 4.257384923554909051, -49.92812500047795510, 25.37105061671875461 ) ) ;
#5833=CARTESIAN_POINT ( 'NONE',  ( 7.757384923554902834, -51.48541666762258018, 31.21447844416572792 ) ) ;
#5835=CARTESIAN_POINT ( 'NONE',  ( 0.7573849235549129366, -44.99999999999999289, 29.19375250200204164 ) ) ;
#5861=CARTESIAN_POINT ( 'NONE',  ( 2.602106451679909505, -48.30729166714461087, 32.06077891596451224 ) ) ;
#5866=CARTESIAN_POINT ( 'NONE',  ( 6.007384923554907274, -46.16666666666666430, 26.16266358875650866 ) ) ;
#5873=CARTESIAN_POINT ( 'NONE',  ( 4.257384923554908163, -50.40562499990439704, 33.23520438632941421 ) ) ;
#5875=ORIENTED_EDGE ( 'NONE', *, *, #1923, .F. ) ;
#5878=CYLINDRICAL_SURFACE ( 'NONE', #33019, 3.499999999999996003 ) ;
#5880=CARTESIAN_POINT ( 'NONE',  ( 4.257384923554909051, -46.31875000095590877, 25.15230061767466552 ) ) ;
#5885=CARTESIAN_POINT ( 'NONE',  ( 4.257373627235431890, -46.56920070325035255, 32.69375250196738847 ) ) ;
#5909=ORIENTED_EDGE ( 'NONE', *, *, #33573, .T. ) ;
#5921=VERTEX_POINT ( 'NONE', #12797 ) ;
#5929=CARTESIAN_POINT ( 'NONE',  ( 0.9468279798049125118, -44.30312500047794799, 29.19375250200204164 ) ) ;
#5930=DIRECTION ( 'NONE',  ( -0.000000000000000000, -1.000000000000000000, -0.000000000000000000 ) ) ;
#5952=CARTESIAN_POINT ( 'NONE',  ( -1.074868669588189274, 3.250000000000000444, 26.54616302712299358 ) ) ;
#5959=CARTESIAN_POINT ( 'NONE',  ( 2.732842139880885757, -42.41129863770651554, 32.35500919978411360 ) ) ;
#5961=CARTESIAN_POINT ( 'NONE',  ( 4.257284565358973261, -49.31874761147663833, 25.69375250344087291 ) ) ;
#5963=CARTESIAN_POINT ( 'NONE',  ( 7.567941867304904591, -44.64062500047794657, 29.19375250200204164 ) ) ;
#5965=CARTESIAN_POINT ( 'NONE',  ( 7.567941867304905479, -46.01145833381127659, 27.28240155936039457 ) ) ;
#5970=ORIENTED_EDGE ( 'NONE', *, *, #38528, .T. ) ;
#5975=B_SPLINE_CURVE_WITH_KNOTS ( 'NONE', 1,
 ( #31297, #37891 ),
 .UNSPECIFIED., .F., .F.,
 ( 2, 2 ),
 ( 0.000000000000000000, 1.000000000000000000 ),
 .UNSPECIFIED. ) ;
#5976=CARTESIAN_POINT ( 'NONE',  ( 0.7573849235549138248, -50.73541666762258018, 27.17302655983835180 ) ) ;
#5977=CARTESIAN_POINT ( 'NONE',  ( 7.567941867304904591, -46.64062500047794657, 29.19375250200204164 ) ) ;
#5984=EDGE_LOOP ( 'NONE', ( #17750, #38670, #27792, #5685 ) ) ;
#6009=CARTESIAN_POINT ( 'NONE',  ( 3.874322594413236232, -47.07904369231797403, 32.69375239976304215 ) ) ;
#6011=CARTESIAN_POINT ( 'NONE',  ( 0.7573849235549129366, -49.99999999999998579, 29.19375250200204164 ) ) ;
#6016=CARTESIAN_POINT ( 'NONE',  ( 7.757384923554905498, -51.24999999999999289, 29.19375250200204164 ) ) ;
#6018=CARTESIAN_POINT ( 'NONE',  ( 4.257384923554909051, -52.01562500047794657, 25.37105061671875461 ) ) ;
#6025=CARTESIAN_POINT ( 'NONE',  ( 0.7573849235549138248, -43.07229166657106845, 27.17302655983835180 ) ) ;
#6028=CARTESIAN_POINT ( 'NONE',  ( 3.645301061776913709, -43.80415323193589217, 25.74550170336454258 ) ) ;
#6031=CARTESIAN_POINT ( 'NONE',  ( 7.567941867304905479, -48.51145833381129080, 27.28240155936039812 ) ) ;
#6049=CARTESIAN_POINT ( 'NONE',  ( 7.757384923554902834, -46.79166666666666430, 31.21447844416572792 ) ) ;
#6064=CARTESIAN_POINT ( 'NONE',  ( 0.9468279798049124008, -48.84895833381128227, 31.10510344464368515 ) ) ;
#6069=CARTESIAN_POINT ( 'NONE',  ( 2.602106451679911281, -49.38645833381128369, 26.32672608803957459 ) ) ;
#6075=CARTESIAN_POINT ( 'NONE',  ( 6.007384923554904610, -51.86395833323773275, 32.22484141524757462 ) ) ;
#6083=CARTESIAN_POINT ( 'NONE',  ( 7.757384923554905498, -47.94375000095590877, 29.19375250200204164 ) ) ;
#6088=CARTESIAN_POINT ( 'NONE',  ( 3.119227915952081265, -46.79164887342799517, 25.86940945997289631 ) ) ;
#6111=CARTESIAN_POINT ( 'NONE',  ( 1.490421186781835106, -48.14058451628968527, 31.35540774174545930 ) ) ;
#6116=CARTESIAN_POINT ( 'NONE',  ( 1.448217457205561276, -46.24407940750679558, 27.05506089894496569 ) ) ;
#6117=CARTESIAN_POINT ( 'NONE',  ( 7.567941867304905479, -45.01145833381127659, 27.28240155936039812 ) ) ;
#6119=FACE_OUTER_BOUND ( 'NONE', #35584, .T. ) ;
#6125=CARTESIAN_POINT ( 'NONE',  ( 7.387670274871020126, -47.90705596867327642, 27.62757742376139447 ) ) ;
#6132=VERTEX_POINT ( 'NONE', #3226 ) ;
#6139=TOROIDAL_SURFACE ( 'NONE', #37422, 8.161279603635192004, 2.000000000000000000 ) ;
#6164=CARTESIAN_POINT ( 'NONE',  ( 1.082422815364890267, -45.72757365916418593, 27.71979338561974870 ) ) ;
#6170=CARTESIAN_POINT ( 'NONE',  ( 6.007384923554904610, -42.83333333333332149, 32.22484141524757462 ) ) ;
#6171=VERTEX_POINT ( 'NONE', #32769 ) ;
#6176=CARTESIAN_POINT ( 'NONE',  ( 7.567941867304904591, -45.09895833381128227, 27.28240155936039812 ) ) ;
#6177=CARTESIAN_POINT ( 'NONE',  ( 0.9468279798049125118, -45.80312500047794799, 29.19375250200204164 ) ) ;
#6185=CARTESIAN_POINT ( 'NONE',  ( 2.602106451679912169, -45.47395833381128227, 26.32672608803957459 ) ) ;
#6186=VERTEX_POINT ( 'NONE', #20019 ) ;
#6220=CARTESIAN_POINT ( 'NONE',  ( 3.319562750045979005, -50.39732909936925154, 32.69375250200202743 ) ) ;
#6221=CARTESIAN_POINT ( 'NONE',  ( 3.216123017577583010, -47.29496912360560401, 25.84197997154288018 ) ) ;
#6223=CARTESIAN_POINT ( 'NONE',  ( 7.757384923554904610, -48.70833333333332860, 27.17302655983835180 ) ) ;
#6227=CARTESIAN_POINT ( 'NONE',  ( 6.786426097275578329, -43.38222351362738749, 26.77111960792089462 ) ) ;
#6228=CARTESIAN_POINT ( 'NONE',  ( 7.567941867304904591, -51.14062500047794657, 29.19375250200204164 ) ) ;
#6237=CARTESIAN_POINT ( 'NONE',  ( 2.507384923554909495, -50.91666666666665719, 32.22484141524756751 ) ) ;
#6240=DIRECTION ( 'NONE',  ( 0.000000000000000000, 1.000000000000000000, 0.000000000000000000 ) ) ;
#6242=CARTESIAN_POINT ( 'NONE',  ( 0.9468279798049125118, -47.80312500047795510, 29.19375250200204164 ) ) ;
#6245=CARTESIAN_POINT ( 'NONE',  ( 4.243231566435547109, -48.81841304733880804, 25.69377387954355285 ) ) ;
#6261=CARTESIAN_POINT ( 'NONE',  ( 4.257384923554907274, -42.87499999999998579, 32.69375250200203453 ) ) ;
#6264=LINE ( 'NONE', #36017, #9877 ) ;
#6277=CARTESIAN_POINT ( 'NONE',  ( 0.9468279798049124008, -48.34895833381128227, 31.10510344464368515 ) ) ;
#6279=CARTESIAN_POINT ( 'NONE',  ( 4.257384923554909051, -52.75000000000000000, 29.19375250200204164 ) ) ;
#6283=CARTESIAN_POINT ( 'NONE',  ( 7.567941867304905479, -50.55312500047794799, 29.19375250200204164 ) ) ;
#6289=CARTESIAN_POINT ( 'NONE',  ( 2.507384923554911715, -48.61395833323773275, 26.16266358875650866 ) ) ;
#6292=B_SPLINE_CURVE_WITH_KNOTS ( 'NONE', 3,
 ( #31532, #7368, #40114, #10768, #14170, #14384, #5591, #2184, #31325, #18562, #11965, #36716, #7581, #2400, #41117, #27360, #33308, #36937, #30541, #1410, #30121, #20555, #23547, #997, #26944, #40333, #39905, #5373, #30331, #8777, #27147 ),
 .UNSPECIFIED., .F., .F.,
 ( 4, 2, 2, 2, 2, 2, 2, 2, 2, 2, 2, 1, 2, 2, 2, 4 ),
 ( 0.08848910052190732400, 0.09171115576556215787, 0.09251666957647587675, 0.09291942648193274312, 0.09332218338738962338, 0.09493321100921707500, 0.09815526625287193663, 0.1013773214965267983, 0.1045993767401816599, 0.1050021336456385124, 0.1052035120983669247, 0.1054048905510953371, 0.1062104043620089727, 0.1078214319838362578, 0.1110434872274908280, 0.1142655424711453982 ),
 .UNSPECIFIED. ) ;
#6295=CARTESIAN_POINT ( 'NONE',  ( 2.507384923554911715, -47.27708333428923737, 26.16266358875650866 ) ) ;
#6326=ORIENTED_EDGE ( 'NONE', *, *, #36438, .T. ) ;
#6328=CARTESIAN_POINT ( 'NONE',  ( 0.7484393592536344730, -46.20256796738419780, 28.79278630262570715 ) ) ;
#6329=CARTESIAN_POINT ( 'NONE',  ( 5.912663395429907709, -45.96979166714461229, 26.32672608803957459 ) ) ;
#6338=CARTESIAN_POINT ( 'NONE',  ( 6.229484066789795271, -48.02162552298980813, 32.08667045211768709 ) ) ;
#6343=CARTESIAN_POINT ( 'NONE',  ( 4.257384923554909051, -52.75000000000000000, 29.19375250200204164 ) ) ;
#6348=CARTESIAN_POINT ( 'NONE',  ( 4.016126221559384923, -50.81344534091775955, 25.70090420402475218 ) ) ;
#6371=CARTESIAN_POINT ( 'NONE',  ( 4.257384923554933032, -47.12499999999998579, 25.69375250200204519 ) ) ;
#6385=CARTESIAN_POINT ( 'NONE',  ( 7.567941867304904591, -42.59895833381128227, 27.28240155936039812 ) ) ;
#6386=CARTESIAN_POINT ( 'NONE',  ( 5.912663395429905044, -45.13645833381128369, 32.06077891596451224 ) ) ;
#6393=CARTESIAN_POINT ( 'NONE',  ( 0.9468279798049124008, -46.34895833381128227, 31.10510344464368515 ) ) ;
#6399=( BOUNDED_CURVE ( )  B_SPLINE_CURVE ( 2, ( #18013, #23997, #24613, #11620, #14623, #23780, #5034, #17187, #37577 ),
 .UNSPECIFIED., .F., .T. ) 
 B_SPLINE_CURVE_WITH_KNOTS ( ( 3, 2, 2, 2, 3 ),
 ( 0.1875000000000000000, 0.1916666666666666796, 0.2000000000000000111, 0.2083333333333333426, 0.2124999999999999944 ),
 .UNSPECIFIED. ) 
 CURVE ( )  GEOMETRIC_REPRESENTATION_ITEM ( )  RATIONAL_B_SPLINE_CURVE ( ( 0.9330127018922194093, 0.9330127018922194093, 1.000000000000000000, 0.8660254037844387076, 1.000000000000000000, 0.8660254037844387076, 1.000000000000000000, 0.9330127018922196314, 0.9330127018922194093 ) ) 
 REPRESENTATION_ITEM ( '' )  );
#6400=DIRECTION ( 'NONE',  ( 0.000000000000000000, 0.000000000000000000, -1.000000000000000000 ) ) ;
#6405=DIRECTION ( 'NONE',  ( 0.000000000000000000, 0.000000000000000000, -1.000000000000000000 ) ) ;
#6424=DIRECTION ( 'NONE',  ( -0.000000000000000000, -1.000000000000000000, -0.000000000000000000 ) ) ;
#6430=CARTESIAN_POINT ( 'NONE',  ( 5.912663395429905044, -50.13645833381128369, 32.06077891596451224 ) ) ;
#6431=CARTESIAN_POINT ( 'NONE',  ( 4.199126471681860373, -47.31743656691902800, 25.69416811096508013 ) ) ;
#6434=CARTESIAN_POINT ( 'NONE',  ( 7.757384923554905498, -50.24999999999998579, 29.19375250200204164 ) ) ;
#6439=AXIS2_PLACEMENT_3D ( 'NONE', #3673, #10482, #30468 ) ;
#6441=CARTESIAN_POINT ( 'NONE',  ( 4.793417624836986413, -43.33047171055636682, 25.73337050339662824 ) ) ;
#6447=ORIENTED_EDGE ( 'NONE', *, *, #10764, .T. ) ;
#6448=CARTESIAN_POINT ( 'NONE',  ( 6.007384923554907274, -50.16666666666665719, 26.16266358875650866 ) ) ;
#6476=LINE ( 'NONE', #41580, #24125 ) ;
#6484=CARTESIAN_POINT ( 'NONE',  ( 4.257384923554909051, -42.40485061181025372, 29.19375250200204164 ) ) ;
#6490=EDGE_CURVE ( 'NONE', #11420, #40970, #34247, .T. ) ;
#6491=CARTESIAN_POINT ( 'NONE',  ( 5.912663395429907709, -47.05729166714461087, 26.32672608803957459 ) ) ;
#6495=CARTESIAN_POINT ( 'NONE',  ( 2.602106451679909505, -50.21979166714461940, 32.06077891596451224 ) ) ;
#6504=CARTESIAN_POINT ( 'NONE',  ( 7.757384923554904610, -48.73895833323773985, 27.17302655983835180 ) ) ;
#6511=CARTESIAN_POINT ( 'NONE',  ( 0.7573849235549120484, -44.65208333428923737, 31.21447844416572792 ) ) ;
#6547=CARTESIAN_POINT ( 'NONE',  ( 2.602106451679909505, -45.71979166714461229, 32.06077891596451224 ) ) ;
#6553=CARTESIAN_POINT ( 'NONE',  ( 3.884137871020911792, 7.250000000000000000, 23.25209069347974022 ) ) ;
#6563=ORIENTED_EDGE ( 'NONE', *, *, #26230, .F. ) ;
#6564=CARTESIAN_POINT ( 'NONE',  ( 1.391625388736486890, -50.74273289949884713, 27.18438749348072037 ) ) ;
#6581=DIRECTION ( 'NONE',  ( -0.000000000000000000, -1.000000000000000000, -0.000000000000000000 ) ) ;
#6595=CARTESIAN_POINT ( 'NONE',  ( 3.083737720948865224, -42.59668842538616218, 32.53392196406579018 ) ) ;
#6597=ORIENTED_EDGE ( 'NONE', *, *, #29750, .T. ) ;
#6605=CARTESIAN_POINT ( 'NONE',  ( 5.912663395429907709, -45.55729166714461797, 26.32672608803957459 ) ) ;
#6608=CYLINDRICAL_SURFACE ( 'NONE', #22129, 3.499999999999996003 ) ;
#6609=EDGE_CURVE ( 'NONE', #30506, #15596, #16375, .T. ) ;
#6634=CARTESIAN_POINT ( 'NONE',  ( 7.567941867304904591, -50.09479166714461229, 31.10510344464368870 ) ) ;
#6635=CARTESIAN_POINT ( 'NONE',  ( 3.598976648041220194, -47.30382842909354935, 25.75374524824077582 ) ) ;
#6637=CARTESIAN_POINT ( 'NONE',  ( 0.7573849235549120484, -45.95833333333332149, 31.21447844416572792 ) ) ;
#6645=CARTESIAN_POINT ( 'NONE',  ( 2.602106451679909505, -48.30729166714461087, 32.06077891596451224 ) ) ;
#6649=LINE ( 'NONE', #29177, #33209 ) ;
#6650=( BOUNDED_SURFACE ( )  B_SPLINE_SURFACE ( 1, 2, ( 
 ( #6837, #889, #17053, #29593, #20243, #13859, #35973, #245, #457, #29376, #38966, #13227, #3437, #26213, #32996, #3863, #10041, #10460, #7051, #36404, #16429, #39160, #22591, #16220, #35773, #669, #23004, #13642, #19810, #4068, #19401, #26625, #26413, #39366, #29164, #23213, #38758, #22802, #16842, #29804, #39585, #35567, #9629, #23439, #30016, #7271, #6430, #6634, #32373, #42, #13022, #19597, #8310, #20668, #24081, #21290, #33647, #1520, #14079, #4501, #7695, #24486, #17686, #24278, #8103, #30443, #27265, #17482, #40636, #37249, #27665, #30655, #37455, #21081, #1312, #30232, #37047, #14286, #27052, #1107, #10885, #34259, #27469, #18099, #7907, #7482, #5120, #4287, #40015, #14498, #40227, #34054, #17891, #4706, #40435, #23870, #11097, #31069, #20875, #36835, #33846, #11294, #11494, #4911, #30864, #1726, #14707, #1921, #26839, #39810, #10674, #23656, #36618, #20456, #33423, #17269, #150, #22916, #29278, #31270, #19512, #2932, #15117, #15921, #19095, #35254, #28869, #9744, #12718, #11699, #22488, #25490, #34464, #22282, #35880, #41867, #24697, #19719, #3348, #35469, #22705, #25696, #41650, #9315, #35684, #39074, #6329, #16336, #37659, #16136, #13132, #38660, #6547, #32482, #9528, #6745, #32062, #26115, #3146, #9956, #38869, #25902, #2133, #28657, #32687, #14901, #38453, #27870, #19304, #6117, #40846, #32279, #8516, #21493, #29075, #5324, #42071, #12505, #12926, #18297, #7809, #26531, #36088, #1008, #20352, #26954, #16746, #32897, #39705, #10578, #17169, #33319, #4186, #20784, #23980, #23556, #13765, #3762, #3549, #30131, #29709, #16543, #36728, #14181, #13543, #572, #365, #36516, #39489, #3972, #23761, #7590, #7377, #10993, #7175, #20566, #13976, #39916, #10778, #33541, #10363, #23339, #27159, #4403, #36301, #17381, #20146, #33106, #30341, #16953, #1214, #40125, #36947, #29494, #29920, #19932, #13342, #791, #26324 ),
 ( #39271, #26744, #10151, #23120, #6956, #14393, #8626, #21183, #40545, #40342, #14810, #8837, #33955, #5016, #17997, #24386, #17586, #33754, #34371, #25016, #5229, #21599, #17790, #8414, #21392, #18206, #27369, #15230, #27578, #30975, #28190, #11402, #31173, #20980, #37355, #14605, #31383, #24596, #2035, #15017, #8210, #34158, #1831, #5436, #27980, #34573, #37561, #2248, #40961, #27777, #37158, #40746, #11602, #4813, #8009, #30763, #1625, #11813, #24810, #41178, #1420, #37771, #30551, #12023, #11205, #18415, #37977, #4607, #24189, #12233, #35627, #5652, #96, #15869, #2664, #15651, #41813, #29221, #31592, #6064, #35415, #13076, #38182, #21814, #2877, #28609, #15443, #34998, #9048, #41384, #22024, #6277, #5861, #34783, #12871, #32429, #31792, #18832, #18627, #28814, #41595, #26061, #22436, #39018, #19043, #2458, #16281, #25221, #12452, #25645, #9262, #29024, #25851, #12666, #38605, #25436, #38398, #28398, #9470, #22230, #35199, #19253, #6491, #3091, #32224, #16084, #42021, #32012, #38815, #9690, #22652, #19461, #3293, #39646, #10517, #23063, #36674, #17327, #23710, #26270, #13916, #39428, #10098, #10303, #13486, #29649, #23274, #4127, #7112, #6690, #16897, #19869, #29436, #16693, #30290, #36240, #19659, #14129, #39861, #29864, #17111, #20087, #36031, #3704, #30075, #33481, #730, #10723, #32631, #23498, #7538, #33051, #950, #26895, #3917, #1161, #26471, #20512, #36461, #4346, #33261, #27105, #39218, #6897, #9902, #22859, #32836, #35827, #13704, #513, #3495, #26683, #16485, #305, #7325, #13286, #40497, #14343, #27728, #37110, #2197, #20932, #30498, #37512, #40697, #21349, #24139, #27322, #34111, #4968, #11554, #24545, #8367, #15177, #18365, #17950, #21138, #40285, #40073, #7963, #1368, #33903, #4762, #17741, #30715, #8581, #7754, #1985, #23924, #34528, #36893, #1580, #31336, #5386, #34321, #14558, #11763, #20729, #10940 ) ),
 .UNSPECIFIED., .F., .F., .T. ) 
 B_SPLINE_SURFACE_WITH_KNOTS ( ( 2, 2 ),
 ( 3, 2, 2, 2, 2, 2, 2, 2, 2, 2, 2, 2, 2, 2, 2, 2, 2, 2, 2, 2, 2, 2, 2, 2, 2, 2, 2, 2, 2, 2, 2, 2, 2, 2, 2, 2, 2, 2, 2, 2, 2, 2, 2, 2, 2, 2, 2, 2, 2, 2, 2, 2, 2, 2, 2, 2, 2, 2, 2, 2, 2, 2, 2, 2, 2, 2, 2, 2, 2, 2, 2, 2, 2, 2, 2, 2, 2, 2, 2, 2, 2, 2, 2, 2, 2, 2, 2, 2, 2, 2, 2, 2, 2, 2, 2, 2, 2, 2, 2, 2, 2, 2, 2, 2, 2, 2, 2, 2, 2, 2, 2, 2, 2, 2, 2, 2, 2, 2, 2, 3 ),
 ( 0.000000000000000000, 1.000000000000000000 ),
 ( 0.000000000000000000, 0.008333333333333333218, 0.01666666666666666644, 0.02500000000000000139, 0.03333333333333333287, 0.04166666666666666435, 0.05000000000000000278, 0.05833333333333333426, 0.06666666666666666574, 0.07499999999999999722, 0.08333333333333332871, 0.09166666666666666019, 0.1000000000000000056, 0.1083333333333333370, 0.1166666666666666685, 0.1250000000000000000, 0.1333333333333333315, 0.1416666666666666630, 0.1499999999999999944, 0.1583333333333333259, 0.1666666666666666574, 0.1749999999999999889, 0.1833333333333333204, 0.1916666666666666796, 0.2000000000000000111, 0.2083333333333333426, 0.2166666666666666741, 0.2250000000000000056, 0.2333333333333333370, 0.2416666666666666685, 0.2500000000000000000, 0.2583333333333333592, 0.2666666666666666630, 0.2750000000000000222, 0.2833333333333333259, 0.2916666666666666852, 0.2999999999999999889, 0.3083333333333333481, 0.3166666666666666519, 0.3250000000000000111, 0.3333333333333333148, 0.3416666666666666741, 0.3499999999999999778, 0.3583333333333333370, 0.3666666666666666408, 0.3750000000000000000, 0.3833333333333333592, 0.3916666666666666630, 0.4000000000000000222, 0.4083333333333333259, 0.4166666666666666852, 0.4249999999999999889, 0.4333333333333333481, 0.4416666666666666519, 0.4500000000000000111, 0.4583333333333333148, 0.4666666666666666741, 0.4749999999999999778, 0.4833333333333333370, 0.4916666666666666408, 0.5000000000000000000, 0.5083333333333333037, 0.5166666666666667185, 0.5250000000000000222, 0.5333333333333333259, 0.5416666666666666297, 0.5500000000000000444, 0.5583333333333333481, 0.5666666666666666519, 0.5749999999999999556, 0.5833333333333333703, 0.5916666666666666741, 0.5999999999999999778, 0.6083333333333332815, 0.6166666666666666963, 0.6250000000000000000, 0.6333333333333333037, 0.6416666666666667185, 0.6500000000000000222, 0.6583333333333333259, 0.6666666666666666297, 0.6750000000000000444, 0.6833333333333333481, 0.6916666666666666519, 0.6999999999999999556, 0.7083333333333333703, 0.7166666666666666741, 0.7249999999999999778, 0.7333333333333332815, 0.7416666666666666963, 0.7500000000000000000, 0.7583333333333333037, 0.7666666666666667185, 0.7750000000000000222, 0.7833333333333333259, 0.7916666666666666297, 0.8000000000000000444, 0.8083333333333333481, 0.8166666666666666519, 0.8249999999999999556, 0.8333333333333333703, 0.8416666666666666741, 0.8499999999999999778, 0.8583333333333332815, 0.8666666666666666963, 0.8750000000000000000, 0.8833333333333333037, 0.8916666666666667185, 0.9000000000000000222, 0.9083333333333333259, 0.9166666666666666297, 0.9250000000000000444, 0.9333333333333333481, 0.9416666666666666519, 0.9499999999999999556, 0.9583333333333333703, 0.9666666666666666741, 0.9749999999999999778, 0.9833333333333332815, 0.9845488016436891865 ),
 .UNSPECIFIED. ) 
 GEOMETRIC_REPRESENTATION_ITEM ( )  RATIONAL_B_SPLINE_SURFACE ( (
 ( 1.000000000000000000, 0.8660254037844387076, 1.000000000000000000, 0.8660254037844387076, 1.000000000000000000, 0.8660254037844387076, 1.000000000000000000, 0.8660254037844387076, 1.000000000000000000, 0.8660254037844387076, 1.000000000000000000, 0.8660254037844387076, 1.000000000000000000, 0.8660254037844387076, 1.000000000000000000, 0.8660254037844387076, 1.000000000000000000, 0.8660254037844387076, 1.000000000000000000, 0.8660254037844387076, 1.000000000000000000, 0.8660254037844387076, 1.000000000000000000, 0.8660254037844387076, 1.000000000000000000, 0.8660254037844387076, 1.000000000000000000, 0.8660254037844387076, 1.000000000000000000, 0.8660254037844387076, 1.000000000000000000, 0.8660254037844387076, 1.000000000000000000, 0.8660254037844387076, 1.000000000000000000, 0.8660254037844387076, 1.000000000000000000, 0.8660254037844387076, 1.000000000000000000, 0.8660254037844387076, 1.000000000000000000, 0.8660254037844387076, 1.000000000000000000, 0.8660254037844387076, 1.000000000000000000, 0.8660254037844387076, 1.000000000000000000, 0.8660254037844387076, 1.000000000000000000, 0.8660254037844387076, 1.000000000000000000, 0.8660254037844387076, 1.000000000000000000, 0.8660254037844387076, 1.000000000000000000, 0.8660254037844387076, 1.000000000000000000, 0.8660254037844387076, 1.000000000000000000, 0.8660254037844387076, 1.000000000000000000, 0.8660254037844387076, 1.000000000000000000, 0.8660254037844387076, 1.000000000000000000, 0.8660254037844387076, 1.000000000000000000, 0.8660254037844387076, 1.000000000000000000, 0.8660254037844387076, 1.000000000000000000, 0.8660254037844387076, 1.000000000000000000, 0.8660254037844387076, 1.000000000000000000, 0.8660254037844387076, 1.000000000000000000, 0.8660254037844387076, 1.000000000000000000, 0.8660254037844387076, 1.000000000000000000, 0.8660254037844387076, 1.000000000000000000, 0.8660254037844387076, 1.000000000000000000, 0.8660254037844387076, 1.000000000000000000, 0.8660254037844387076, 1.000000000000000000, 0.8660254037844387076, 1.000000000000000000, 0.8660254037844387076, 1.000000000000000000, 0.8660254037844387076, 1.000000000000000000, 0.8660254037844387076, 1.000000000000000000, 0.8660254037844387076, 1.000000000000000000, 0.8660254037844387076, 1.000000000000000000, 0.8660254037844387076, 1.000000000000000000, 0.8660254037844387076, 1.000000000000000000, 0.8660254037844387076, 1.000000000000000000, 0.8660254037844387076, 1.000000000000000000, 0.8660254037844387076, 1.000000000000000000, 0.8660254037844387076, 1.000000000000000000, 0.8660254037844387076, 1.000000000000000000, 0.8660254037844387076, 1.000000000000000000, 0.8660254037844387076, 1.000000000000000000, 0.8660254037844387076, 1.000000000000000000, 0.8660254037844387076, 1.000000000000000000, 0.8660254037844387076, 1.000000000000000000, 0.8660254037844387076, 1.000000000000000000, 0.8660254037844387076, 1.000000000000000000, 0.8660254037844387076, 1.000000000000000000, 0.8660254037844387076, 1.000000000000000000, 0.8660254037844387076, 1.000000000000000000, 0.8660254037844387076, 1.000000000000000000, 0.8660254037844387076, 1.000000000000000000, 0.8660254037844387076, 1.000000000000000000, 0.8660254037844387076, 1.000000000000000000, 0.8660254037844387076, 1.000000000000000000, 0.8660254037844387076, 1.000000000000000000, 0.8660254037844387076, 1.000000000000000000, 0.8660254037844387076, 1.000000000000000000, 0.8660254037844387076, 1.000000000000000000, 0.8660254037844387076, 1.000000000000000000, 0.8660254037844387076, 1.000000000000000000, 0.8660254037844387076, 1.000000000000000000, 0.8660254037844387076, 1.000000000000000000, 0.8660254037844387076, 1.000000000000000000, 0.8660254037844387076, 1.000000000000000000, 0.8660254037844387076, 1.000000000000000000, 0.8660254037844387076, 1.000000000000000000, 0.8660254037844387076, 1.000000000000000000, 0.8660254037844387076, 1.000000000000000000, 0.8660254037844387076, 1.000000000000000000, 0.8660254037844387076, 1.000000000000000000, 0.8660254037844387076, 1.000000000000000000, 0.8660254037844387076, 1.000000000000000000, 0.8660254037844387076, 1.000000000000000000, 0.8660254037844387076, 1.000000000000000000, 0.8660254037844387076, 1.000000000000000000, 0.8660254037844387076, 1.000000000000000000, 0.8660254037844387076, 1.000000000000000000, 0.8660254037844387076, 1.000000000000000000, 0.8660254037844387076, 1.000000000000000000, 0.8660254037844387076, 1.000000000000000000, 0.8660254037844387076, 1.000000000000000000, 0.8660254037844387076, 1.000000000000000000, 0.8660254037844387076, 1.000000000000000000, 0.8660254037844387076, 1.000000000000000000, 0.8660254037844387076, 1.000000000000000000, 0.8660254037844387076, 1.000000000000000000, 0.8660254037844387076, 1.000000000000000000, 0.8660254037844387076, 1.000000000000000000, 0.8660254037844387076, 1.000000000000000000, 0.8660254037844387076, 1.000000000000000000, 0.8660254037844387076, 1.000000000000000000, 0.8660254037844387076, 1.000000000000000000, 0.8660254037844387076, 1.000000000000000000, 0.8660254037844387076, 1.000000000000000000, 0.8660254037844387076, 1.000000000000000000, 0.8660254037844387076, 1.000000000000000000, 0.8660254037844387076, 1.000000000000000000, 0.8660254037844387076, 1.000000000000000000, 0.8660254037844387076, 1.000000000000000000, 0.8660254037844387076, 1.000000000000000000, 0.9804589748688710138, 0.9666183089694433406),
 ( 1.000000000000000000, 0.8660254037844387076, 1.000000000000000000, 0.8660254037844387076, 1.000000000000000000, 0.8660254037844387076, 1.000000000000000000, 0.8660254037844387076, 1.000000000000000000, 0.8660254037844387076, 1.000000000000000000, 0.8660254037844387076, 1.000000000000000000, 0.8660254037844387076, 1.000000000000000000, 0.8660254037844387076, 1.000000000000000000, 0.8660254037844387076, 1.000000000000000000, 0.8660254037844387076, 1.000000000000000000, 0.8660254037844387076, 1.000000000000000000, 0.8660254037844387076, 1.000000000000000000, 0.8660254037844387076, 1.000000000000000000, 0.8660254037844387076, 1.000000000000000000, 0.8660254037844387076, 1.000000000000000000, 0.8660254037844387076, 1.000000000000000000, 0.8660254037844387076, 1.000000000000000000, 0.8660254037844387076, 1.000000000000000000, 0.8660254037844387076, 1.000000000000000000, 0.8660254037844387076, 1.000000000000000000, 0.8660254037844387076, 1.000000000000000000, 0.8660254037844387076, 1.000000000000000000, 0.8660254037844387076, 1.000000000000000000, 0.8660254037844387076, 1.000000000000000000, 0.8660254037844387076, 1.000000000000000000, 0.8660254037844387076, 1.000000000000000000, 0.8660254037844387076, 1.000000000000000000, 0.8660254037844387076, 1.000000000000000000, 0.8660254037844387076, 1.000000000000000000, 0.8660254037844387076, 1.000000000000000000, 0.8660254037844387076, 1.000000000000000000, 0.8660254037844387076, 1.000000000000000000, 0.8660254037844387076, 1.000000000000000000, 0.8660254037844387076, 1.000000000000000000, 0.8660254037844387076, 1.000000000000000000, 0.8660254037844387076, 1.000000000000000000, 0.8660254037844387076, 1.000000000000000000, 0.8660254037844387076, 1.000000000000000000, 0.8660254037844387076, 1.000000000000000000, 0.8660254037844387076, 1.000000000000000000, 0.8660254037844387076, 1.000000000000000000, 0.8660254037844387076, 1.000000000000000000, 0.8660254037844387076, 1.000000000000000000, 0.8660254037844387076, 1.000000000000000000, 0.8660254037844387076, 1.000000000000000000, 0.8660254037844387076, 1.000000000000000000, 0.8660254037844387076, 1.000000000000000000, 0.8660254037844387076, 1.000000000000000000, 0.8660254037844387076, 1.000000000000000000, 0.8660254037844387076, 1.000000000000000000, 0.8660254037844387076, 1.000000000000000000, 0.8660254037844387076, 1.000000000000000000, 0.8660254037844387076, 1.000000000000000000, 0.8660254037844387076, 1.000000000000000000, 0.8660254037844387076, 1.000000000000000000, 0.8660254037844387076, 1.000000000000000000, 0.8660254037844387076, 1.000000000000000000, 0.8660254037844387076, 1.000000000000000000, 0.8660254037844387076, 1.000000000000000000, 0.8660254037844387076, 1.000000000000000000, 0.8660254037844387076, 1.000000000000000000, 0.8660254037844387076, 1.000000000000000000, 0.8660254037844387076, 1.000000000000000000, 0.8660254037844387076, 1.000000000000000000, 0.8660254037844387076, 1.000000000000000000, 0.8660254037844387076, 1.000000000000000000, 0.8660254037844387076, 1.000000000000000000, 0.8660254037844387076, 1.000000000000000000, 0.8660254037844387076, 1.000000000000000000, 0.8660254037844387076, 1.000000000000000000, 0.8660254037844387076, 1.000000000000000000, 0.8660254037844387076, 1.000000000000000000, 0.8660254037844387076, 1.000000000000000000, 0.8660254037844387076, 1.000000000000000000, 0.8660254037844387076, 1.000000000000000000, 0.8660254037844387076, 1.000000000000000000, 0.8660254037844387076, 1.000000000000000000, 0.8660254037844387076, 1.000000000000000000, 0.8660254037844387076, 1.000000000000000000, 0.8660254037844387076, 1.000000000000000000, 0.8660254037844387076, 1.000000000000000000, 0.8660254037844387076, 1.000000000000000000, 0.8660254037844387076, 1.000000000000000000, 0.8660254037844387076, 1.000000000000000000, 0.8660254037844387076, 1.000000000000000000, 0.8660254037844387076, 1.000000000000000000, 0.8660254037844387076, 1.000000000000000000, 0.8660254037844387076, 1.000000000000000000, 0.8660254037844387076, 1.000000000000000000, 0.8660254037844387076, 1.000000000000000000, 0.8660254037844387076, 1.000000000000000000, 0.8660254037844387076, 1.000000000000000000, 0.8660254037844387076, 1.000000000000000000, 0.8660254037844387076, 1.000000000000000000, 0.8660254037844387076, 1.000000000000000000, 0.8660254037844387076, 1.000000000000000000, 0.8660254037844387076, 1.000000000000000000, 0.8660254037844387076, 1.000000000000000000, 0.8660254037844387076, 1.000000000000000000, 0.8660254037844387076, 1.000000000000000000, 0.8660254037844387076, 1.000000000000000000, 0.8660254037844387076, 1.000000000000000000, 0.8660254037844387076, 1.000000000000000000, 0.8660254037844387076, 1.000000000000000000, 0.8660254037844387076, 1.000000000000000000, 0.8660254037844387076, 1.000000000000000000, 0.8660254037844387076, 1.000000000000000000, 0.8660254037844387076, 1.000000000000000000, 0.8660254037844387076, 1.000000000000000000, 0.8660254037844387076, 1.000000000000000000, 0.8660254037844387076, 1.000000000000000000, 0.8660254037844387076, 1.000000000000000000, 0.8660254037844387076, 1.000000000000000000, 0.8660254037844387076, 1.000000000000000000, 0.8660254037844387076, 1.000000000000000000, 0.8660254037844387076, 1.000000000000000000, 0.8660254037844387076, 1.000000000000000000, 0.8660254037844387076, 1.000000000000000000, 0.9804589748688710138, 0.9666183089694433406) ) ) 
 REPRESENTATION_ITEM ( '' )  SURFACE ( )  );
#6652=CARTESIAN_POINT ( 'NONE',  ( 7.757384923554902834, -51.29166666666666430, 31.21447844416572792 ) ) ;
#6659=CARTESIAN_POINT ( 'NONE',  ( 4.207637791565947083, -48.81756596034435347, 25.69405536588158157 ) ) ;
#6662=CARTESIAN_POINT ( 'NONE',  ( 0.7573849235549120484, -51.65208333428923737, 31.21447844416572792 ) ) ;
#6672=CARTESIAN_POINT ( 'NONE',  ( 0.7448776224096232967, -44.19208448081445795, 29.24353518660518247 ) ) ;
#6690=CARTESIAN_POINT ( 'NONE',  ( 0.9468279798049143992, -45.93229166714461087, 27.28240155936039812 ) ) ;
#6694=CARTESIAN_POINT ( 'NONE',  ( 4.257384923554908163, -50.67812500047794799, 33.01645438728532866 ) ) ;
#6697=VERTEX_POINT ( 'NONE', #40171 ) ;
#6701=CARTESIAN_POINT ( 'NONE',  ( 7.757384923554902834, -48.82229166657106845, 31.21447844416572792 ) ) ;
#6708=CARTESIAN_POINT ( 'NONE',  ( 6.007384923554904610, -44.52708333428923737, 32.22484141524757462 ) ) ;
#6724=CARTESIAN_POINT ( 'NONE',  ( 1.206093470055251915, -51.73365478101325010, 27.41906282711480358 ) ) ;
#6745=CARTESIAN_POINT ( 'NONE',  ( 7.567941867304904591, -45.59479166714461229, 31.10510344464368870 ) ) ;
#6751=CARTESIAN_POINT ( 'NONE',  ( 5.431072640116468619, -51.84668943685245068, 25.85359527568743587 ) ) ;
#6761=EDGE_LOOP ( 'NONE', ( #2892, #38731, #25769, #1795 ) ) ;
#6762=CARTESIAN_POINT ( 'NONE',  ( 2.973864942388035004, -50.78972610979749902, 25.92892739770275412 ) ) ;
#6763=CARTESIAN_POINT ( 'NONE',  ( 6.007384923554907274, -51.86041666762257307, 26.16266358875650866 ) ) ;
#6769=DIRECTION ( 'NONE',  ( -0.000000000000000000, -1.000000000000000000, -0.000000000000000000 ) ) ;
#6801=CARTESIAN_POINT ( 'NONE',  ( 7.567941867304905479, -43.01145833381127659, 27.28240155936039457 ) ) ;
#6806=VECTOR ( 'NONE', #10012, 999.9999999999998863 ) ;
#6812=ORIENTED_EDGE ( 'NONE', *, *, #6490, .F. ) ;
#6813=CARTESIAN_POINT ( 'NONE',  ( 4.257386978954926349, -46.06866506076136147, 32.69375250200084793 ) ) ;
#6837=CARTESIAN_POINT ( 'NONE',  ( 7.567941867304905479, -52.05312500047794799, 29.19375250200204164 ) ) ;
#6838=CARTESIAN_POINT ( 'NONE',  ( 1.707893204742154225, -47.13445147569633775, 31.62829582693292707 ) ) ;
#6842=CARTESIAN_POINT ( 'NONE',  ( 0.7573849235549138248, -47.54166666666666430, 27.17302655983835180 ) ) ;
#6844=FACE_OUTER_BOUND ( 'NONE', #34006, .T. ) ;
#6850=CARTESIAN_POINT ( 'NONE',  ( 0.9468279798049124008, -48.84895833381128227, 31.10510344464368515 ) ) ;
#6856=CARTESIAN_POINT ( 'NONE',  ( 2.507384923554911715, -49.08333333333332860, 26.16266358875650866 ) ) ;
#6860=AXIS2_PLACEMENT_3D ( 'NONE', #21999, #12844, #38373 ) ;
#6868=CARTESIAN_POINT ( 'NONE',  ( 4.257384923554909051, -49.31875000095590877, 25.15230061767466552 ) ) ;
#6870=EDGE_CURVE ( 'NONE', #30827, #11963, #31691, .T. ) ;
#6897=CARTESIAN_POINT ( 'NONE',  ( 4.257384923554909051, -44.51562500047793947, 25.37105061671875461 ) ) ;
#6901=CARTESIAN_POINT ( 'NONE',  ( 7.567941867304902814, -51.09479166714461940, 31.10510344464368870 ) ) ;
#6908=CARTESIAN_POINT ( 'NONE',  ( 7.757384923554904610, -47.23895833323773985, 27.17302655983835180 ) ) ;
#6914=CARTESIAN_POINT ( 'NONE',  ( 0.7573849235549120484, -45.15208333428923737, 31.21447844416572792 ) ) ;
#6915=CARTESIAN_POINT ( 'NONE',  ( 0.7573849235549129366, -44.19375000095590877, 29.19375250200204164 ) ) ;
#6920=EDGE_CURVE ( 'NONE', #2889, #219, #8355, .T. ) ;
#6939=LINE ( 'NONE', #3957, #37695 ) ;
#6956=CARTESIAN_POINT ( 'NONE',  ( 2.602106451679912169, -51.97395833381127517, 26.32672608803957459 ) ) ;
#6966=LINE ( 'NONE', #4615, #27809 ) ;
#6977=CARTESIAN_POINT ( 'NONE',  ( 0.7573849235549120484, -42.95833333333332149, 31.21447844416572792 ) ) ;
#7000=CARTESIAN_POINT ( 'NONE',  ( 4.257384923554907274, -47.87499999999998579, 32.69375250200203453 ) ) ;
#7004=CARTESIAN_POINT ( 'NONE',  ( 9.216391464164017222, 3.250000000000000444, 25.89968016835878828 ) ) ;
#7015=CARTESIAN_POINT ( 'NONE',  ( 2.815359705850238203, -42.21442365662065299, 32.18390073966531162 ) ) ;
#7022=CARTESIAN_POINT ( 'NONE',  ( 5.912663395429907709, -48.96979166714461940, 26.32672608803957459 ) ) ;
#7027=CARTESIAN_POINT ( 'NONE',  ( 5.054850468987194034, -46.04974488278707412, 32.60215666277660773 ) ) ;
#7051=CARTESIAN_POINT ( 'NONE',  ( 0.9468279798049125118, -51.30312500047794799, 29.19375250200204164 ) ) ;
#7055=CARTESIAN_POINT ( 'NONE',  ( 7.757384923554905498, -47.74999999999999289, 29.19375250200204164 ) ) ;
#7063=CARTESIAN_POINT ( 'NONE',  ( 2.602106451679909505, -49.80729166714461087, 32.06077891596451224 ) ) ;
#7067=ORIENTED_EDGE ( 'NONE', *, *, #39674, .T. ) ;
#7071=CARTESIAN_POINT ( 'NONE',  ( 7.757384923554904610, -48.70833333333332860, 27.17302655983835180 ) ) ;
#7072=CARTESIAN_POINT ( 'NONE',  ( 4.257384923554908163, -51.26562500047794657, 33.01645438728532866 ) ) ;
#7075=CARTESIAN_POINT ( 'NONE',  ( 7.753308668142990356, -46.43293264035850143, 28.64661842978646078 ) ) ;
#7076=CARTESIAN_POINT ( 'NONE',  ( 1.467598420238623413, -43.14167172227107017, 31.30874891896506895 ) ) ;
#7082=CARTESIAN_POINT ( 'NONE',  ( 2.507384923554909495, -50.11041666762257307, 32.22484141524756751 ) ) ;
#7098=CARTESIAN_POINT ( 'NONE',  ( 3.874323125386055278, -44.57904350424352913, 32.69375239977542691 ) ) ;
#7100=CARTESIAN_POINT ( 'NONE',  ( 6.007384923554904610, -43.02708333428924448, 32.22484141524757462 ) ) ;
#7101=VECTOR ( 'NONE', #26105, 1000.000000000000000 ) ;
#7112=CARTESIAN_POINT ( 'NONE',  ( 2.602106451679912169, -45.97395833381128227, 26.32672608803957459 ) ) ;
#7118=CARTESIAN_POINT ( 'NONE',  ( 5.912663395429907709, -46.96979166714461229, 26.32672608803957459 ) ) ;
#7125=CARTESIAN_POINT ( 'NONE',  ( 7.757384923554904610, -49.23895833323774696, 27.17302655983835180 ) ) ;
#7132=CARTESIAN_POINT ( 'NONE',  ( 6.007384923554904610, -44.52708333428923737, 32.22484141524757462 ) ) ;
#7133=CARTESIAN_POINT ( 'NONE',  ( 0.7573849235549129366, -43.19375000095590167, 29.19375250200204164 ) ) ;
#7134=DIRECTION ( 'NONE',  ( 0.000000000000000000, 0.000000000000000000, -1.000000000000000000 ) ) ;
#7159=DIRECTION ( 'NONE',  ( -0.06269504844767276319, 0.000000000000000000, -0.9980327303751835855 ) ) ;
#7175=CARTESIAN_POINT ( 'NONE',  ( 5.912663395429905044, -43.13645833381128369, 32.06077891596451224 ) ) ;
#7177=CARTESIAN_POINT ( 'NONE',  ( 4.630631976088899648, 7.250000000000000000, 35.13541431052434660 ) ) ;
#7180=CARTESIAN_POINT ( 'NONE',  ( 7.757384923554904610, -51.93739396430994759, 28.88550110664623105 ) ) ;
#7184=CARTESIAN_POINT ( 'NONE',  ( 6.609555611976475120, -42.40348350966320368, 26.58669445190447789 ) ) ;
#7185=VERTEX_POINT ( 'NONE', #17320 ) ;
#7193=CARTESIAN_POINT ( 'NONE',  ( 1.450562746511960599, -50.74513189330684781, 27.10201926690882956 ) ) ;
#7194=CARTESIAN_POINT ( 'NONE',  ( 2.507384923554911715, -43.08333333333332149, 26.16266358875650866 ) ) ;
#7198=AXIS2_PLACEMENT_3D ( 'NONE', #8748, #17913, #27689 ) ;
#7221=CARTESIAN_POINT ( 'NONE',  ( 7.771270866252558029, -42.40485061181024662, 28.67992134089934453 ) ) ;
#7224=FACE_OUTER_BOUND ( 'NONE', #7717, .T. ) ;
#7235=ORIENTED_EDGE ( 'NONE', *, *, #41636, .F. ) ;
#7236=CARTESIAN_POINT ( 'NONE',  ( 2.602106451679911281, -42.88645833381128369, 26.32672608803957459 ) ) ;
#7238=VERTEX_POINT ( 'NONE', #34725 ) ;
#7241=CARTESIAN_POINT ( 'NONE',  ( 0.9468279798049125118, -45.80312500047794799, 29.19375250200204164 ) ) ;
#7263=CARTESIAN_POINT ( 'NONE',  ( 3.319562750045975452, -47.60267090063072715, 25.69375250200204519 ) ) ;
#7271=CARTESIAN_POINT ( 'NONE',  ( 4.257384923554908163, -50.17812500047794799, 33.01645438728532866 ) ) ;
#7274=CARTESIAN_POINT ( 'NONE',  ( 2.507384923554909495, -46.41666666666666430, 32.22484141524756751 ) ) ;
#7277=CARTESIAN_POINT ( 'NONE',  ( 7.539511857869623412, -49.41615532851295711, 27.97788138825265136 ) ) ;
#7282=CARTESIAN_POINT ( 'NONE',  ( 5.912663395429907709, -49.55729166714461087, 26.32672608803957459 ) ) ;
#7288=CARTESIAN_POINT ( 'NONE',  ( 2.507384923554909495, -48.41666666666665719, 32.22484141524756751 ) ) ;
#7289=CARTESIAN_POINT ( 'NONE',  ( 0.9468279798049143992, -49.93229166714461087, 27.28240155936039457 ) ) ;
#7292=CARTESIAN_POINT ( 'NONE',  ( 0.7720403373718807138, -43.20942893590223122, 28.55350710908417255 ) ) ;
#7298=CARTESIAN_POINT ( 'NONE',  ( 7.757384923554902834, -48.98541666762257307, 31.21447844416572792 ) ) ;
#7310=CARTESIAN_POINT ( 'NONE',  ( 4.254945224872334286, -44.81869499998192907, 25.69375248914514742 ) ) ;
#7325=CARTESIAN_POINT ( 'NONE',  ( 5.912663395429907709, -44.05729166714461797, 26.32672608803957459 ) ) ;
#7329=CARTESIAN_POINT ( 'NONE',  ( 7.567941867304905479, -49.01145833381127659, 27.28240155936039457 ) ) ;
#7335=CARTESIAN_POINT ( 'NONE',  ( 4.257384923554909051, -46.15562499990439704, 25.15230061767466552 ) ) ;
#7341=CARTESIAN_POINT ( 'NONE',  ( 7.757384923554902834, -43.48541666762257307, 31.21447844416572792 ) ) ;
#7343=APPLICATION_CONTEXT ( 'automotive_design' ) ;
#7351=LINE ( 'NONE', #22887, #28573 ) ;
#7356=CARTESIAN_POINT ( 'NONE',  ( 7.492868907063256145, -51.41324652391548256, 27.80504890350500702 ) ) ;
#7363=LINE ( 'NONE', #1199, #1033 ) ;
#7368=CARTESIAN_POINT ( 'NONE',  ( 4.741926879912544912, -51.05650742677216414, 32.69375246162329773 ) ) ;
#7377=CARTESIAN_POINT ( 'NONE',  ( 2.602106451679909505, -43.21979166714461940, 32.06077891596451224 ) ) ;
#7384=EDGE_CURVE ( 'NONE', #36237, #2260, #38698, .T. ) ;
#7388=CARTESIAN_POINT ( 'NONE',  ( 6.522812667733104419, -48.51169790649085201, 31.89943741123822818 ) ) ;
#7393=CARTESIAN_POINT ( 'NONE',  ( 0.8193576531996143997, -44.20801188736880505, 28.53784375251166239 ) ) ;
#7397=ORIENTED_EDGE ( 'NONE', *, *, #17927, .T. ) ;
#7400=CARTESIAN_POINT ( 'NONE',  ( 7.757384923554902834, -50.98541666762257307, 31.21447844416572792 ) ) ;
#7401=CARTESIAN_POINT ( 'NONE',  ( 7.567941867304902814, -43.18229166714461797, 31.10510344464368870 ) ) ;
#7404=CARTESIAN_POINT ( 'NONE',  ( 0.7573849235549138248, -52.04166666666666430, 27.17302655983835180 ) ) ;
#7414=CARTESIAN_POINT ( 'NONE',  ( 0.7573849235549138248, -44.04166666666665719, 27.17302655983835180 ) ) ;
#7429=DIRECTION ( 'NONE',  ( -0.000000000000000000, -1.000000000000000000, -0.000000000000000000 ) ) ;
#7432=CARTESIAN_POINT ( 'NONE',  ( 7.666289227044870813, -49.92101608122666789, 28.27763467795875840 ) ) ;
#7449=CARTESIAN_POINT ( 'NONE',  ( 4.257384923554909051, -46.92812500047795510, 25.37105061671875461 ) ) ;
#7453=CARTESIAN_POINT ( 'NONE',  ( 0.7573849235549120484, -46.95833333333332149, 31.21447844416572792 ) ) ;
#7457=ADVANCED_FACE ( 'NONE', ( #16634 ), #6650, .T. ) ;
#7466=DIRECTION ( 'NONE',  ( 0.000000000000000000, 0.000000000000000000, -1.000000000000000000 ) ) ;
#7482=CARTESIAN_POINT ( 'NONE',  ( 7.567941867304905479, -48.51145833381129080, 27.28240155936039812 ) ) ;
#7486=CARTESIAN_POINT ( 'NONE',  ( 0.7573849235549129366, -48.49999999999998579, 29.19375250200204164 ) ) ;
#7492=CARTESIAN_POINT ( 'NONE',  ( 5.912663395429904156, -48.72395833381128227, 32.06077891596451224 ) ) ;
#7496=CARTESIAN_POINT ( 'NONE',  ( 4.257384923554909051, -52.75000000000000000, 29.19375250200204164 ) ) ;
#7499=EDGE_CURVE ( 'NONE', #14568, #20255, #11358, .T. ) ;
#7500=CARTESIAN_POINT ( 'NONE',  ( 6.007384923554904610, -47.33333333333332149, 32.22484141524757462 ) ) ;
#7501=CARTESIAN_POINT ( 'NONE',  ( 2.602106451679912169, -49.97395833381128227, 26.32672608803957459 ) ) ;
#7507=ADVANCED_FACE ( 'NONE', ( #34946 ), #2546, .T. ) ;
#7511=CARTESIAN_POINT ( 'NONE',  ( 6.007384923554904610, -49.52708333428924448, 32.22484141524757462 ) ) ;
#7525=( BOUNDED_CURVE ( )  B_SPLINE_CURVE ( 2, ( #22169, #33147, #34928, #29156, #12596, #4011, #29957, #28956, #25578 ),
 .UNSPECIFIED., .F., .T. ) 
 B_SPLINE_CURVE_WITH_KNOTS ( ( 3, 2, 2, 2, 3 ),
 ( 0.7624999999999999556, 0.7666666666666667185, 0.7750000000000000222, 0.7833333333333333259, 0.7874999999999999778 ),
 .UNSPECIFIED. ) 
 CURVE ( )  GEOMETRIC_REPRESENTATION_ITEM ( )  RATIONAL_B_SPLINE_CURVE ( ( 0.9330127018922194093, 0.9330127018922185211, 1.000000000000000000, 0.8660254037844387076, 1.000000000000000000, 0.8660254037844387076, 1.000000000000000000, 0.9330127018922194093, 0.9330127018922194093 ) ) 
 REPRESENTATION_ITEM ( '' )  );
#7527=CARTESIAN_POINT ( 'NONE',  ( 2.507384923554909495, -42.11041666762257307, 32.22484141524756751 ) ) ;
#7538=CARTESIAN_POINT ( 'NONE',  ( 5.912663395429907709, -45.05729166714461797, 26.32672608803957459 ) ) ;
#7547=CARTESIAN_POINT ( 'NONE',  ( 7.757384923554904610, -46.73895833323773275, 27.17302655983835180 ) ) ;
#7549=ORIENTED_EDGE ( 'NONE', *, *, #41390, .T. ) ;
#7552=CARTESIAN_POINT ( 'NONE',  ( 2.507384923554909495, -45.11041666762257307, 32.22484141524756751 ) ) ;
#7553=DIRECTION ( 'NONE',  ( -0.000000000000000000, -1.000000000000000000, -0.000000000000000000 ) ) ;
#7581=CARTESIAN_POINT ( 'NONE',  ( 7.143294403654272706, -50.99412010465364631, 31.22555619547587114 ) ) ;
#7590=CARTESIAN_POINT ( 'NONE',  ( 0.9468279798049115126, -43.26145833381128369, 31.10510344464368515 ) ) ;
#7591=CARTESIAN_POINT ( 'NONE',  ( 2.507384923554909495, -48.41666666666665719, 32.22484141524756751 ) ) ;
#7598=CARTESIAN_POINT ( 'NONE',  ( 0.7901003357267470939, -42.40525878933519976, 29.74720725560691648 ) ) ;
#7603=CARTESIAN_POINT ( 'NONE',  ( 0.7485707470435462030, -50.19356944708604118, 29.25727845053753384 ) ) ;
#7610=CARTESIAN_POINT ( 'NONE',  ( 4.257384923554909051, -42.40485061181025372, 34.19375250200204164 ) ) ;
#7611=CARTESIAN_POINT ( 'NONE',  ( 0.7573849235549129366, -49.69375000095590167, 29.19375250200204164 ) ) ;
#7612=CARTESIAN_POINT ( 'NONE',  ( 4.257384923554908163, -43.76562500047794657, 33.01645438728532866 ) ) ;
#7638=CARTESIAN_POINT ( 'NONE',  ( 0.7573849235549129366, -45.49999999999999289, 29.19375250200204164 ) ) ;
#7649=DIRECTION ( 'NONE',  ( 1.000000000000000000, -0.000000000000000000, 1.224646799147353207E-16 ) ) ;
#7664=CARTESIAN_POINT ( 'NONE',  ( 7.567941867304905479, -45.55312500047794799, 29.19375250200204164 ) ) ;
#7678=VECTOR ( 'NONE', #7429, 1000.000000000000000 ) ;
#7695=CARTESIAN_POINT ( 'NONE',  ( 7.567941867304905479, -49.55312500047794799, 29.19375250200204164 ) ) ;
#7699=CARTESIAN_POINT ( 'NONE',  ( 7.757384923554904610, -43.20833333333332860, 27.17302655983835180 ) ) ;
#7701=CARTESIAN_POINT ( 'NONE',  ( 7.311496322569527528, -49.48412794485479083, 30.96332654542574403 ) ) ;
#7705=CARTESIAN_POINT ( 'NONE',  ( 2.602106451679909505, -45.30729166714461797, 32.06077891596451224 ) ) ;
#7710=EDGE_CURVE ( 'NONE', #26970, #3545, #40290, .T. ) ;
#7713=CARTESIAN_POINT ( 'NONE',  ( 4.257384923554908163, -46.87499999999999289, 33.23520438632941421 ) ) ;
#7715=CARTESIAN_POINT ( 'NONE',  ( 5.912663395429907709, -49.55729166714461087, 26.32672608803957459 ) ) ;
#7717=EDGE_LOOP ( 'NONE', ( #20247, #28571, #8687, #3839 ) ) ;
#7719=CARTESIAN_POINT ( 'NONE',  ( 3.535361955981045856, -43.30304719599500629, 25.74584789587558831 ) ) ;
#7727=CARTESIAN_POINT ( 'NONE',  ( 2.507384923554911715, -49.27708333428924448, 26.16266358875650866 ) ) ;
#7736=DIRECTION ( 'NONE',  ( -0.000000000000000000, -1.000000000000000000, -0.000000000000000000 ) ) ;
#7739=CARTESIAN_POINT ( 'NONE',  ( 1.707895049979424540, -44.63445127038220051, 31.62829771472926055 ) ) ;
#7750=ORIENTED_EDGE ( 'NONE', *, *, #39674, .F. ) ;
#7754=CARTESIAN_POINT ( 'NONE',  ( 5.912663395429904156, -42.72395833381127517, 32.06077891596451224 ) ) ;
#7756=EDGE_CURVE ( 'NONE', #631, #13147, #426, .T. ) ;
#7764=EDGE_LOOP ( 'NONE', ( #31302, #34801, #12715 ) ) ;
#7765=CARTESIAN_POINT ( 'NONE',  ( 6.007384923554904610, -45.36395833323773275, 32.22484141524757462 ) ) ;
#7770=CARTESIAN_POINT ( 'NONE',  ( 6.007384923554907274, -50.66666666666665719, 26.16266358875650866 ) ) ;
#7771=CARTESIAN_POINT ( 'NONE',  ( 7.757384923554905498, -44.44375000095590877, 29.19375250200204164 ) ) ;
#7787=CARTESIAN_POINT ( 'NONE',  ( 4.851202240586965253, -51.33290820753545347, 25.74134986343766229 ) ) ;
#7792=CARTESIAN_POINT ( 'NONE',  ( 4.257384923554909051, -52.75000000000000000, 32.69375250200203453 ) ) ;
#7794=LINE ( 'NONE', #10762, #20734 ) ;
#7809=CARTESIAN_POINT ( 'NONE',  ( 7.567941867304905479, -44.55312500047794799, 29.19375250200204164 ) ) ;
#7810=CARTESIAN_POINT ( 'NONE',  ( 7.757384923554905498, -47.74999999999999289, 29.19375250200204164 ) ) ;
#7818=CARTESIAN_POINT ( 'NONE',  ( 1.012938453569780295, -42.40351285130786607, 27.85020765150549238 ) ) ;
#7824=CARTESIAN_POINT ( 'NONE',  ( 0.9650653575388427052, -50.16678507030218981, 30.38157446731898403 ) ) ;
#7830=CARTESIAN_POINT ( 'NONE',  ( 7.757384923554905498, -48.44375000095590167, 29.19375250200204164 ) ) ;
#7838=CARTESIAN_POINT ( 'NONE',  ( 4.257384923554909051, -52.75000000000000000, 32.69375250200203453 ) ) ;
#7852=CARTESIAN_POINT ( 'NONE',  ( 6.003187684283656900, -43.02609810994699302, 32.26374296416377518 ) ) ;
#7864=CARTESIAN_POINT ( 'NONE',  ( 6.020051778985226143, -50.02506218355480172, 32.25200461302806332 ) ) ;
#7866=CARTESIAN_POINT ( 'NONE',  ( 4.257388422463325384, -49.06861128833901375, 32.69375250199872340 ) ) ;
#7875=ORIENTED_EDGE ( 'NONE', *, *, #16569, .T. ) ;
#7878=CARTESIAN_POINT ( 'NONE',  ( 0.9468279798049115126, -46.76145833381129080, 31.10510344464368515 ) ) ;
#7907=CARTESIAN_POINT ( 'NONE',  ( 7.567941867304905479, -48.55312500047794799, 29.19375250200204164 ) ) ;
#7911=CARTESIAN_POINT ( 'NONE',  ( 7.757384923554902834, -45.29166666666666430, 31.21447844416572792 ) ) ;
#7913=CARTESIAN_POINT ( 'NONE',  ( 7.755803369879989084, -49.45365190499531849, 29.66285495050615140 ) ) ;
#7917=CARTESIAN_POINT ( 'NONE',  ( 5.912663395429907709, -47.55729166714461087, 26.32672608803957459 ) ) ;
#7922=DIRECTION ( 'NONE',  ( 0.000000000000000000, 1.000000000000000000, 0.000000000000000000 ) ) ;
#7925=CARTESIAN_POINT ( 'NONE',  ( 6.007384923554904610, -48.33333333333332860, 32.22484141524757462 ) ) ;
#7926=CARTESIAN_POINT ( 'NONE',  ( 2.602106451679912169, -51.47395833381127517, 26.32672608803957459 ) ) ;
#7929=CARTESIAN_POINT ( 'NONE',  ( 3.778689929657686353, -43.07812907436771610, 32.69375260931086302 ) ) ;
#7936=CARTESIAN_POINT ( 'NONE',  ( 7.757384923554905498, -45.94375000095590877, 29.19375250200204164 ) ) ;
#7945=CARTESIAN_POINT ( 'NONE',  ( 4.715551447165649890, -44.82907898347898623, 25.69375490737408896 ) ) ;
#7952=CARTESIAN_POINT ( 'NONE',  ( 0.8475292882116416404, -49.71573082094933227, 28.28100721189862554 ) ) ;
#7963=CARTESIAN_POINT ( 'NONE',  ( 4.257384923554909051, -43.01562500047794657, 25.37105061671875461 ) ) ;
#7967=CARTESIAN_POINT ( 'NONE',  ( 6.505502237194838777, -44.51528588173866297, 31.89678446012991131 ) ) ;
#7970=CARTESIAN_POINT ( 'NONE',  ( 2.507384923554909495, -46.94729166657106134, 32.22484141524756751 ) ) ;
#7977=CARTESIAN_POINT ( 'NONE',  ( 2.602106451679911281, -50.88645833381127659, 26.32672608803957459 ) ) ;
#7993=LINE ( 'NONE', #1401, #15309 ) ;
#7995=CARTESIAN_POINT ( 'NONE',  ( 0.7573849235549129366, -46.49999999999999289, 29.19375250200204164 ) ) ;
#8001=CARTESIAN_POINT ( 'NONE',  ( 0.7573849235549138248, -49.54166666666665719, 27.17302655983835180 ) ) ;
#8009=CARTESIAN_POINT ( 'NONE',  ( 0.9468279798049132889, -49.89062500047794657, 29.19375250200204164 ) ) ;
#8018=ORIENTED_EDGE ( 'NONE', *, *, #16772, .F. ) ;
#8021=CARTESIAN_POINT ( 'NONE',  ( 3.496534321434709103, -50.30229481474027153, 25.75334213162221531 ) ) ;
#8023=ORIENTED_EDGE ( 'NONE', *, *, #41636, .T. ) ;
#8025=( BOUNDED_CURVE ( )  B_SPLINE_CURVE ( 2, ( #39358, #7263, #33197, #23207, #36611, #36174, #882, #662, #36396 ),
 .UNSPECIFIED., .F., .T. ) 
 B_SPLINE_CURVE_WITH_KNOTS ( ( 3, 2, 2, 2, 3 ),
 ( 0.4625000000000000222, 0.4666666666666666741, 0.4749999999999999778, 0.4833333333333333370, 0.4874999999999999889 ),
 .UNSPECIFIED. ) 
 CURVE ( )  GEOMETRIC_REPRESENTATION_ITEM ( )  RATIONAL_B_SPLINE_CURVE ( ( 0.9330127018922194093, 0.9330127018922198534, 1.000000000000000000, 0.8660254037844387076, 1.000000000000000000, 0.8660254037844387076, 1.000000000000000000, 0.9330127018922194093, 0.9330127018922194093 ) ) 
 REPRESENTATION_ITEM ( '' )  );
#8029=CARTESIAN_POINT ( 'NONE',  ( 6.007384923554904610, -50.52708333428924448, 32.22484141524757462 ) ) ;
#8030=CARTESIAN_POINT ( 'NONE',  ( 0.9468279798049124008, -42.34895833381128227, 31.10510344464368515 ) ) ;
#8032=ORIENTED_EDGE ( 'NONE', *, *, #6609, .F. ) ;
#8056=ORIENTED_EDGE ( 'NONE', *, *, #28567, .F. ) ;
#8070=EDGE_LOOP ( 'NONE', ( #12086, #39127, #16895, #2524 ) ) ;
#8073=CARTESIAN_POINT ( 'NONE',  ( 4.257384923554908163, -45.17812500047794799, 33.01645438728532866 ) ) ;
#8077=EDGE_CURVE ( 'NONE', #29198, #7238, #22646, .T. ) ;
#8087=CARTESIAN_POINT ( 'NONE',  ( 4.257386978954926349, -46.06866506076136147, 32.69375250200084793 ) ) ;
#8089=FACE_OUTER_BOUND ( 'NONE', #10464, .T. ) ;
#8103=CARTESIAN_POINT ( 'NONE',  ( 2.602106451679911281, -49.38645833381128369, 26.32672608803957459 ) ) ;
#8108=CARTESIAN_POINT ( 'NONE',  ( 6.007384923554907274, -45.16666666666665719, 26.16266358875650866 ) ) ;
#8110=ORIENTED_EDGE ( 'NONE', *, *, #1747, .T. ) ;
#8111=CARTESIAN_POINT ( 'NONE',  ( 7.548154475579048395, -49.41670159172083032, 28.00142196154426344 ) ) ;
#8112=CARTESIAN_POINT ( 'NONE',  ( 0.7950706427006638544, -49.17571997047964771, 29.91638407858596693 ) ) ;
#8114=CARTESIAN_POINT ( 'NONE',  ( 0.9468279798049143992, -47.43229166714461087, 27.28240155936039812 ) ) ;
#8115=CARTESIAN_POINT ( 'NONE',  ( 5.912663395429905044, -47.13645833381128369, 32.06077891596451224 ) ) ;
#8122=CARTESIAN_POINT ( 'NONE',  ( 6.007384923554904610, -44.33333333333332149, 32.22484141524757462 ) ) ;
#8123=CARTESIAN_POINT ( 'NONE',  ( 0.9468279798049132889, -48.39062500047794657, 29.19375250200204164 ) ) ;
#8126=FACE_OUTER_BOUND ( 'NONE', #39962, .T. ) ;
#8133=CARTESIAN_POINT ( 'NONE',  ( 4.257384923554909051, -48.31875000095590167, 25.15230061767466552 ) ) ;
#8135=VECTOR ( 'NONE', #38662, 1000.000000000000000 ) ;
#8150=CARTESIAN_POINT ( 'NONE',  ( 2.105048086681646780, -49.76764037802448115, 26.39595594772032427 ) ) ;
#8158=ORIENTED_EDGE ( 'NONE', *, *, #3250, .F. ) ;
#8160=CARTESIAN_POINT ( 'NONE',  ( 6.431115608063843858, -43.87294227602484398, 26.42218229702558574 ) ) ;
#8169=CARTESIAN_POINT ( 'NONE',  ( 4.257384923554909051, -44.65562499990439704, 25.15230061767466552 ) ) ;
#8172=ORIENTED_EDGE ( 'NONE', *, *, #16575, .F. ) ;
#8178=CARTESIAN_POINT ( 'NONE',  ( 4.257384923554908163, -51.67812500047794799, 33.01645438728532866 ) ) ;
#8179=DIRECTION ( 'NONE',  ( -0.000000000000000000, -1.000000000000000000, -0.000000000000000000 ) ) ;
#8196=CARTESIAN_POINT ( 'NONE',  ( 2.507384923554911715, -46.58333333333332149, 26.16266358875650866 ) ) ;
#8198=DIRECTION ( 'NONE',  ( -0.000000000000000000, -1.000000000000000000, -0.000000000000000000 ) ) ;
#8207=ORIENTED_EDGE ( 'NONE', *, *, #41194, .F. ) ;
#8210=CARTESIAN_POINT ( 'NONE',  ( 2.602106451679912169, -50.47395833381128227, 26.32672608803957459 ) ) ;
#8215=CARTESIAN_POINT ( 'NONE',  ( 7.757384923554905498, -46.24999999999999289, 29.19375250200204164 ) ) ;
#8218=ORIENTED_EDGE ( 'NONE', *, *, #10764, .F. ) ;
#8227=ORIENTED_EDGE ( 'NONE', *, *, #37827, .F. ) ;
#8232=CARTESIAN_POINT ( 'NONE',  ( 4.257384923554908163, -50.06875000095590877, 33.23520438632941421 ) ) ;
#8233=CARTESIAN_POINT ( 'NONE',  ( 2.602106451679912169, -43.47395833381127517, 26.32672608803957459 ) ) ;
#8243=VERTEX_POINT ( 'NONE', #31230 ) ;
#8263=CARTESIAN_POINT ( 'NONE',  ( 4.257384923554919709, -49.37499999999997868, 32.69375250200203453 ) ) ;
#8271=( BOUNDED_SURFACE ( )  B_SPLINE_SURFACE ( 1, 2, ( 
 ( #22241, #31394, #2261, #8426, #18217, #15244, #40973, #21611, #41609, #28204, #6075, #5242, #12465, #12035, #41190, #31186, #5663, #41826, #24823, #37988, #8850, #25027, #21405, #24607, #25231, #15881, #38196, #25449, #8639, #41399, #12247, #9060, #38410, #34382, #31606, #2890, #19054, #18426, #22036, #11826, #21825, #5449, #35213, #15455, #35011, #5873, #34797, #18641, #2471, #9275, #18845, #32024, #28410, #28826, #31804, #37573, #2679, #2046, #15665, #28621, #27994, #15029, #37782, #34585, #16096, #38826, #9703, #25862, #29035, #23287, #22447, #16702, #38617, #7125, #9484, #42032, #3928, #20098, #36040, #3105, #26485, #35427, #33061, #6701, #35640, #6504, #32642, #16908, #6289, #39029, #26280, #29875, #12884, #12677, #35839, #19473, #19263, #22664, #32441, #32235, #3304, #16292, #13496, #26072, #29232, #108, #9914, #22871, #13088, #25656, #16498, #39441, #19670, #3506, #29447, #318, #13298, #36252, #39228, #10110, #23074, #6908, #19883, #32849, #3714, #29659, #525, #10314, #7970, #14138, #14565, #11164, #40506, #7547, #20520, #26694, #36472, #33494, #17123, #39872, #17751, #4355, #24348, #23510, #30722, #30298, #17336, #7335, #23933, #17957, #960, #27113, #40082, #1169, #39656, #743, #1375, #34118, #14351, #1587, #26907, #17541, #30507, #27328, #27541, #10527, #7765, #21145, #37317, #36683, #40295, #30087, #10948, #23719, #11363, #33713, #24149, #37118, #36902, #20738, #4564, #20939, #33910, #8169, #4770, #4977, #13715, #20305, #33274, #4138, #13927, #10734, #34535, #31137, #34330, #14977, #27943, #1993, #5192, #41555, #40704, #34952, #14774, #25395, #27735, #18167, #22192, #38356, #12194, #21356, #2624, #11561, #9219, #24977, #11773, #24769, #8799, #35161, #24554, #15186, #2418, #6025, #40915, #30935, #11984, #37732, #37519, #8590, #21562, #8377, #5395, #18373, #31754, #2205, #31344, #28149, #41137, #37938, #21771, #1792, #34743 ),
 ( #5612, #18586, #25186, #31549, #38147, #9004, #15406, #21983, #28358, #41344, #5821, #18794, #15610, #28568, #12409, #16445, #35790, #265, #16652, #41766, #12623, #35586, #32589, #6652, #19617, #36198, #39387, #26017, #29179, #19212, #19001, #3455, #6237, #31968, #10061, #29610, #28981, #3048, #15824, #13039, #16040, #26433, #29394, #10265, #16238, #25602, #23231, #2838, #28771, #9429, #6448, #26231, #23022, #38983, #9864, #41978, #25810, #13447, #22819, #32183, #19420, #477, #38562, #35990, #22395, #35373, #12826, #38776, #9646, #22607, #13247, #32390, #32794, #3255, #57, #39179, #6856, #19828, #3666, #14518, #16862, #33443, #20687, #27489, #23458, #7071, #30251, #30036, #691, #20258, #36423, #26644, #7288, #13661, #7925, #20475, #39602, #39827, #4304, #17288, #10477, #1536, #10902, #33864, #20050, #1123, #11312, #40458, #14094, #30671, #24299, #27068, #10690, #40033, #23673, #33224, #36636, #13878, #7500, #1331, #14302, #23887, #20891, #17498, #4723, #26857, #36853, #33013, #4087, #7713, #17071, #907, #24099, #33665, #3881, #29824, #37068, #4516, #30460, #27281, #40245, #11114, #17702, #8537, #21515, #27891, #21099, #37269, #37885, #28516, #8743, #12138, #21306, #11932, #24926, #21719, #8951, #34072, #2149, #15558, #18744, #31089, #34691, #24506, #1942, #18118, #34902, #28099, #5558, #18532, #40865, #37680, #14924, #21925, #31500, #38096, #41084, #5770, #2368, #11719, #40656, #34484, #24718, #37473, #11513, #34278, #5141, #8329, #5343, #18317, #8122, #28307, #31706, #31290, #15136, #4927, #15358, #41291, #2574, #25131, #41504, #12356, #17908, #30886, #1745, #14727, #27684, #13360, #33126, #16974, #3784, #16768, #9379, #32706, #20373, #19954, #12568, #383, #591, #39726, #7194, #29728, #13565, #6977, #16562, #36323, #812, #13783, #32917, #26551, #39508, #10383, #38514, #10600, #33340, #23578, #41713, #29939, #26342, #25554, #39290 ),
 ( #4208, #23359, #6763, #19737, #20168, #17189, #35112, #10170, #3991, #30150, #22344, #25340, #26763, #3568, #18951, #35322, #29516, #2786, #23138, #31915, #36537, #36106, #15767, #7400, #1028, #38300, #28720, #9166, #22141, #5976, #26974, #24207, #18224, #34388, #8029, #37579, #31193, #11224, #17609, #33975, #4628, #14203, #30572, #20800, #1441, #8232, #21206, #27388, #27796, #24406, #11622, #33773, #14413, #39936, #7611, #40360, #30362, #11013, #30992, #37175, #8434, #36748, #1849, #21000, #4833, #20587, #17811, #13999, #1235, #30781, #36970, #24617, #1643, #11418, #37374, #14625, #27596, #40564, #40767, #34177, #14828, #5036, #21411, #18015, #7830, #17402, #5248, #10800, #27180, #40146, #23999, #23782, #33562, #4422, #12684, #11832, #6083, #28000, #38625, #40982, #18433, #35434, #9490, #25455, #34593, #15888, #24831, #22455, #38203, #25034, #37996, #22042, #6295, #37789, #28417, #15671, #19269, #31401, #2053, #25238, #8857, #8645, #15253, #2267, #21616, #28210, #5455, #2896, #15463, #41199, #34804, #41406, #12253, #12041, #15037, #5880, #28832, #21831, #9066, #5670, #18647, #35017, #25662, #31613, #18851, #2477, #31814, #2686, #28627, #41616, #12471, #38417, #9281, #22248, #35221, #41832, #19060, #32030, #114, #13095, #3111, #42038, #26078, #22670, #32447, #16708, #29241, #10322, #12892, #29668, #39036, #9920, #25869, #19678, #33068, #6511, #22879, #35845, #6708, #16101, #32244, #23082, #29042, #32857, #23296, #32648, #6915, #19893, #3723, #20105, #35647, #10117, #38833, #9709, #3514, #532, #19479, #16505, #3313, #29455, #326, #16299, #13305, #26289, #13505, #39236, #26493, #36048, #39448, #36261, #7133, #717, #30276, #32617, #7100, #36449, #1149, #39206, #22846, #3905, #3693, #16473, #36019, #10086, #292, #23050, #29422, #23698, #36228, #13275, #13474, #20076, #33039, #26258, #17314, #26670, #7527, #35815, #16887, #27092, #14117 ) ),
 .UNSPECIFIED., .F., .F., .T. ) 
 B_SPLINE_SURFACE_WITH_KNOTS ( ( 2, 1, 2 ),
 ( 3, 2, 2, 2, 2, 2, 2, 2, 2, 2, 2, 2, 2, 2, 2, 2, 2, 2, 2, 2, 2, 2, 2, 2, 2, 2, 2, 2, 2, 2, 2, 2, 2, 2, 2, 2, 2, 2, 2, 2, 2, 2, 2, 2, 2, 2, 2, 2, 2, 2, 2, 2, 2, 2, 2, 2, 2, 2, 2, 2, 2, 2, 2, 2, 2, 2, 2, 2, 2, 2, 2, 2, 2, 2, 2, 2, 2, 2, 2, 2, 2, 2, 2, 2, 2, 2, 2, 2, 2, 2, 2, 2, 2, 2, 2, 2, 2, 2, 2, 2, 2, 2, 2, 2, 2, 2, 2, 2, 2, 2, 2, 2, 2, 2, 2, 2, 2, 2, 2, 2, 3 ),
 ( -0.1000000000000000056, 0.000000000000000000, 1.000000000000000000 ),
 ( 0.000000000000000000, 0.008333333333333333218, 0.01666666666666666644, 0.02500000000000000139, 0.03333333333333333287, 0.04166666666666666435, 0.05000000000000000278, 0.05833333333333333426, 0.06666666666666666574, 0.07499999999999999722, 0.08333333333333332871, 0.09166666666666666019, 0.1000000000000000056, 0.1083333333333333370, 0.1166666666666666685, 0.1250000000000000000, 0.1333333333333333315, 0.1416666666666666630, 0.1499999999999999944, 0.1583333333333333259, 0.1666666666666666574, 0.1749999999999999889, 0.1833333333333333204, 0.1916666666666666796, 0.2000000000000000111, 0.2083333333333333426, 0.2166666666666666741, 0.2250000000000000056, 0.2333333333333333370, 0.2416666666666666685, 0.2500000000000000000, 0.2583333333333333592, 0.2666666666666666630, 0.2750000000000000222, 0.2833333333333333259, 0.2916666666666666852, 0.2999999999999999889, 0.3083333333333333481, 0.3166666666666666519, 0.3250000000000000111, 0.3333333333333333148, 0.3416666666666666741, 0.3499999999999999778, 0.3583333333333333370, 0.3666666666666666408, 0.3750000000000000000, 0.3833333333333333592, 0.3916666666666666630, 0.4000000000000000222, 0.4083333333333333259, 0.4166666666666666852, 0.4249999999999999889, 0.4333333333333333481, 0.4416666666666666519, 0.4500000000000000111, 0.4583333333333333148, 0.4666666666666666741, 0.4749999999999999778, 0.4833333333333333370, 0.4916666666666666408, 0.5000000000000000000, 0.5083333333333333037, 0.5166666666666667185, 0.5250000000000000222, 0.5333333333333333259, 0.5416666666666666297, 0.5500000000000000444, 0.5583333333333333481, 0.5666666666666666519, 0.5749999999999999556, 0.5833333333333333703, 0.5916666666666666741, 0.5999999999999999778, 0.6083333333333332815, 0.6166666666666666963, 0.6250000000000000000, 0.6333333333333333037, 0.6416666666666667185, 0.6500000000000000222, 0.6583333333333333259, 0.6666666666666666297, 0.6750000000000000444, 0.6833333333333333481, 0.6916666666666666519, 0.6999999999999999556, 0.7083333333333333703, 0.7166666666666666741, 0.7249999999999999778, 0.7333333333333332815, 0.7416666666666666963, 0.7500000000000000000, 0.7583333333333333037, 0.7666666666666667185, 0.7750000000000000222, 0.7833333333333333259, 0.7916666666666666297, 0.8000000000000000444, 0.8083333333333333481, 0.8166666666666666519, 0.8249999999999999556, 0.8333333333333333703, 0.8416666666666666741, 0.8499999999999999778, 0.8583333333333332815, 0.8666666666666666963, 0.8750000000000000000, 0.8833333333333333037, 0.8916666666666667185, 0.9000000000000000222, 0.9083333333333333259, 0.9166666666666666297, 0.9250000000000000444, 0.9333333333333333481, 0.9416666666666666519, 0.9499999999999999556, 0.9583333333333333703, 0.9666666666666666741, 0.9749999999999999778, 0.9833333333333332815, 0.9845487628594339347, 0.9943942504880283195 ),
 .UNSPECIFIED. ) 
 GEOMETRIC_REPRESENTATION_ITEM ( )  RATIONAL_B_SPLINE_SURFACE ( (
 ( 1.000000000000000000, 0.8660254037844387076, 1.000000000000000000, 0.8660254037844387076, 1.000000000000000000, 0.8660254037844387076, 1.000000000000000000, 0.8660254037844387076, 1.000000000000000000, 0.8660254037844387076, 1.000000000000000000, 0.8660254037844387076, 1.000000000000000000, 0.8660254037844387076, 1.000000000000000000, 0.8660254037844387076, 1.000000000000000000, 0.8660254037844387076, 1.000000000000000000, 0.8660254037844387076, 1.000000000000000000, 0.8660254037844387076, 1.000000000000000000, 0.8660254037844387076, 1.000000000000000000, 0.8660254037844387076, 1.000000000000000000, 0.8660254037844387076, 1.000000000000000000, 0.8660254037844387076, 1.000000000000000000, 0.8660254037844387076, 1.000000000000000000, 0.8660254037844387076, 1.000000000000000000, 0.8660254037844387076, 1.000000000000000000, 0.8660254037844387076, 1.000000000000000000, 0.8660254037844387076, 1.000000000000000000, 0.8660254037844387076, 1.000000000000000000, 0.8660254037844387076, 1.000000000000000000, 0.8660254037844387076, 1.000000000000000000, 0.8660254037844387076, 1.000000000000000000, 0.8660254037844387076, 1.000000000000000000, 0.8660254037844387076, 1.000000000000000000, 0.8660254037844387076, 1.000000000000000000, 0.8660254037844387076, 1.000000000000000000, 0.8660254037844387076, 1.000000000000000000, 0.8660254037844387076, 1.000000000000000000, 0.8660254037844387076, 1.000000000000000000, 0.8660254037844387076, 1.000000000000000000, 0.8660254037844387076, 1.000000000000000000, 0.8660254037844387076, 1.000000000000000000, 0.8660254037844387076, 1.000000000000000000, 0.8660254037844387076, 1.000000000000000000, 0.8660254037844387076, 1.000000000000000000, 0.8660254037844387076, 1.000000000000000000, 0.8660254037844387076, 1.000000000000000000, 0.8660254037844387076, 1.000000000000000000, 0.8660254037844387076, 1.000000000000000000, 0.8660254037844387076, 1.000000000000000000, 0.8660254037844387076, 1.000000000000000000, 0.8660254037844387076, 1.000000000000000000, 0.8660254037844387076, 1.000000000000000000, 0.8660254037844387076, 1.000000000000000000, 0.8660254037844387076, 1.000000000000000000, 0.8660254037844387076, 1.000000000000000000, 0.8660254037844387076, 1.000000000000000000, 0.8660254037844387076, 1.000000000000000000, 0.8660254037844387076, 1.000000000000000000, 0.8660254037844387076, 1.000000000000000000, 0.8660254037844387076, 1.000000000000000000, 0.8660254037844387076, 1.000000000000000000, 0.8660254037844387076, 1.000000000000000000, 0.8660254037844387076, 1.000000000000000000, 0.8660254037844387076, 1.000000000000000000, 0.8660254037844387076, 1.000000000000000000, 0.8660254037844387076, 1.000000000000000000, 0.8660254037844387076, 1.000000000000000000, 0.8660254037844387076, 1.000000000000000000, 0.8660254037844387076, 1.000000000000000000, 0.8660254037844387076, 1.000000000000000000, 0.8660254037844387076, 1.000000000000000000, 0.8660254037844387076, 1.000000000000000000, 0.8660254037844387076, 1.000000000000000000, 0.8660254037844387076, 1.000000000000000000, 0.8660254037844387076, 1.000000000000000000, 0.8660254037844387076, 1.000000000000000000, 0.8660254037844387076, 1.000000000000000000, 0.8660254037844387076, 1.000000000000000000, 0.8660254037844387076, 1.000000000000000000, 0.8660254037844387076, 1.000000000000000000, 0.8660254037844387076, 1.000000000000000000, 0.8660254037844387076, 1.000000000000000000, 0.8660254037844387076, 1.000000000000000000, 0.8660254037844387076, 1.000000000000000000, 0.8660254037844387076, 1.000000000000000000, 0.8660254037844387076, 1.000000000000000000, 0.8660254037844387076, 1.000000000000000000, 0.8660254037844387076, 1.000000000000000000, 0.8660254037844387076, 1.000000000000000000, 0.8660254037844387076, 1.000000000000000000, 0.8660254037844387076, 1.000000000000000000, 0.8660254037844387076, 1.000000000000000000, 0.8660254037844387076, 1.000000000000000000, 0.8660254037844387076, 1.000000000000000000, 0.8660254037844387076, 1.000000000000000000, 0.8660254037844387076, 1.000000000000000000, 0.8660254037844387076, 1.000000000000000000, 0.8660254037844387076, 1.000000000000000000, 0.8660254037844387076, 1.000000000000000000, 0.8660254037844387076, 1.000000000000000000, 0.8660254037844387076, 1.000000000000000000, 0.8660254037844387076, 1.000000000000000000, 0.8660254037844387076, 1.000000000000000000, 0.8660254037844387076, 1.000000000000000000, 0.8660254037844387076, 1.000000000000000000, 0.8660254037844387076, 1.000000000000000000, 0.8660254037844387076, 1.000000000000000000, 0.8660254037844387076, 1.000000000000000000, 0.8660254037844387076, 1.000000000000000000, 0.8660254037844387076, 1.000000000000000000, 0.8660254037844387076, 1.000000000000000000, 0.8660254037844387076, 1.000000000000000000, 0.8660254037844387076, 1.000000000000000000, 0.8660254037844387076, 1.000000000000000000, 0.8660254037844387076, 1.000000000000000000, 0.8660254037844387076, 1.000000000000000000, 0.8660254037844387076, 1.000000000000000000, 0.8660254037844387076, 1.000000000000000000, 0.8660254037844387076, 1.000000000000000000, 0.8660254037844387076, 1.000000000000000000, 0.8660254037844387076, 1.000000000000000000, 0.8660254037844387076, 1.000000000000000000, 0.8660254037844387076, 1.000000000000000000, 0.8660254037844387076, 1.000000000000000000, 0.8660254037844387076, 1.000000000000000000, 0.9804595984014634613, 0.9666191922560610772, 0.9666191922560610772, 0.9666191922560610772),
 ( 1.000000000000000000, 0.8660254037844387076, 1.000000000000000000, 0.8660254037844387076, 1.000000000000000000, 0.8660254037844387076, 1.000000000000000000, 0.8660254037844387076, 1.000000000000000000, 0.8660254037844387076, 1.000000000000000000, 0.8660254037844387076, 1.000000000000000000, 0.8660254037844387076, 1.000000000000000000, 0.8660254037844387076, 1.000000000000000000, 0.8660254037844387076, 1.000000000000000000, 0.8660254037844387076, 1.000000000000000000, 0.8660254037844387076, 1.000000000000000000, 0.8660254037844387076, 1.000000000000000000, 0.8660254037844387076, 1.000000000000000000, 0.8660254037844387076, 1.000000000000000000, 0.8660254037844387076, 1.000000000000000000, 0.8660254037844387076, 1.000000000000000000, 0.8660254037844387076, 1.000000000000000000, 0.8660254037844387076, 1.000000000000000000, 0.8660254037844387076, 1.000000000000000000, 0.8660254037844387076, 1.000000000000000000, 0.8660254037844387076, 1.000000000000000000, 0.8660254037844387076, 1.000000000000000000, 0.8660254037844387076, 1.000000000000000000, 0.8660254037844387076, 1.000000000000000000, 0.8660254037844387076, 1.000000000000000000, 0.8660254037844387076, 1.000000000000000000, 0.8660254037844387076, 1.000000000000000000, 0.8660254037844387076, 1.000000000000000000, 0.8660254037844387076, 1.000000000000000000, 0.8660254037844387076, 1.000000000000000000, 0.8660254037844387076, 1.000000000000000000, 0.8660254037844387076, 1.000000000000000000, 0.8660254037844387076, 1.000000000000000000, 0.8660254037844387076, 1.000000000000000000, 0.8660254037844387076, 1.000000000000000000, 0.8660254037844387076, 1.000000000000000000, 0.8660254037844387076, 1.000000000000000000, 0.8660254037844387076, 1.000000000000000000, 0.8660254037844387076, 1.000000000000000000, 0.8660254037844387076, 1.000000000000000000, 0.8660254037844387076, 1.000000000000000000, 0.8660254037844387076, 1.000000000000000000, 0.8660254037844387076, 1.000000000000000000, 0.8660254037844387076, 1.000000000000000000, 0.8660254037844387076, 1.000000000000000000, 0.8660254037844387076, 1.000000000000000000, 0.8660254037844387076, 1.000000000000000000, 0.8660254037844387076, 1.000000000000000000, 0.8660254037844387076, 1.000000000000000000, 0.8660254037844387076, 1.000000000000000000, 0.8660254037844387076, 1.000000000000000000, 0.8660254037844387076, 1.000000000000000000, 0.8660254037844387076, 1.000000000000000000, 0.8660254037844387076, 1.000000000000000000, 0.8660254037844387076, 1.000000000000000000, 0.8660254037844387076, 1.000000000000000000, 0.8660254037844387076, 1.000000000000000000, 0.8660254037844387076, 1.000000000000000000, 0.8660254037844387076, 1.000000000000000000, 0.8660254037844387076, 1.000000000000000000, 0.8660254037844387076, 1.000000000000000000, 0.8660254037844387076, 1.000000000000000000, 0.8660254037844387076, 1.000000000000000000, 0.8660254037844387076, 1.000000000000000000, 0.8660254037844387076, 1.000000000000000000, 0.8660254037844387076, 1.000000000000000000, 0.8660254037844387076, 1.000000000000000000, 0.8660254037844387076, 1.000000000000000000, 0.8660254037844387076, 1.000000000000000000, 0.8660254037844387076, 1.000000000000000000, 0.8660254037844387076, 1.000000000000000000, 0.8660254037844387076, 1.000000000000000000, 0.8660254037844387076, 1.000000000000000000, 0.8660254037844387076, 1.000000000000000000, 0.8660254037844387076, 1.000000000000000000, 0.8660254037844387076, 1.000000000000000000, 0.8660254037844387076, 1.000000000000000000, 0.8660254037844387076, 1.000000000000000000, 0.8660254037844387076, 1.000000000000000000, 0.8660254037844387076, 1.000000000000000000, 0.8660254037844387076, 1.000000000000000000, 0.8660254037844387076, 1.000000000000000000, 0.8660254037844387076, 1.000000000000000000, 0.8660254037844387076, 1.000000000000000000, 0.8660254037844387076, 1.000000000000000000, 0.8660254037844387076, 1.000000000000000000, 0.8660254037844387076, 1.000000000000000000, 0.8660254037844387076, 1.000000000000000000, 0.8660254037844387076, 1.000000000000000000, 0.8660254037844387076, 1.000000000000000000, 0.8660254037844387076, 1.000000000000000000, 0.8660254037844387076, 1.000000000000000000, 0.8660254037844387076, 1.000000000000000000, 0.8660254037844387076, 1.000000000000000000, 0.8660254037844387076, 1.000000000000000000, 0.8660254037844387076, 1.000000000000000000, 0.8660254037844387076, 1.000000000000000000, 0.8660254037844387076, 1.000000000000000000, 0.8660254037844387076, 1.000000000000000000, 0.8660254037844387076, 1.000000000000000000, 0.8660254037844387076, 1.000000000000000000, 0.8660254037844387076, 1.000000000000000000, 0.8660254037844387076, 1.000000000000000000, 0.8660254037844387076, 1.000000000000000000, 0.8660254037844387076, 1.000000000000000000, 0.8660254037844387076, 1.000000000000000000, 0.8660254037844387076, 1.000000000000000000, 0.8660254037844387076, 1.000000000000000000, 0.8660254037844387076, 1.000000000000000000, 0.8660254037844387076, 1.000000000000000000, 0.8660254037844387076, 1.000000000000000000, 0.8660254037844387076, 1.000000000000000000, 0.8660254037844387076, 1.000000000000000000, 0.8660254037844387076, 1.000000000000000000, 0.8660254037844387076, 1.000000000000000000, 0.8660254037844387076, 1.000000000000000000, 0.8660254037844387076, 1.000000000000000000, 0.8660254037844387076, 1.000000000000000000, 0.9804595984014634613, 0.9666191922560610772, 0.9666191922560610772, 0.9666191922560610772),
 ( 1.000000000000000000, 0.8660254037844387076, 1.000000000000000000, 0.8660254037844387076, 1.000000000000000000, 0.8660254037844387076, 1.000000000000000000, 0.8660254037844387076, 1.000000000000000000, 0.8660254037844387076, 1.000000000000000000, 0.8660254037844387076, 1.000000000000000000, 0.8660254037844387076, 1.000000000000000000, 0.8660254037844387076, 1.000000000000000000, 0.8660254037844387076, 1.000000000000000000, 0.8660254037844387076, 1.000000000000000000, 0.8660254037844387076, 1.000000000000000000, 0.8660254037844387076, 1.000000000000000000, 0.8660254037844387076, 1.000000000000000000, 0.8660254037844387076, 1.000000000000000000, 0.8660254037844387076, 1.000000000000000000, 0.8660254037844387076, 1.000000000000000000, 0.8660254037844387076, 1.000000000000000000, 0.8660254037844387076, 1.000000000000000000, 0.8660254037844387076, 1.000000000000000000, 0.8660254037844387076, 1.000000000000000000, 0.8660254037844387076, 1.000000000000000000, 0.8660254037844387076, 1.000000000000000000, 0.8660254037844387076, 1.000000000000000000, 0.8660254037844387076, 1.000000000000000000, 0.8660254037844387076, 1.000000000000000000, 0.8660254037844387076, 1.000000000000000000, 0.8660254037844387076, 1.000000000000000000, 0.8660254037844387076, 1.000000000000000000, 0.8660254037844387076, 1.000000000000000000, 0.8660254037844387076, 1.000000000000000000, 0.8660254037844387076, 1.000000000000000000, 0.8660254037844387076, 1.000000000000000000, 0.8660254037844387076, 1.000000000000000000, 0.8660254037844387076, 1.000000000000000000, 0.8660254037844387076, 1.000000000000000000, 0.8660254037844387076, 1.000000000000000000, 0.8660254037844387076, 1.000000000000000000, 0.8660254037844387076, 1.000000000000000000, 0.8660254037844387076, 1.000000000000000000, 0.8660254037844387076, 1.000000000000000000, 0.8660254037844387076, 1.000000000000000000, 0.8660254037844387076, 1.000000000000000000, 0.8660254037844387076, 1.000000000000000000, 0.8660254037844387076, 1.000000000000000000, 0.8660254037844387076, 1.000000000000000000, 0.8660254037844387076, 1.000000000000000000, 0.8660254037844387076, 1.000000000000000000, 0.8660254037844387076, 1.000000000000000000, 0.8660254037844387076, 1.000000000000000000, 0.8660254037844387076, 1.000000000000000000, 0.8660254037844387076, 1.000000000000000000, 0.8660254037844387076, 1.000000000000000000, 0.8660254037844387076, 1.000000000000000000, 0.8660254037844387076, 1.000000000000000000, 0.8660254037844387076, 1.000000000000000000, 0.8660254037844387076, 1.000000000000000000, 0.8660254037844387076, 1.000000000000000000, 0.8660254037844387076, 1.000000000000000000, 0.8660254037844387076, 1.000000000000000000, 0.8660254037844387076, 1.000000000000000000, 0.8660254037844387076, 1.000000000000000000, 0.8660254037844387076, 1.000000000000000000, 0.8660254037844387076, 1.000000000000000000, 0.8660254037844387076, 1.000000000000000000, 0.8660254037844387076, 1.000000000000000000, 0.8660254037844387076, 1.000000000000000000, 0.8660254037844387076, 1.000000000000000000, 0.8660254037844387076, 1.000000000000000000, 0.8660254037844387076, 1.000000000000000000, 0.8660254037844387076, 1.000000000000000000, 0.8660254037844387076, 1.000000000000000000, 0.8660254037844387076, 1.000000000000000000, 0.8660254037844387076, 1.000000000000000000, 0.8660254037844387076, 1.000000000000000000, 0.8660254037844387076, 1.000000000000000000, 0.8660254037844387076, 1.000000000000000000, 0.8660254037844387076, 1.000000000000000000, 0.8660254037844387076, 1.000000000000000000, 0.8660254037844387076, 1.000000000000000000, 0.8660254037844387076, 1.000000000000000000, 0.8660254037844387076, 1.000000000000000000, 0.8660254037844387076, 1.000000000000000000, 0.8660254037844387076, 1.000000000000000000, 0.8660254037844387076, 1.000000000000000000, 0.8660254037844387076, 1.000000000000000000, 0.8660254037844387076, 1.000000000000000000, 0.8660254037844387076, 1.000000000000000000, 0.8660254037844387076, 1.000000000000000000, 0.8660254037844387076, 1.000000000000000000, 0.8660254037844387076, 1.000000000000000000, 0.8660254037844387076, 1.000000000000000000, 0.8660254037844387076, 1.000000000000000000, 0.8660254037844387076, 1.000000000000000000, 0.8660254037844387076, 1.000000000000000000, 0.8660254037844387076, 1.000000000000000000, 0.8660254037844387076, 1.000000000000000000, 0.8660254037844387076, 1.000000000000000000, 0.8660254037844387076, 1.000000000000000000, 0.8660254037844387076, 1.000000000000000000, 0.8660254037844387076, 1.000000000000000000, 0.8660254037844387076, 1.000000000000000000, 0.8660254037844387076, 1.000000000000000000, 0.8660254037844387076, 1.000000000000000000, 0.8660254037844387076, 1.000000000000000000, 0.8660254037844387076, 1.000000000000000000, 0.8660254037844387076, 1.000000000000000000, 0.8660254037844387076, 1.000000000000000000, 0.8660254037844387076, 1.000000000000000000, 0.8660254037844387076, 1.000000000000000000, 0.8660254037844387076, 1.000000000000000000, 0.8660254037844387076, 1.000000000000000000, 0.8660254037844387076, 1.000000000000000000, 0.8660254037844387076, 1.000000000000000000, 0.8660254037844387076, 1.000000000000000000, 0.8660254037844387076, 1.000000000000000000, 0.8660254037844387076, 1.000000000000000000, 0.8660254037844387076, 1.000000000000000000, 0.8660254037844387076, 1.000000000000000000, 0.9804595984014634613, 0.9666191922560610772, 0.9666191922560610772, 0.9666191922560610772) ) ) 
 REPRESENTATION_ITEM ( '' )  SURFACE ( )  );
#8274=VERTEX_POINT ( 'NONE', #34841 ) ;
#8282=CARTESIAN_POINT ( 'NONE',  ( 4.257384923554908163, -43.67812500047794799, 33.01645438728532866 ) ) ;
#8283=DIRECTION ( 'NONE',  ( 0.000000000000000000, -1.000000000000000000, -0.000000000000000000 ) ) ;
#8296=CARTESIAN_POINT ( 'NONE',  ( 6.007384923554907274, -45.66666666666666430, 26.16266358875650866 ) ) ;
#8310=CARTESIAN_POINT ( 'NONE',  ( 2.602106451679911281, -49.88645833381128369, 26.32672608803957459 ) ) ;
#8315=CARTESIAN_POINT ( 'NONE',  ( 7.757384923554905498, -45.24999999999999289, 29.19375250200204164 ) ) ;
#8317=CARTESIAN_POINT ( 'NONE',  ( 4.272717523592460154, -49.31911502300007299, 25.69378392957671764 ) ) ;
#8320=CARTESIAN_POINT ( 'NONE',  ( 0.9468279798049132889, -47.39062500047794657, 29.19375250200204164 ) ) ;
#8321=EDGE_CURVE ( 'NONE', #31713, #9899, #1189, .T. ) ;
#8322=CARTESIAN_POINT ( 'NONE',  ( 5.912663395429905044, -47.63645833381128369, 32.06077891596451224 ) ) ;
#8324=ORIENTED_EDGE ( 'NONE', *, *, #30169, .F. ) ;
#8325=FACE_OUTER_BOUND ( 'NONE', #25023, .T. ) ;
#8326=CARTESIAN_POINT ( 'NONE',  ( 4.257384923554909051, -52.75000000000000000, 29.19375250200204164 ) ) ;
#8329=CARTESIAN_POINT ( 'NONE',  ( 0.7573849235549120484, -44.45833333333332149, 31.21447844416572792 ) ) ;
#8330=CARTESIAN_POINT ( 'NONE',  ( 7.567941867304902814, -49.18229166714461087, 31.10510344464368870 ) ) ;
#8332=FACE_OUTER_BOUND ( 'NONE', #7764, .T. ) ;
#8339=ORIENTED_EDGE ( 'NONE', *, *, #5200, .T. ) ;
#8340=CARTESIAN_POINT ( 'NONE',  ( 2.507384923554909495, -47.11041666762257307, 32.22484141524756751 ) ) ;
#8342=SHAPE_REPRESENTATION_RELATIONSHIP ( 'NONE' , 'NONE' ,  #33982, #33566 ) ;
#8354=CARTESIAN_POINT ( 'NONE',  ( 4.257384924376430568, -51.81875000097547002, 25.69375250200204519 ) ) ;
#8355=LINE ( 'NONE', #24746, #25013 ) ;
#8367=CARTESIAN_POINT ( 'NONE',  ( 2.602106451679909505, -43.30729166714461797, 32.06077891596451224 ) ) ;
#8373=CARTESIAN_POINT ( 'NONE',  ( 7.685709041677953657, -44.46633436916538784, 30.11653414308214494 ) ) ;
#8377=CARTESIAN_POINT ( 'NONE',  ( 7.757384923554904610, -42.73895833323773275, 27.17302655983835180 ) ) ;
#8381=CARTESIAN_POINT ( 'NONE',  ( 2.531011446252514840, -43.60986721335597593, 32.24760195695999698 ) ) ;
#8382=CARTESIAN_POINT ( 'NONE',  ( 5.912663395429905044, -51.63645833381128369, 32.06077891596451224 ) ) ;
#8396=CARTESIAN_POINT ( 'NONE',  ( 6.007384923554907274, -43.16666666666665719, 26.16266358875650866 ) ) ;
#8398=CARTESIAN_POINT ( 'NONE',  ( 4.257384923554907274, -46.37499999999999289, 32.69375250200203453 ) ) ;
#8414=CARTESIAN_POINT ( 'NONE',  ( 7.567941867304902814, -51.18229166714461797, 31.10510344464368870 ) ) ;
#8415=CARTESIAN_POINT ( 'NONE',  ( 3.319562750045980337, -48.60267090063072715, 25.69375250200204519 ) ) ;
#8417=CARTESIAN_POINT ( 'NONE',  ( 4.257385003886612118, -45.31875000283309163, 25.69375250200204874 ) ) ;
#8419=CARTESIAN_POINT ( 'NONE',  ( 2.602106451679909505, -51.71979166714461940, 32.06077891596451224 ) ) ;
#8426=CARTESIAN_POINT ( 'NONE',  ( 4.257384923554909051, -52.15562499990439704, 25.15230061767466552 ) ) ;
#8428=VERTEX_POINT ( 'NONE', #35887 ) ;
#8432=CARTESIAN_POINT ( 'NONE',  ( 7.344996782761040066, -42.40485064068575838, 27.54531907653889888 ) ) ;
#8434=CARTESIAN_POINT ( 'NONE',  ( 7.757384923554905498, -49.44375000095590167, 29.19375250200204164 ) ) ;
#8435=CARTESIAN_POINT ( 'NONE',  ( 4.257384923554909051, 5.249999999999997335, 29.19375250200204164 ) ) ;
#8437=VERTEX_POINT ( 'NONE', #6553 ) ;
#8462=CARTESIAN_POINT ( 'NONE',  ( 4.257393644456948678, -47.56839819610503639, 32.69375250198117300 ) ) ;
#8467=CARTESIAN_POINT ( 'NONE',  ( 4.257384923554909051, -52.75000000000000000, 29.19375250200204164 ) ) ;
#8471=CARTESIAN_POINT ( 'NONE',  ( 7.499097361181975785, -48.97792384355577866, 30.61680336016634740 ) ) ;
#8484=CARTESIAN_POINT ( 'NONE',  ( 7.567941867304904591, -43.59479166714461229, 31.10510344464368870 ) ) ;
#8486=AXIS2_PLACEMENT_3D ( 'NONE', #27693, #24726, #11520 ) ;
#8490=CARTESIAN_POINT ( 'NONE',  ( 6.007384923554904610, -44.83333333333332149, 32.22484141524757462 ) ) ;
#8516=CARTESIAN_POINT ( 'NONE',  ( 2.602106451679911281, -44.88645833381128369, 26.32672608803957459 ) ) ;
#8521=CARTESIAN_POINT ( 'NONE',  ( 2.507384923554909495, -44.91666666666665719, 32.22484141524756751 ) ) ;
#8528=CARTESIAN_POINT ( 'NONE',  ( 7.567941867304902814, -47.18229166714461797, 31.10510344464368870 ) ) ;
#8529=CYLINDRICAL_SURFACE ( 'NONE', #26569, 10.16127960363519200 ) ;
#8530=CARTESIAN_POINT ( 'NONE',  ( 7.567941867304905479, -47.55312500047795510, 29.19375250200204164 ) ) ;
#8533=CARTESIAN_POINT ( 'NONE',  ( 4.257384923554909939, -42.40485061181025372, 24.19375250200203453 ) ) ;
#8537=CARTESIAN_POINT ( 'NONE',  ( 7.757384923554902834, -46.29166666666665719, 31.21447844416572792 ) ) ;
#8538=CARTESIAN_POINT ( 'NONE',  ( 0.9468279798049132889, -48.89062500047794657, 29.19375250200204164 ) ) ;
#8545=VERTEX_POINT ( 'NONE', #20358 ) ;
#8550=CARTESIAN_POINT ( 'NONE',  ( 4.257384923554909051, -46.31875000095590877, 25.15230061767466552 ) ) ;
#8568=CARTESIAN_POINT ( 'NONE',  ( 0.7568403900594281586, -49.70525479967141536, 28.73943170402002778 ) ) ;
#8581=CARTESIAN_POINT ( 'NONE',  ( 4.257384923554908163, -42.76562500047794657, 33.01645438728532866 ) ) ;
#8585=CARTESIAN_POINT ( 'NONE',  ( 6.012486179341784975, -44.36149487455679719, 26.14869758701784974 ) ) ;
#8590=CARTESIAN_POINT ( 'NONE',  ( 7.757384923554902834, -42.82229166657106845, 31.21447844416572792 ) ) ;
#8596=CARTESIAN_POINT ( 'NONE',  ( 5.912663395429907709, -51.46979166714461940, 26.32672608803957459 ) ) ;
#8613=CARTESIAN_POINT ( 'NONE',  ( 3.319562750045979005, -46.39732909936925864, 32.69375250200202743 ) ) ;
#8626=CARTESIAN_POINT ( 'NONE',  ( 0.9468279798049132889, -51.89062500047794657, 29.19375250200204164 ) ) ;
#8636=ORIENTED_EDGE ( 'NONE', *, *, #18361, .T. ) ;
#8639=CARTESIAN_POINT ( 'NONE',  ( 2.507384923554911715, -51.11395833323773985, 26.16266358875650866 ) ) ;
#8645=CARTESIAN_POINT ( 'NONE',  ( 7.757384923554904610, -46.90208333428923027, 27.17302655983835180 ) ) ;
#8648=CARTESIAN_POINT ( 'NONE',  ( 4.257384923554909051, -52.75000000000000000, 29.19375250200204164 ) ) ;
#8672=EDGE_CURVE ( 'NONE', #5244, #2991, #15606, .T. ) ;
#8677=CARTESIAN_POINT ( 'NONE',  ( 6.900449678350088156, -49.00186627713353005, 31.50469661487660744 ) ) ;
#8687=ORIENTED_EDGE ( 'NONE', *, *, #17608, .T. ) ;
#8688=VERTEX_POINT ( 'NONE', #15448 ) ;
#8692=CARTESIAN_POINT ( 'NONE',  ( 7.567941867304905479, -43.05312500047794799, 29.19375250200204164 ) ) ;
#8696=CARTESIAN_POINT ( 'NONE',  ( 4.257384923554931255, -44.87499999999998579, 32.69375250200203453 ) ) ;
#8708=DIRECTION ( 'NONE',  ( 0.000000000000000000, 0.000000000000000000, -1.000000000000000000 ) ) ;
#8714=EDGE_CURVE ( 'NONE', #4835, #19251, #18838, .T. ) ;
#8716=CARTESIAN_POINT ( 'NONE',  ( 5.101241539050272777, -45.54811274992092507, 32.60856463385103865 ) ) ;
#8729=CARTESIAN_POINT ( 'NONE',  ( 6.486252034663674060, -49.37456221794578681, 26.45810428671586578 ) ) ;
#8732=CARTESIAN_POINT ( 'NONE',  ( 0.9468279798049132889, -44.39062500047794657, 29.19375250200204164 ) ) ;
#8734=CARTESIAN_POINT ( 'NONE',  ( 7.567941867304902814, -45.09479166714461940, 31.10510344464368870 ) ) ;
#8743=CARTESIAN_POINT ( 'NONE',  ( 0.7573849235549129366, -45.99999999999999289, 29.19375250200204164 ) ) ;
#8744=CARTESIAN_POINT ( 'NONE',  ( 0.9468279798049124008, -47.34895833381128938, 31.10510344464368515 ) ) ;
#8748=CARTESIAN_POINT ( 'NONE',  ( 3.884137871020911792, 3.250000000000000444, 23.25209069347974022 ) ) ;
#8757=CARTESIAN_POINT ( 'NONE',  ( 6.007384923554907274, -46.86041666762257307, 26.16266358875650866 ) ) ;
#8773=DIRECTION ( 'NONE',  ( 0.000000000000000000, 0.000000000000000000, -1.000000000000000000 ) ) ;
#8777=CARTESIAN_POINT ( 'NONE',  ( 4.723334405713389472, -50.82897607747590740, 25.69375284710765683 ) ) ;
#8780=CARTESIAN_POINT ( 'NONE',  ( 2.507384923554911715, -50.58333333333332860, 26.16266358875650866 ) ) ;
#8783=CARTESIAN_POINT ( 'NONE',  ( 2.507384923554911715, -49.08333333333332860, 26.16266358875650866 ) ) ;
#8793=CARTESIAN_POINT ( 'NONE',  ( 7.567941867304904591, -50.59895833381128227, 27.28240155936039812 ) ) ;
#8799=CARTESIAN_POINT ( 'NONE',  ( 7.757384923554905498, -43.28062499990439704, 29.19375250200204164 ) ) ;
#8805=CARTESIAN_POINT ( 'NONE',  ( 7.757384923554905498, -43.74999999999999289, 29.19375250200204164 ) ) ;
#8806=CARTESIAN_POINT ( 'NONE',  ( 0.9468279798049115126, -50.26145833381128369, 31.10510344464368515 ) ) ;
#8813=AXIS2_PLACEMENT_3D ( 'NONE', #25266, #31845, #28653 ) ;
#8835=ORIENTED_EDGE ( 'NONE', *, *, #5340, .F. ) ;
#8837=CARTESIAN_POINT ( 'NONE',  ( 7.567941867304902814, -51.68229166714461797, 31.10510344464368870 ) ) ;
#8839=CARTESIAN_POINT ( 'NONE',  ( 2.103542921812969979, -45.12041828996618165, 31.99045087826605283 ) ) ;
#8850=CARTESIAN_POINT ( 'NONE',  ( 2.507384923554909495, -51.44729166657106845, 32.22484141524756751 ) ) ;
#8851=EDGE_CURVE ( 'NONE', #11420, #38358, #946, .T. ) ;
#8856=CARTESIAN_POINT ( 'NONE',  ( 7.683827143474763588, -42.45975875323841819, 29.94732443707984970 ) ) ;
#8857=CARTESIAN_POINT ( 'NONE',  ( 7.757384923554905498, -46.94375000095590877, 29.19375250200204164 ) ) ;
#8859=ORIENTED_EDGE ( 'NONE', *, *, #28194, .T. ) ;
#8863=CARTESIAN_POINT ( 'NONE',  ( 4.145602678882920777, -46.81609267449614009, 25.69527593769323914 ) ) ;
#8875=CARTESIAN_POINT ( 'NONE',  ( 4.257384923554909051, -42.40485061181025372, 29.19375250200204164 ) ) ;
#8886=CARTESIAN_POINT ( 'NONE',  ( 1.059960492504041563, -48.22644895421416322, 27.76917647441567993 ) ) ;
#8891=CARTESIAN_POINT ( 'NONE',  ( 4.257384923554907274, -43.87499999999999289, 32.69375250200203453 ) ) ;
#8892=CARTESIAN_POINT ( 'NONE',  ( 7.757384923554902834, -48.79166666666665719, 31.21447844416572792 ) ) ;
#8901=LINE ( 'NONE', #28882, #37520 ) ;
#8906=CARTESIAN_POINT ( 'NONE',  ( 0.9468279798049115126, -44.76145833381128369, 31.10510344464368515 ) ) ;
#8919=CARTESIAN_POINT ( 'NONE',  ( 7.757384923554904610, -45.70833333333332149, 27.17302655983835180 ) ) ;
#8926=CARTESIAN_POINT ( 'NONE',  ( 5.946155649072560223, -45.52853994753701272, 32.25959167152854690 ) ) ;
#8930=CARTESIAN_POINT ( 'NONE',  ( 0.7573849235549129366, -50.99999999999999289, 29.19375250200204164 ) ) ;
#8936=CARTESIAN_POINT ( 'NONE',  ( 2.507384923554909495, -42.91666666666665719, 32.22484141524756751 ) ) ;
#8941=CARTESIAN_POINT ( 'NONE',  ( 7.567941867304902814, -45.18229166714461797, 31.10510344464368870 ) ) ;
#8942=CARTESIAN_POINT ( 'NONE',  ( 7.567941867304905479, -45.05312500047794799, 29.19375250200204164 ) ) ;
#8945=ORIENTED_EDGE ( 'NONE', *, *, #10851, .F. ) ;
#8951=CARTESIAN_POINT ( 'NONE',  ( 7.757384923554905498, -45.74999999999999289, 29.19375250200204164 ) ) ;
#8952=CARTESIAN_POINT ( 'NONE',  ( 2.602106451679912169, -46.97395833381128227, 26.32672608803957459 ) ) ;
#8966=CARTESIAN_POINT ( 'NONE',  ( 0.7573849235549129366, -45.69375000095590877, 29.19375250200204164 ) ) ;
#8968=( LENGTH_UNIT ( ) NAMED_UNIT ( * ) SI_UNIT ( .MILLI., .METRE. ) );
#8973=AXIS2_PLACEMENT_3D ( 'NONE', #39973, #7649, #37824 ) ;
#8991=CARTESIAN_POINT ( 'NONE',  ( 2.507384923554911715, -51.08333333333332860, 26.16266358875650866 ) ) ;
#8997=CARTESIAN_POINT ( 'NONE',  ( 7.049840346354167231, -50.38940380233340477, 27.03487094519274692 ) ) ;
#9000=CARTESIAN_POINT ( 'NONE',  ( 2.878398474557042341, -51.10137576128364145, 32.41096674978382453 ) ) ;
#9004=CARTESIAN_POINT ( 'NONE',  ( 0.7573849235549138248, -52.04166666666666430, 27.17302655983835180 ) ) ;
#9012=CARTESIAN_POINT ( 'NONE',  ( 7.567941867304904591, -49.09479166714461940, 31.10510344464368870 ) ) ;
#9016=CARTESIAN_POINT ( 'NONE',  ( 6.007384923554904610, -51.52708333428923737, 32.22484141524757462 ) ) ;
#9045=ORIENTED_EDGE ( 'NONE', *, *, #41299, .T. ) ;
#9048=CARTESIAN_POINT ( 'NONE',  ( 2.602106451679912169, -48.47395833381128227, 26.32672608803957459 ) ) ;
#9060=CARTESIAN_POINT ( 'NONE',  ( 0.7573849235549120484, -50.98895833323773985, 31.21447844416572792 ) ) ;
#9065=DIRECTION ( 'NONE',  ( -0.000000000000000000, -1.000000000000000000, -0.000000000000000000 ) ) ;
#9066=CARTESIAN_POINT ( 'NONE',  ( 0.7573849235549129366, -46.19375000095590877, 29.19375250200204164 ) ) ;
#9072=CARTESIAN_POINT ( 'NONE',  ( 1.171970729110777931, -46.65292105772387288, 30.93680740961659126 ) ) ;
#9075=ADVANCED_FACE ( 'NONE', ( #37011 ), #34430, .T. ) ;
#9089=CARTESIAN_POINT ( 'NONE',  ( 7.757384923554904610, -42.70833333333332149, 27.17302655983835180 ) ) ;
#9098=CARTESIAN_POINT ( 'NONE',  ( 4.232664640759728591, -46.31816152816268328, 25.69382713205364865 ) ) ;
#9106=CARTESIAN_POINT ( 'NONE',  ( 5.746197110196767710, -48.03326372875569916, 32.36491846050388688 ) ) ;
#9116=CARTESIAN_POINT ( 'NONE',  ( 7.567941867304904591, -42.59479166714461940, 31.10510344464368870 ) ) ;
#9117=CARTESIAN_POINT ( 'NONE',  ( 2.732834801182218776, -42.10504881339334560, 32.35500496278447002 ) ) ;
#9138=CARTESIAN_POINT ( 'NONE',  ( 6.595764855467499466, -45.51206314043998447, 31.82289193860904319 ) ) ;
#9139=B_SPLINE_CURVE_WITH_KNOTS ( 'NONE', 3,
 ( #10587, #4411, #30350, #16756, #1222, #39925, #20792, #581, #10787, #17389, #4195, #13985, #23988, #36524, #23567, #7388, #36736, #27168, #40133, #39280, #11001, #36956, #33762, #16553, #33116, #10162, #39498, #23129, #3981 ),
 .UNSPECIFIED., .F., .F.,
 ( 4, 2, 1, 2, 2, 1, 1, 2, 2, 2, 2, 2, 2, 2, 2, 4 ),
 ( 0.3431936459176440635, 0.3439747730041011198, 0.3441700547757153839, 0.3441944649971671599, 0.3442188752186189360, 0.3442676956615225436, 0.3443653365473296479, 0.3447559000905581761, 0.3463181542634722887, 0.3494426626093005139, 0.3525671709551286837, 0.3556916793009569089, 0.3588161876467850786, 0.3619406959926133038, 0.3650652043384414736, 0.3681897126842696988 ),
 .UNSPECIFIED. ) ;
#9143=CARTESIAN_POINT ( 'NONE',  ( 1.002754673719796985, -45.72340132160120874, 27.90561301744746459 ) ) ;
#9149=CARTESIAN_POINT ( 'NONE',  ( 4.257384923554908163, -42.87499999999998579, 33.23520438632941421 ) ) ;
#9151=CARTESIAN_POINT ( 'NONE',  ( 4.248057434019180789, -42.81852792667460506, 25.69376412581424418 ) ) ;
#9154=CARTESIAN_POINT ( 'NONE',  ( 7.567941867304904591, -45.14062500047794657, 29.19375250200204164 ) ) ;
#9155=CARTESIAN_POINT ( 'NONE',  ( 5.912663395429907709, -43.96979166714461940, 26.32672608803957459 ) ) ;
#9165=CARTESIAN_POINT ( 'NONE',  ( 4.624068042992287353, -47.06206013212894135, 32.69375259986968274 ) ) ;
#9166=CARTESIAN_POINT ( 'NONE',  ( 4.257384923554909051, -50.81875000095590877, 25.15230061767466552 ) ) ;
#9167=CARTESIAN_POINT ( 'NONE',  ( 2.602106451679909505, -45.80729166714461797, 32.06077891596451224 ) ) ;
#9168=ORIENTED_EDGE ( 'NONE', *, *, #5578, .T. ) ;
#9194=CYLINDRICAL_SURFACE ( 'NONE', #31411, 3.499999999999996003 ) ;
#9204=CARTESIAN_POINT ( 'NONE',  ( 4.257384923554909051, -51.12499999999998579, 25.15230061767466552 ) ) ;
#9210=CARTESIAN_POINT ( 'NONE',  ( 4.257384923554907274, -51.37499999999998579, 32.69375250200203453 ) ) ;
#9212=CARTESIAN_POINT ( 'NONE',  ( 7.309609189845841293, -50.39981609718487476, 27.42104161388248684 ) ) ;
#9219=CARTESIAN_POINT ( 'NONE',  ( 2.507384923554909495, -43.44729166657106845, 32.22484141524756751 ) ) ;
#9220=CARTESIAN_POINT ( 'NONE',  ( 4.257384923554909051, 0.8500000000000035305, 19.03247289836684786 ) ) ;
#9225=CARTESIAN_POINT ( 'NONE',  ( 5.912663395429907709, -49.96979166714461940, 26.32672608803957459 ) ) ;
#9235=EDGE_CURVE ( 'NONE', #38358, #9447, #35720, .T. ) ;
#9245=CARTESIAN_POINT ( 'NONE',  ( 5.195207097063835988, -46.85267090063072715, 32.69375250200204164 ) ) ;
#9262=CARTESIAN_POINT ( 'NONE',  ( 5.912663395429907709, -47.55729166714461087, 26.32672608803957459 ) ) ;
#9275=CARTESIAN_POINT ( 'NONE',  ( 7.757384923554904610, -50.23895833323773275, 27.17302655983835180 ) ) ;
#9278=VERTEX_POINT ( 'NONE', #2521 ) ;
#9281=CARTESIAN_POINT ( 'NONE',  ( 2.507384923554909495, -45.61041666762256597, 32.22484141524756751 ) ) ;
#9288=EDGE_CURVE ( 'NONE', #37984, #19510, #8901, .T. ) ;
#9298=CARTESIAN_POINT ( 'NONE',  ( 3.649388371515208007, -51.80427389259929782, 25.69375250200204164 ) ) ;
#9305=CARTESIAN_POINT ( 'NONE',  ( 4.257384923554909051, -42.62499999999998579, 25.69375250200204519 ) ) ;
#9311=CARTESIAN_POINT ( 'NONE',  ( 1.022893204820070290, -48.16298578482678039, 30.53246160498033390 ) ) ;
#9315=CARTESIAN_POINT ( 'NONE',  ( 7.567941867304904591, -46.09479166714460519, 31.10510344464368870 ) ) ;
#9318=CARTESIAN_POINT ( 'NONE',  ( 0.7573849235549129366, -49.99999999999998579, 29.19375250200204164 ) ) ;
#9323=CARTESIAN_POINT ( 'NONE',  ( 7.434302941516371277, -47.90961851546533978, 27.72498157714251832 ) ) ;
#9337=CARTESIAN_POINT ( 'NONE',  ( 7.307774966076294731, -42.40391780584809567, 27.47736923338838011 ) ) ;
#9354=CARTESIAN_POINT ( 'NONE',  ( 7.434308360410959438, -45.40961882154294926, 27.72499329931801171 ) ) ;
#9358=CARTESIAN_POINT ( 'NONE',  ( 1.556826442781300335, -45.74720036570938930, 26.92546344081617349 ) ) ;
#9359=CARTESIAN_POINT ( 'NONE',  ( -1.074868669588189274, 3.250000000000000444, 26.54616302712299358 ) ) ;
#9365=CARTESIAN_POINT ( 'NONE',  ( 0.7573849235549138248, -42.54166666666665719, 27.17302655983835180 ) ) ;
#9370=CARTESIAN_POINT ( 'NONE',  ( 2.602106451679909505, -44.80729166714461797, 32.06077891596451224 ) ) ;
#9371=CARTESIAN_POINT ( 'NONE',  ( 2.602106451679909505, -43.71979166714461940, 32.06077891596451224 ) ) ;
#9379=CARTESIAN_POINT ( 'NONE',  ( 2.507384923554909495, -43.41666666666665719, 32.22484141524756751 ) ) ;
#9380=CARTESIAN_POINT ( 'NONE',  ( 0.9468279798049124008, -44.84895833381128227, 31.10510344464368515 ) ) ;
#9415=CARTESIAN_POINT ( 'NONE',  ( 7.757386089165675180, -47.43265851066849592, 28.73561324964162367 ) ) ;
#9417=CARTESIAN_POINT ( 'NONE',  ( 7.757384923554905498, -48.74999999999998579, 29.19375250200204164 ) ) ;
#9422=CARTESIAN_POINT ( 'NONE',  ( 7.040307338499027345, -43.39140885012515980, 27.06990054365128628 ) ) ;
#9423=CARTESIAN_POINT ( 'NONE',  ( 7.567941867304904591, -51.59895833381127517, 27.28240155936039812 ) ) ;
#9426=CARTESIAN_POINT ( 'NONE',  ( 0.8715102345420511210, -51.21537385160661415, 28.19956573226468421 ) ) ;
#9429=CARTESIAN_POINT ( 'NONE',  ( 7.757384923554904610, -50.20833333333332860, 27.17302655983835180 ) ) ;
#9432=CARTESIAN_POINT ( 'NONE',  ( 2.873188380932412134, -43.60172089658139782, 32.40881808356178340 ) ) ;
#9434=CARTESIAN_POINT ( 'NONE',  ( 0.9468279798049115126, -49.26145833381128369, 31.10510344464368515 ) ) ;
#9437=CARTESIAN_POINT ( 'NONE',  ( 0.7694785405755856234, -48.68761166175606547, 29.48446378192401696 ) ) ;
#9447=VERTEX_POINT ( 'NONE', #32496 ) ;
#9470=CARTESIAN_POINT ( 'NONE',  ( 5.912663395429904156, -47.22395833381128227, 32.06077891596451224 ) ) ;
#9476=CARTESIAN_POINT ( 'NONE',  ( 2.602106451679911281, -50.38645833381128369, 26.32672608803957459 ) ) ;
#9483=ORIENTED_EDGE ( 'NONE', *, *, #20926, .F. ) ;
#9484=CARTESIAN_POINT ( 'NONE',  ( 6.007384923554907274, -49.19729166657106845, 26.16266358875650866 ) ) ;
#9490=CARTESIAN_POINT ( 'NONE',  ( 0.7573849235549129366, -47.69375000095590877, 29.19375250200204164 ) ) ;
#9505=CARTESIAN_POINT ( 'NONE',  ( 4.257384923554909051, -51.62499999999999289, 25.69375250200204519 ) ) ;
#9508=CARTESIAN_POINT ( 'NONE',  ( 0.7573819988493579736, -51.70010665539159334, 28.88547886669008946 ) ) ;
#9526=CARTESIAN_POINT ( 'NONE',  ( 0.8281788362723863095, -46.17826680364034786, 29.90904940899214637 ) ) ;
#9528=CARTESIAN_POINT ( 'NONE',  ( 5.912663395429905044, -45.63645833381128369, 32.06077891596451224 ) ) ;
#9530=CARTESIAN_POINT ( 'NONE',  ( 4.257384923554919709, -48.87499999999998579, 32.69375250200203453 ) ) ;
#9538=CARTESIAN_POINT ( 'NONE',  ( 7.421826608251363311, -47.90891937123841871, 27.69829092125678116 ) ) ;
#9539=ADVANCED_FACE ( 'NONE', ( #23354 ), #36316, .T. ) ;
#9548=CARTESIAN_POINT ( 'NONE',  ( 3.208483784363420632, -50.79526363627021368, 25.84466283885256033 ) ) ;
#9560=EDGE_CURVE ( 'NONE', #20255, #39859, #11795, .T. ) ;
#9563=DIRECTION ( 'NONE',  ( -0.000000000000000000, -1.000000000000000000, -0.000000000000000000 ) ) ;
#9574=CARTESIAN_POINT ( 'NONE',  ( 3.384437249246886825, -45.79861159814041827, 25.79721784803343709 ) ) ;
#9575=EDGE_CURVE ( 'NONE', #8688, #24091, #23993, .T. ) ;
#9581=ORIENTED_EDGE ( 'NONE', *, *, #16240, .T. ) ;
#9583=VECTOR ( 'NONE', #8179, 1000.000000000000000 ) ;
#9586=CARTESIAN_POINT ( 'NONE',  ( 4.257384923554909051, -43.01562500047794657, 25.37105061671875461 ) ) ;
#9587=CARTESIAN_POINT ( 'NONE',  ( 4.257384923554909051, -44.42812500047794799, 25.37105061671875106 ) ) ;
#9591=DIRECTION ( 'NONE',  ( -0.000000000000000000, -1.000000000000000000, -0.000000000000000000 ) ) ;
#9596=CARTESIAN_POINT ( 'NONE',  ( 7.567941867304902814, -45.68229166714462508, 31.10510344464368870 ) ) ;
#9606=ORIENTED_EDGE ( 'NONE', *, *, #37049, .F. ) ;
#9629=CARTESIAN_POINT ( 'NONE',  ( 0.9468279798049125118, -50.30312500047794799, 29.19375250200204164 ) ) ;
#9630=CARTESIAN_POINT ( 'NONE',  ( 7.056226643708400026, -47.39116790341027752, 27.04284925932331518 ) ) ;
#9633=CARTESIAN_POINT ( 'NONE',  ( 6.007384923554907274, -50.16666666666665719, 26.16266358875650866 ) ) ;
#9634=ORIENTED_EDGE ( 'NONE', *, *, #26030, .F. ) ;
#9637=CARTESIAN_POINT ( 'NONE',  ( 7.397164905045658934, -43.40677908233681848, 27.62152550366842618 ) ) ;
#9638=CARTESIAN_POINT ( 'NONE',  ( 2.602106451679909505, -50.80729166714461797, 32.06077891596451224 ) ) ;
#9641=CARTESIAN_POINT ( 'NONE',  ( 1.993328489047882401, -51.12571092256362704, 31.90082722451136732 ) ) ;
#9646=CARTESIAN_POINT ( 'NONE',  ( 2.507384923554909495, -49.41666666666665719, 32.22484141524756751 ) ) ;
#9651=CARTESIAN_POINT ( 'NONE',  ( 7.567941867304904591, -50.09479166714461229, 31.10510344464368870 ) ) ;
#9690=CARTESIAN_POINT ( 'NONE',  ( 4.257384923554908163, -46.76562500047794657, 33.01645438728532866 ) ) ;
#9693=VECTOR ( 'NONE', #4417, 1000.000000000000114 ) ;
#9697=CARTESIAN_POINT ( 'NONE',  ( 4.257384923554908163, -51.17812500047794799, 33.01645438728532866 ) ) ;
#9703=CARTESIAN_POINT ( 'NONE',  ( 0.7573849235549129366, -49.53062499990439704, 29.19375250200204164 ) ) ;
#9709=CARTESIAN_POINT ( 'NONE',  ( 7.757384923554904610, -43.90208333428925158, 27.17302655983835180 ) ) ;
#9724=CARTESIAN_POINT ( 'NONE',  ( 5.195207097063836876, -51.64732909936925154, 25.69375250200204519 ) ) ;
#9725=PRODUCT_DEFINITION_CONTEXT ( 'detailed design', #7343, 'design' ) ;
#9744=CARTESIAN_POINT ( 'NONE',  ( 0.9468279798049115126, -46.76145833381129080, 31.10510344464368515 ) ) ;
#9747=LINE ( 'NONE', #32064, #8135 ) ;
#9752=ADVANCED_FACE ( 'NONE', ( #33332 ), #8271, .T. ) ;
#9754=CARTESIAN_POINT ( 'NONE',  ( 7.417236664926148748, -47.90866548907692390, 27.68862998831227529 ) ) ;
#9788=CARTESIAN_POINT ( 'NONE',  ( 6.996214575651692691, -45.38966122731357444, 27.00126882110546944 ) ) ;
#9789=MANIFOLD_SOLID_BREP ( 'Cut-Extrude10', #17242 ) ;
#9792=CARTESIAN_POINT ( 'NONE',  ( 1.081981671424814051, -45.65953155659904183, 30.66585277509100749 ) ) ;
#9812=CARTESIAN_POINT ( 'NONE',  ( 4.257384923554909051, -45.01562500047794657, 25.37105061671875106 ) ) ;
#9848=CARTESIAN_POINT ( 'NONE',  ( 7.757384923554905498, -46.24999999999999289, 29.19375250200204164 ) ) ;
#9853=CIRCLE ( 'NONE', #30882, 3.499999999999996003 ) ;
#9855=CARTESIAN_POINT ( 'NONE',  ( 4.257363451562580003, -43.56959840651998661, 32.69375250187801640 ) ) ;
#9856=CARTESIAN_POINT ( 'NONE',  ( 7.567941867304902814, -48.18229166714461087, 31.10510344464368870 ) ) ;
#9864=CARTESIAN_POINT ( 'NONE',  ( 0.7573849235549129366, -49.99999999999998579, 29.19375250200204164 ) ) ;
#9867=CARTESIAN_POINT ( 'NONE',  ( 2.785110068302266040, -43.60380459902658856, 32.36909148889228760 ) ) ;
#9873=CARTESIAN_POINT ( 'NONE',  ( 3.933779999948343153, -48.57614691426380915, 32.69375250526948662 ) ) ;
#9876=CARTESIAN_POINT ( 'NONE',  ( 0.7573849235549138248, -51.73541666762258018, 27.17302655983835180 ) ) ;
#9877=VECTOR ( 'NONE', #9888, 1000.000000000000000 ) ;
#9888=DIRECTION ( 'NONE',  ( -0.000000000000000000, -1.000000000000000000, -0.000000000000000000 ) ) ;
#9899=VERTEX_POINT ( 'NONE', #8354 ) ;
#9902=CARTESIAN_POINT ( 'NONE',  ( 2.602106451679912169, -44.47395833381127517, 26.32672608803957459 ) ) ;
#9907=CARTESIAN_POINT ( 'NONE',  ( 7.567941867304905479, -51.51145833381128369, 27.28240155936039457 ) ) ;
#9914=CARTESIAN_POINT ( 'NONE',  ( 6.007384923554904610, -47.86395833323773275, 32.22484141524757462 ) ) ;
#9920=CARTESIAN_POINT ( 'NONE',  ( 4.257384923554909051, -44.81875000095590877, 25.15230061767466552 ) ) ;
#9935=CARTESIAN_POINT ( 'NONE',  ( 7.757384923554904610, -51.70833333333332149, 27.17302655983835180 ) ) ;
#9940=FACE_OUTER_BOUND ( 'NONE', #25591, .T. ) ;
#9947=CARTESIAN_POINT ( 'NONE',  ( 4.257384923554909051, -52.24999999999999289, 29.19375250200204164 ) ) ;
#9949=CARTESIAN_POINT ( 'NONE',  ( 4.257384923554909051, -41.90485061181026083, 29.19375250200204164 ) ) ;
#9956=CARTESIAN_POINT ( 'NONE',  ( 4.257384923554909051, -45.42812500047795510, 25.37105061671875461 ) ) ;
#9971=CARTESIAN_POINT ( 'NONE',  ( 2.977923052860024900, -50.59921341509968329, 32.45151693723130393 ) ) ;
#9990=CARTESIAN_POINT ( 'NONE',  ( 0.7573849235549129366, -47.99999999999999289, 29.19375250200204164 ) ) ;
#9993=CARTESIAN_POINT ( 'NONE',  ( 3.853489023972045402, -45.57615526562285879, 32.69375262531539050 ) ) ;
#10001=CARTESIAN_POINT ( 'NONE',  ( 4.257384923414707423, -42.56875000095865147, 32.69375250200203453 ) ) ;
#10010=( BOUNDED_CURVE ( )  B_SPLINE_CURVE ( 2, ( #886, #19807, #20240, #241, #13224, #30013, #32776, #23652, #10241 ),
 .UNSPECIFIED., .F., .F. ) 
 B_SPLINE_CURVE_WITH_KNOTS ( ( 3, 2, 2, 2, 3 ),
 ( 0.7874999999999999778, 0.7916666666666666297, 0.8000000000000000444, 0.8083333333333333481, 0.8125000000000000000 ),
 .UNSPECIFIED. ) 
 CURVE ( )  GEOMETRIC_REPRESENTATION_ITEM ( )  RATIONAL_B_SPLINE_CURVE ( ( 0.9330127018922194093, 0.9330127018922194093, 1.000000000000000000, 0.8660254037844387076, 1.000000000000000000, 0.8660254037844387076, 1.000000000000000000, 0.9330127018922194093, 0.9330127018922194093 ) ) 
 REPRESENTATION_ITEM ( '' )  );
#10012=DIRECTION ( 'NONE',  ( -0.8329741740894178736, 0.000000000000000000, 0.5533118698347725406 ) ) ;
#10013=CARTESIAN_POINT ( 'NONE',  ( 0.9468279798049132889, -44.89062500047794657, 29.19375250200204164 ) ) ;
#10022=ORIENTED_EDGE ( 'NONE', *, *, #11016, .F. ) ;
#10023=ADVANCED_FACE ( 'NONE', ( #28545 ), #24955, .T. ) ;
#10041=CARTESIAN_POINT ( 'NONE',  ( 2.602106451679911281, -51.38645833381127659, 26.32672608803957459 ) ) ;
#10042=LINE ( 'NONE', #38548, #35370 ) ;
#10045=CARTESIAN_POINT ( 'NONE',  ( 4.257384923554909051, -48.12499999999998579, 25.15230061767466552 ) ) ;
#10051=CARTESIAN_POINT ( 'NONE',  ( 5.318571071633443559, -43.34235963978197503, 25.85157020721602450 ) ) ;
#10052=CARTESIAN_POINT ( 'NONE',  ( 0.9468279798049143992, -49.93229166714461087, 27.28240155936039812 ) ) ;
#10056=ADVANCED_FACE ( 'NONE', ( #38332 ), #9194, .T. ) ;
#10061=CARTESIAN_POINT ( 'NONE',  ( 6.007384923554904610, -50.83333333333332860, 32.22484141524757462 ) ) ;
#10063=CARTESIAN_POINT ( 'NONE',  ( 7.632842012204433146, -46.42179389685124846, 28.16118920018944749 ) ) ;
#10066=CARTESIAN_POINT ( 'NONE',  ( 1.185792583776665854, -48.73362267974268747, 27.45169794356740667 ) ) ;
#10069=CARTESIAN_POINT ( 'NONE',  ( 4.257384923554909051, -50.31875000095590877, 25.15230061767466552 ) ) ;
#10084=CARTESIAN_POINT ( 'NONE',  ( 2.975064734268261013, -42.40508397444173738, 32.45039488375558534 ) ) ;
#10086=CARTESIAN_POINT ( 'NONE',  ( 0.7573849235549120484, -42.65208333428924448, 31.21447844416572792 ) ) ;
#10098=CARTESIAN_POINT ( 'NONE',  ( 5.912663395429904156, -46.22395833381128227, 32.06077891596451224 ) ) ;
#10103=CARTESIAN_POINT ( 'NONE',  ( 0.9468279798049125118, -50.80312500047794799, 29.19375250200204164 ) ) ;
#10110=CARTESIAN_POINT ( 'NONE',  ( 7.757384923554902834, -47.32229166657106845, 31.21447844416572792 ) ) ;
#10116=CARTESIAN_POINT ( 'NONE',  ( 6.007384923554907274, -43.86041666762257307, 26.16266358875650866 ) ) ;
#10117=CARTESIAN_POINT ( 'NONE',  ( 7.757384923554902834, -43.98541666762258018, 31.21447844416572792 ) ) ;
#10125=FACE_OUTER_BOUND ( 'NONE', #855, .T. ) ;
#10144=VECTOR ( 'NONE', #35301, 1000.000000000000114 ) ;
#10151=CARTESIAN_POINT ( 'NONE',  ( 5.912663395429907709, -52.05729166714461797, 26.32672608803957459 ) ) ;
#10154=CARTESIAN_POINT ( 'NONE',  ( 4.707280140967346149, -43.82938952684293099, 25.71220187189605610 ) ) ;
#10162=CARTESIAN_POINT ( 'NONE',  ( 5.992653910530063577, -48.35846868484923533, 26.12101183036794083 ) ) ;
#10169=CARTESIAN_POINT ( 'NONE',  ( 2.911006399112987530, -50.60081140274053979, 32.42448198648213520 ) ) ;
#10170=CARTESIAN_POINT ( 'NONE',  ( 0.7573849235549120484, -51.65208333428923737, 31.21447844416572792 ) ) ;
#10174=VECTOR ( 'NONE', #16956, 1000.000000000000000 ) ;
#10192=CARTESIAN_POINT ( 'NONE',  ( 6.506261649816483583, -45.37284209939341650, 26.46882246860878496 ) ) ;
#10209=CARTESIAN_POINT ( 'NONE',  ( 7.567941867304905479, -43.51145833381128369, 27.28240155936039457 ) ) ;
#10241=CARTESIAN_POINT ( 'NONE',  ( 4.257384923554909051, -44.12499999999999289, 25.69375250200204519 ) ) ;
#10245=CARTESIAN_POINT ( 'NONE',  ( 0.7579440735085177794, -47.20543382706027558, 28.71274451778470649 ) ) ;
#10248=CARTESIAN_POINT ( 'NONE',  ( 4.257384923554908163, -46.87499999999999289, 33.23520438632941421 ) ) ;
#10257=CARTESIAN_POINT ( 'NONE',  ( 2.602106451679912169, -49.47395833381128227, 26.32672608803957459 ) ) ;
#10260=ORIENTED_EDGE ( 'NONE', *, *, #26535, .T. ) ;
#10262=FACE_OUTER_BOUND ( 'NONE', #31970, .T. ) ;
#10265=CARTESIAN_POINT ( 'NONE',  ( 0.7573849235549120484, -50.45833333333332149, 31.21447844416572792 ) ) ;
#10266=CARTESIAN_POINT ( 'NONE',  ( 0.9468279798049132889, -49.39062500047794657, 29.19375250200204164 ) ) ;
#10268=CARTESIAN_POINT ( 'NONE',  ( 7.646920258271509674, -46.46908733638845490, 30.24284080179819156 ) ) ;
#10274=CARTESIAN_POINT ( 'NONE',  ( 7.757384923554905498, -49.94375000095590167, 29.19375250200204164 ) ) ;
#10282=EDGE_CURVE ( 'NONE', #2889, #31605, #8025, .T. ) ;
#10301=AXIS2_PLACEMENT_3D ( 'NONE', #8875, #14843, #24424 ) ;
#10303=CARTESIAN_POINT ( 'NONE',  ( 7.567941867304902814, -46.18229166714461087, 31.10510344464368870 ) ) ;
#10307=CARTESIAN_POINT ( 'NONE',  ( 7.567941867304902814, -49.59479166714463361, 31.10510344464368870 ) ) ;
#10309=DIRECTION ( 'NONE',  ( 0.000000000000000000, 0.000000000000000000, 1.000000000000000000 ) ) ;
#10314=CARTESIAN_POINT ( 'NONE',  ( 0.7573849235549120484, -46.98895833323773985, 31.21447844416572792 ) ) ;
#10321=CARTESIAN_POINT ( 'NONE',  ( 0.7573849235549138248, -45.23541666762257307, 27.17302655983835180 ) ) ;
#10322=CARTESIAN_POINT ( 'NONE',  ( 7.757384923554902834, -44.98541666762258018, 31.21447844416572792 ) ) ;
#10343=CARTESIAN_POINT ( 'NONE',  ( 4.257384923554907274, -48.37499999999998579, 32.69375250200203453 ) ) ;
#10349=AXIS2_PLACEMENT_3D ( 'NONE', #6343, #12939, #38882 ) ;
#10363=CARTESIAN_POINT ( 'NONE',  ( 2.602106451679911281, -42.88645833381128369, 26.32672608803957459 ) ) ;
#10366=CARTESIAN_POINT ( 'NONE',  ( 4.257384923554909051, -52.75000000000000000, 25.69375250200204519 ) ) ;
#10369=CARTESIAN_POINT ( 'NONE',  ( 7.492928105787981075, -51.91325006685026722, 27.80519113137021137 ) ) ;
#10372=CARTESIAN_POINT ( 'NONE',  ( 6.054268267883907484, -42.40445412197200170, 26.18718149845503973 ) ) ;
#10374=VERTEX_POINT ( 'NONE', #14072 ) ;
#10376=CARTESIAN_POINT ( 'NONE',  ( 4.229855717591596509, -44.31809470075489799, 25.69384504159660310 ) ) ;
#10381=CARTESIAN_POINT ( 'NONE',  ( 1.375280990468229936, -50.74205418371479226, 27.20790870366911918 ) ) ;
#10383=CARTESIAN_POINT ( 'NONE',  ( 4.257384923554909051, -42.62499999999998579, 25.15230061767466552 ) ) ;
#10408=EDGE_LOOP ( 'NONE', ( #40756, #9581, #13499 ) ) ;
#10413=CARTESIAN_POINT ( 'NONE',  ( 3.407513500635413806, -45.58628816725937583, 32.62314792665948460 ) ) ;
#10421=DIRECTION ( 'NONE',  ( -0.000000000000000000, -1.000000000000000000, -0.000000000000000000 ) ) ;
#10429=CARTESIAN_POINT ( 'NONE',  ( 5.912663395429905044, -46.13645833381128369, 32.06077891596451224 ) ) ;
#10434=CARTESIAN_POINT ( 'NONE',  ( 5.541032900951168294, -46.03789658137771568, 32.45764149820281830 ) ) ;
#10460=CARTESIAN_POINT ( 'NONE',  ( 0.9468279798049134000, -51.34479166714461940, 27.28240155936039457 ) ) ;
#10463=CARTESIAN_POINT ( 'NONE',  ( 4.257384923554909051, -47.12499999999999289, 25.15230061767466552 ) ) ;
#10464=EDGE_LOOP ( 'NONE', ( #20507, #17011, #30988, #8636 ) ) ;
#10465=CARTESIAN_POINT ( 'NONE',  ( 4.257404373735115044, -49.56795750272889478, 32.69375250189725080 ) ) ;
#10471=CARTESIAN_POINT ( 'NONE',  ( 4.257384923554908163, -49.26562500047793947, 33.01645438728532866 ) ) ;
#10477=CARTESIAN_POINT ( 'NONE',  ( 2.507384923554911715, -48.08333333333332860, 26.16266358875650866 ) ) ;
#10478=CARTESIAN_POINT ( 'NONE',  ( 5.912663395429904156, -51.22395833381127517, 32.06077891596451224 ) ) ;
#10482=DIRECTION ( 'NONE',  ( -0.000000000000000000, -1.000000000000000000, -0.000000000000000000 ) ) ;
#10485=CARTESIAN_POINT ( 'NONE',  ( 7.757384923554902834, -50.98541666762257307, 31.21447844416572792 ) ) ;
#10517=CARTESIAN_POINT ( 'NONE',  ( 5.912663395429907709, -46.55729166714461087, 26.32672608803957459 ) ) ;
#10521=CARTESIAN_POINT ( 'NONE',  ( 7.567941867304905479, -48.51145833381128369, 27.28240155936039457 ) ) ;
#10524=VERTEX_POINT ( 'NONE', #28695 ) ;
#10526=EDGE_LOOP ( 'NONE', ( #24676, #28498, #36147, #23513 ) ) ;
#10527=CARTESIAN_POINT ( 'NONE',  ( 4.257384923554908163, -45.40562499990439704, 33.23520438632941421 ) ) ;
#10533=AXIS2_PLACEMENT_3D ( 'NONE', #4680, #11069, #2107 ) ;
#10534=CARTESIAN_POINT ( 'NONE',  ( 5.195207097063839541, -50.64732909936925154, 25.69375250200204874 ) ) ;
#10544=PLANE ( 'NONE',  #20054 ) ;
#10552=CARTESIAN_POINT ( 'NONE',  ( 5.430995388116433453, -51.54081244522072325, 32.53393362252825227 ) ) ;
#10557=ADVANCED_FACE ( 'NONE', ( #21689 ), #38700, .T. ) ;
#10578=CARTESIAN_POINT ( 'NONE',  ( 4.257384923554908163, -44.17812500047794799, 33.01645438728532866 ) ) ;
#10587=CARTESIAN_POINT ( 'NONE',  ( 4.257386979189129228, -48.56866505152967761, 32.69375250200084793 ) ) ;
#10591=CARTESIAN_POINT ( 'NONE',  ( 1.062894555283318221, -44.22799304788494368, 27.68292585479225565 ) ) ;
#10597=ORIENTED_EDGE ( 'NONE', *, *, #14756, .F. ) ;
#10600=CARTESIAN_POINT ( 'NONE',  ( 0.7573849235549138248, -42.54166666666665719, 27.17302655983835180 ) ) ;
#10601=ORIENTED_EDGE ( 'NONE', *, *, #5633, .F. ) ;
#10604=AXIS2_PLACEMENT_3D ( 'NONE', #28935, #35538, #6400 ) ;
#10620=DIRECTION ( 'NONE',  ( -0.000000000000000000, -1.000000000000000000, -0.000000000000000000 ) ) ;
#10621=EDGE_CURVE ( 'NONE', #24350, #40959, #40453, .T. ) ;
#10638=EDGE_CURVE ( 'NONE', #31605, #36320, #34353, .T. ) ;
#10642=ORIENTED_EDGE ( 'NONE', *, *, #21921, .F. ) ;
#10645=CARTESIAN_POINT ( 'NONE',  ( 4.257384923554908163, -46.17812500047794799, 33.01645438728532866 ) ) ;
#10651=VERTEX_POINT ( 'NONE', #32318 ) ;
#10674=CARTESIAN_POINT ( 'NONE',  ( 5.912663395429907709, -47.46979166714461229, 26.32672608803957459 ) ) ;
#10677=CARTESIAN_POINT ( 'NONE',  ( 0.7573849235549138248, -48.04166666666665719, 27.17302655983835180 ) ) ;
#10683=CARTESIAN_POINT ( 'NONE',  ( 5.912663395429907709, -49.05729166714461087, 26.32672608803957459 ) ) ;
#10690=CARTESIAN_POINT ( 'NONE',  ( 2.507384923554911715, -47.58333333333332149, 26.16266358875650866 ) ) ;
#10691=CARTESIAN_POINT ( 'NONE',  ( 2.602106451679909505, -49.80729166714461087, 32.06077891596451224 ) ) ;
#10700=CARTESIAN_POINT ( 'NONE',  ( 2.507384923554911715, -49.77708333428924448, 26.16266358875650866 ) ) ;
#10711=CARTESIAN_POINT ( 'NONE',  ( 1.240396410933131799, -44.73794479704661597, 27.35160872423474743 ) ) ;
#10718=EDGE_CURVE ( 'NONE', #34704, #35642, #25923, .T. ) ;
#10723=CARTESIAN_POINT ( 'NONE',  ( 7.567941867304902814, -45.18229166714461797, 31.10510344464368870 ) ) ;
#10727=CARTESIAN_POINT ( 'NONE',  ( 0.9468279798049134000, -47.34479166714463361, 27.28240155936039102 ) ) ;
#10734=CARTESIAN_POINT ( 'NONE',  ( 7.757384923554902834, -44.32229166657106845, 31.21447844416572792 ) ) ;
#10740=CARTESIAN_POINT ( 'NONE',  ( 7.757384923554902834, -42.98541666762257307, 31.21447844416572792 ) ) ;
#10750=CARTESIAN_POINT ( 'NONE',  ( -0.7016216170541935693, 7.250000000000000000, 32.48782483564529855 ) ) ;
#10755=CARTESIAN_POINT ( 'NONE',  ( 4.257351432995529983, -51.31874920356175096, 25.69375250216227613 ) ) ;
#10762=CARTESIAN_POINT ( 'NONE',  ( 4.257384923554909051, -52.75000000000000000, 25.69375250200204519 ) ) ;
#10764=EDGE_CURVE ( 'NONE', #6171, #8437, #32943, .T. ) ;
#10768=CARTESIAN_POINT ( 'NONE',  ( 5.635806484272968042, -51.03589381121867774, 32.41239413688044380 ) ) ;
#10778=CARTESIAN_POINT ( 'NONE',  ( 5.912663395429907709, -42.96979166714461940, 26.32672608803957459 ) ) ;
#10779=CARTESIAN_POINT ( 'NONE',  ( 0.7573849235549120484, -48.45833333333332860, 31.21447844416572792 ) ) ;
#10787=CARTESIAN_POINT ( 'NONE',  ( 4.889417799458270153, -48.55370147308967432, 32.63622021838954623 ) ) ;
#10791=CARTESIAN_POINT ( 'NONE',  ( 0.8100753645903089328, -44.20685852425354057, 28.58842960206429851 ) ) ;
#10792=CARTESIAN_POINT ( 'NONE',  ( 2.349588616910264882, -50.27492711584692842, 26.22630329765502566 ) ) ;
#10796=EDGE_CURVE ( 'NONE', #3545, #4835, #12571, .T. ) ;
#10800=CARTESIAN_POINT ( 'NONE',  ( 4.257384923554909051, -48.31875000095590167, 25.15230061767466552 ) ) ;
#10801=CARTESIAN_POINT ( 'NONE',  ( 4.257384923554909051, -42.51562500047793947, 25.37105061671875106 ) ) ;
#10825=CARTESIAN_POINT ( 'NONE',  ( 0.8465296012773773082, -47.67291467615015677, 30.10294010355664440 ) ) ;
#10833=CARTESIAN_POINT ( 'NONE',  ( 7.666289376911301190, -49.96242198217387909, 30.10986976837243390 ) ) ;
#10842=EDGE_LOOP ( 'NONE', ( #25190, #18234, #30023, #36578 ) ) ;
#10849=CARTESIAN_POINT ( 'NONE',  ( 7.567941867304905479, -47.05312500047795510, 29.19375250200204164 ) ) ;
#10851=EDGE_CURVE ( 'NONE', #2991, #679, #39964, .T. ) ;
#10855=CARTESIAN_POINT ( 'NONE',  ( 7.644363515772192308, -45.91895924813888286, 28.20316174213841620 ) ) ;
#10858=ORIENTED_EDGE ( 'NONE', *, *, #3947, .F. ) ;
#10885=CARTESIAN_POINT ( 'NONE',  ( 2.602106451679909505, -48.71979166714461229, 32.06077891596451224 ) ) ;
#10889=CARTESIAN_POINT ( 'NONE',  ( 7.757384923554905498, -43.24999999999999289, 29.19375250200204164 ) ) ;
#10891=CARTESIAN_POINT ( 'NONE',  ( 4.714538381248575938, -49.55662968464661589, 32.69375242325607189 ) ) ;
#10897=CARTESIAN_POINT ( 'NONE',  ( 0.9468279798049124008, -45.34895833381127517, 31.10510344464368515 ) ) ;
#10902=CARTESIAN_POINT ( 'NONE',  ( 0.7573849235549129366, -47.99999999999999289, 29.19375250200204164 ) ) ;
#10903=CARTESIAN_POINT ( 'NONE',  ( 0.9468279798049124008, -51.84895833381126806, 31.10510344464368515 ) ) ;
#10907=CARTESIAN_POINT ( 'NONE',  ( 3.909920614216715773, -43.31123083963191789, 25.69375724186110688 ) ) ;
#10913=CARTESIAN_POINT ( 'NONE',  ( 2.507384923554911715, -50.27708333428924448, 26.16266358875650866 ) ) ;
#10926=CARTESIAN_POINT ( 'NONE',  ( 0.8451507265551257975, -44.67417659358298465, 30.09738925367734907 ) ) ;
#10940=CARTESIAN_POINT ( 'NONE',  ( 3.044482980331683741, -42.29615616597445893, 32.27411873898371653 ) ) ;
#10948=CARTESIAN_POINT ( 'NONE',  ( 2.507384923554911715, -45.11395833323773275, 26.16266358875650866 ) ) ;
#10951=ORIENTED_EDGE ( 'NONE', *, *, #33223, .F. ) ;
#10956=CARTESIAN_POINT ( 'NONE',  ( 6.007384923554907274, -44.86041666762257307, 26.16266358875650866 ) ) ;
#10993=CARTESIAN_POINT ( 'NONE',  ( 4.257384923554908163, -43.17812500047794799, 33.01645438728532866 ) ) ;
#10995=CARTESIAN_POINT ( 'NONE',  ( 7.757384923554902834, -47.79166666666665719, 31.21447844416572792 ) ) ;
#11001=CARTESIAN_POINT ( 'NONE',  ( 7.744253389845995095, -48.42914478625770869, 28.65094315150213333 ) ) ;
#11002=ORIENTED_EDGE ( 'NONE', *, *, #14574, .T. ) ;
#11013=CARTESIAN_POINT ( 'NONE',  ( 4.257384923554908163, -49.56875000095590877, 33.23520438632941421 ) ) ;
#11016=EDGE_CURVE ( 'NONE', #8428, #5445, #34599, .T. ) ;
#11021=LINE ( 'NONE', #7838, #30908 ) ;
#11025=VECTOR ( 'NONE', #37761, 1000.000000000000000 ) ;
#11041=CARTESIAN_POINT ( 'NONE',  ( 3.354812166081319713, -47.79862934996641144, 25.80446652396019047 ) ) ;
#11049=CARTESIAN_POINT ( 'NONE',  ( 6.020051278423261820, -49.85943857976597826, 26.13550010245676702 ) ) ;
#11055=FACE_OUTER_BOUND ( 'NONE', #1631, .T. ) ;
#11066=CARTESIAN_POINT ( 'NONE',  ( 4.257384923554909051, -46.42812500047794799, 25.37105061671875461 ) ) ;
#11069=DIRECTION ( 'NONE',  ( -0.000000000000000000, -1.000000000000000000, -0.000000000000000000 ) ) ;
#11080=B_SPLINE_CURVE_WITH_KNOTS ( 'NONE', 3,
 ( #31546, #41763, #18791, #41552, #38559, #32387, #28355, #9426, #16037, #28977, #12190, #12823, #38772, #9641, #22604, #38142, #16236, #41134, #9000, #31751, #21978, #34949, #5818, #2621, #36421, #39824 ),
 .UNSPECIFIED., .F., .F.,
 ( 4, 2, 2, 2, 2, 2, 2, 2, 2, 1, 1, 2, 2, 4 ),
 ( 0.06348112978428653574, 0.06660712612648914122, 0.06973312246869176056, 0.07285911881089436604, 0.07598511515309697151, 0.07911111149529959086, 0.08223710783750219633, 0.08536310417970477404, 0.08546079156539859722, 0.08555847895109242041, 0.08575385372248006677, 0.08614460326525538725, 0.08692610235080602821, 0.08848910052190732400 ),
 .UNSPECIFIED. ) ;
#11094=CARTESIAN_POINT ( 'NONE',  ( 4.257384923554907274, -51.37499999999998579, 32.69375250200203453 ) ) ;
#11097=CARTESIAN_POINT ( 'NONE',  ( 7.567941867304905479, -48.05312500047795510, 29.19375250200204164 ) ) ;
#11101=CARTESIAN_POINT ( 'NONE',  ( 2.507384923554911715, -44.08333333333332149, 26.16266358875650866 ) ) ;
#11103=CARTESIAN_POINT ( 'NONE',  ( 6.016519595293767786, -49.52531905671531831, 32.25388876357207124 ) ) ;
#11108=CARTESIAN_POINT ( 'NONE',  ( 7.567941867304904591, -46.14062500047794657, 29.19375250200204164 ) ) ;
#11111=ORIENTED_EDGE ( 'NONE', *, *, #33735, .F. ) ;
#11114=CARTESIAN_POINT ( 'NONE',  ( 4.257384923554908163, -46.37499999999999289, 33.23520438632941421 ) ) ;
#11115=CARTESIAN_POINT ( 'NONE',  ( 0.9468279798049124008, -49.84895833381128227, 31.10510344464368515 ) ) ;
#11119=CARTESIAN_POINT ( 'NONE',  ( 0.8654412255672281340, -43.17023666226045719, 30.24844632732800775 ) ) ;
#11120=ADVANCED_FACE ( 'NONE', ( #34624 ), #24649, .T. ) ;
#11128=CARTESIAN_POINT ( 'NONE',  ( 4.257384923554908163, -46.56875000095590877, 33.23520438632941421 ) ) ;
#11131=CARTESIAN_POINT ( 'NONE',  ( 0.000000000000000000, 0.000000000000000000, 0.000000000000000000 ) ) ;
#11138=DIRECTION ( 'NONE',  ( 0.000000000000000000, 0.000000000000000000, 1.000000000000000000 ) ) ;
#11144=CARTESIAN_POINT ( 'NONE',  ( 2.111730211861753137, -49.62031731109337329, 31.99667691707370309 ) ) ;
#11153=EDGE_CURVE ( 'NONE', #679, #27540, #37432, .T. ) ;
#11164=CARTESIAN_POINT ( 'NONE',  ( 7.757384923554902834, -46.82229166657106134, 31.21447844416572792 ) ) ;
#11171=CARTESIAN_POINT ( 'NONE',  ( 0.9468279798049134000, -50.34479166714461229, 27.28240155936039457 ) ) ;
#11185=CARTESIAN_POINT ( 'NONE',  ( 7.492892321803050315, -51.47425234583334941, 30.58240586759756496 ) ) ;
#11195=CARTESIAN_POINT ( 'NONE',  ( 3.319562750045980337, -49.60267090063073425, 25.69375250200204519 ) ) ;
#11205=CARTESIAN_POINT ( 'NONE',  ( 2.602106451679912169, -49.47395833381128227, 26.32672608803957459 ) ) ;
#11208=FACE_OUTER_BOUND ( 'NONE', #25382, .T. ) ;
#11213=CYLINDRICAL_SURFACE ( 'NONE', #40046, 3.499999999999996003 ) ;
#11224=CARTESIAN_POINT ( 'NONE',  ( 7.757384923554904610, -50.40208333428924448, 27.17302655983835180 ) ) ;
#11225=CARTESIAN_POINT ( 'NONE',  ( 0.9468279798049143992, -43.93229166714461797, 27.28240155936039457 ) ) ;
#11234=AXIS2_PLACEMENT_3D ( 'NONE', #9949, #41860, #15913 ) ;
#11242=CARTESIAN_POINT ( 'NONE',  ( 7.761447874416249171, -42.93630340548262581, 28.88591739759701582 ) ) ;
#11248=CARTESIAN_POINT ( 'NONE',  ( 0.7573849235549129366, -48.99999999999998579, 29.19375250200204164 ) ) ;
#11251=CARTESIAN_POINT ( 'NONE',  ( 6.505275120585657156, -42.40485061181025372, 31.94300813626039215 ) ) ;
#11266=CARTESIAN_POINT ( 'NONE',  ( 0.9468279798049134000, -45.34479166714461940, 27.28240155936039457 ) ) ;
#11269=CARTESIAN_POINT ( 'NONE',  ( 5.195207097063847534, -44.64732909936925154, 25.69375250200204874 ) ) ;
#11294=CARTESIAN_POINT ( 'NONE',  ( 0.9468279798049134000, -47.84479166714461229, 27.28240155936039457 ) ) ;
#11299=CARTESIAN_POINT ( 'NONE',  ( 0.7573849235549138248, -44.54166666666666430, 27.17302655983835180 ) ) ;
#11301=CARTESIAN_POINT ( 'NONE',  ( 7.576695235213606772, -49.41856815435606620, 28.08224698970517252 ) ) ;
#11306=CARTESIAN_POINT ( 'NONE',  ( 2.602106451679909505, -46.80729166714461087, 32.06077891596451224 ) ) ;
#11312=CARTESIAN_POINT ( 'NONE',  ( 6.007384923554904610, -47.83333333333332149, 32.22484141524757462 ) ) ;
#11313=CARTESIAN_POINT ( 'NONE',  ( 4.257384923554908163, -46.76562500047794657, 33.01645438728532866 ) ) ;
#11315=ADVANCED_FACE ( 'NONE', ( #9940 ), #22897, .T. ) ;
#11325=CARTESIAN_POINT ( 'NONE',  ( 7.757384923554902834, -46.48541666762257307, 31.21447844416572792 ) ) ;
#11340=CARTESIAN_POINT ( 'NONE',  ( 4.257384951507396487, -49.81875000160972178, 25.69375250200204519 ) ) ;
#11352=CARTESIAN_POINT ( 'NONE',  ( 5.238410986165888517, -43.84208121361496069, 25.82311630669410718 ) ) ;
#11353=DIRECTION ( 'NONE',  ( 0.000000000000000000, 0.000000000000000000, -1.000000000000000000 ) ) ;
#11358=B_SPLINE_CURVE_WITH_KNOTS ( 'NONE', 3,
 ( #24761, #37310, #37726, #21555, #17533, #37930, #12401, #41760, #35578, #2412, #28143, #9212, #8997, #21762, #41336, #15399, #5602, #28351, #34736, #28973, #41549, #18788, #25389, #38348, #18577, #22601, #31960 ),
 .UNSPECIFIED., .F., .F.,
 ( 4, 2, 2, 2, 2, 2, 2, 2, 2, 2, 1, 1, 1, 2, 4 ),
 ( 0.1396783341777186604, 0.1428499141952691565, 0.1460214942128196525, 0.1491930742303701485, 0.1523646542479206445, 0.1555362342654711405, 0.1587078142830216088, 0.1618793943005721048, 0.1634651843093473667, 0.1642580793137349837, 0.1646545268159287922, 0.1648527505670256965, 0.1649518624425741486, 0.1650014183803483747, 0.1650509743181226008 ),
 .UNSPECIFIED. ) ;
#11363=CARTESIAN_POINT ( 'NONE',  ( 0.7573849235549129366, -45.03062499990440415, 29.19375250200204164 ) ) ;
#11368=CARTESIAN_POINT ( 'NONE',  ( 5.195207097063847534, -43.64732909936924443, 25.69375250200204874 ) ) ;
#11369=CARTESIAN_POINT ( 'NONE',  ( 2.602106451679909505, -51.21979166714461940, 32.06077891596451224 ) ) ;
#11402=CARTESIAN_POINT ( 'NONE',  ( 0.9468279798049124008, -50.84895833381128938, 31.10510344464368515 ) ) ;
#11409=ORIENTED_EDGE ( 'NONE', *, *, #2785, .T. ) ;
#11411=ORIENTED_EDGE ( 'NONE', *, *, #12313, .F. ) ;
#11417=FACE_OUTER_BOUND ( 'NONE', #2049, .T. ) ;
#11418=CARTESIAN_POINT ( 'NONE',  ( 7.757384923554904610, -48.90208333428923737, 27.17302655983835180 ) ) ;
#11419=CARTESIAN_POINT ( 'NONE',  ( 4.257384923554909051, -44.01562500047795368, 25.37105061671875106 ) ) ;
#11420=VERTEX_POINT ( 'NONE', #18867 ) ;
#11423=CYLINDRICAL_SURFACE ( 'NONE', #16962, 3.499999999999996003 ) ;
#11438=CARTESIAN_POINT ( 'NONE',  ( 7.683931753092501538, -42.95935972888209164, 29.90865668880212169 ) ) ;
#11444=CARTESIAN_POINT ( 'NONE',  ( 0.8510281415512321868, -47.71500041752434385, 28.26785315649001618 ) ) ;
#11451=CARTESIAN_POINT ( 'NONE',  ( 7.745914039160743947, -48.93346122399942999, 28.65837069235388057 ) ) ;
#11464=CARTESIAN_POINT ( 'NONE',  ( 2.602106451679911281, -43.38645833381128369, 26.32672608803957459 ) ) ;
#11477=CARTESIAN_POINT ( 'NONE',  ( 3.933778011664021079, -46.07614698810055387, 32.69375250526813659 ) ) ;
#11494=CARTESIAN_POINT ( 'NONE',  ( 0.9468279798049125118, -47.80312500047795510, 29.19375250200204164 ) ) ;
#11498=CARTESIAN_POINT ( 'NONE',  ( 0.7573849235549120484, -45.45833333333332149, 31.21447844416572792 ) ) ;
#11499=AXIS2_PLACEMENT_3D ( 'NONE', #1479, #24039, #1066 ) ;
#11504=CARTESIAN_POINT ( 'NONE',  ( 5.912663395429904156, -47.72395833381128227, 32.06077891596451224 ) ) ;
#11505=CARTESIAN_POINT ( 'NONE',  ( 2.602106451679909505, -47.71979166714461229, 32.06077891596451224 ) ) ;
#11513=CARTESIAN_POINT ( 'NONE',  ( 2.507384923554911715, -44.58333333333332149, 26.16266358875650866 ) ) ;
#11514=CARTESIAN_POINT ( 'NONE',  ( 4.257384923554909051, -49.01562500047793947, 25.37105061671875106 ) ) ;
#11516=CARTESIAN_POINT ( 'NONE',  ( 4.257384923554909051, -52.75000000000000000, 29.19375250200204164 ) ) ;
#11520=DIRECTION ( 'NONE',  ( 0.000000000000000000, 0.000000000000000000, -1.000000000000000000 ) ) ;
#11525=CARTESIAN_POINT ( 'NONE',  ( 4.257384923554909051, -47.31875000095590877, 25.15230061767466552 ) ) ;
#11537=VECTOR ( 'NONE', #15344, 1000.000000000000000 ) ;
#11554=CARTESIAN_POINT ( 'NONE',  ( 0.9468279798049132889, -43.39062500047794657, 29.19375250200204164 ) ) ;
#11558=AXIS2_PLACEMENT_3D ( 'NONE', #17990, #27768, #27146 ) ;
#11561=CARTESIAN_POINT ( 'NONE',  ( 0.7573849235549120484, -43.48895833323772564, 31.21447844416572792 ) ) ;
#11565=CARTESIAN_POINT ( 'NONE',  ( 1.438471787934466173, -43.64096382934744156, 31.32285674386804075 ) ) ;
#11568=CARTESIAN_POINT ( 'NONE',  ( 5.912663395429907709, -51.96979166714461940, 26.32672608803957459 ) ) ;
#11591=B_SPLINE_CURVE_WITH_KNOTS ( 'NONE', 3,
 ( #12935, #25497, #28456, #38244, #9106, #22086, #18891, #25914, #2726, #13140, #6338, #15711, #41656, #32288, #38878, #35264, #19312, #38460, #38668, #9323, #26125, #9538, #9754, #22290, #6125, #2940, #32491, #22497, #19105, #32071, #23768, #20360, #33326, #373 ),
 .UNSPECIFIED., .F., .F.,
 ( 4, 2, 2, 2, 2, 2, 2, 2, 2, 2, 2, 2, 1, 1, 2, 2, 2, 4 ),
 ( 0.3922791998606462993, 0.3956160726096606406, 0.3972845089841677835, 0.3977016180777945831, 0.3981187271714213827, 0.3989529453586749819, 0.4022898181076893787, 0.4056266908567037754, 0.4089635636057181722, 0.4097977817929717714, 0.4098499204296751075, 0.4099020590663784436, 0.4100063363397851712, 0.4102148908865985710, 0.4106319999802253706, 0.4123004363547326245, 0.4156373091037470768, 0.4189741818527615846 ),
 .UNSPECIFIED. ) ;
#11602=CARTESIAN_POINT ( 'NONE',  ( 2.602106451679912169, -49.97395833381128227, 26.32672608803957459 ) ) ;
#11605=CARTESIAN_POINT ( 'NONE',  ( 0.7562688098096949085, -45.18342907838320599, 29.64402257021835396 ) ) ;
#11620=CARTESIAN_POINT ( 'NONE',  ( 7.757384923554902834, -50.29166666666665009, 31.21447844416572792 ) ) ;
#11621=CARTESIAN_POINT ( 'NONE',  ( 7.743469725335405229, -42.43576016065963330, 28.81036140113019073 ) ) ;
#11622=CARTESIAN_POINT ( 'NONE',  ( 6.007384923554907274, -49.86041666762257307, 26.16266358875650866 ) ) ;
#11644=CARTESIAN_POINT ( 'NONE',  ( 4.376243998815336766, -42.82157995766748826, 25.69375370531728464 ) ) ;
#11649=CARTESIAN_POINT ( 'NONE',  ( 2.507384923554909495, -48.91666666666665719, 32.22484141524756751 ) ) ;
#11671=CARTESIAN_POINT ( 'NONE',  ( 3.044481415175603889, -42.20865620537255580, 32.27411812269911451 ) ) ;
#11699=CARTESIAN_POINT ( 'NONE',  ( 4.257384923554908163, -46.67812500047794799, 33.01645438728532866 ) ) ;
#11705=CARTESIAN_POINT ( 'NONE',  ( 7.757384923554904610, -43.70833333333331439, 27.17302655983835180 ) ) ;
#11710=CARTESIAN_POINT ( 'NONE',  ( 2.602106451679912169, -45.97395833381128227, 26.32672608803957459 ) ) ;
#11712=CARTESIAN_POINT ( 'NONE',  ( 0.9468279798049125118, -47.80312500047795510, 29.19375250200204164 ) ) ;
#11718=CARTESIAN_POINT ( 'NONE',  ( 2.975074105796479795, -42.37818741561596170, 32.45038864544541468 ) ) ;
#11719=CARTESIAN_POINT ( 'NONE',  ( 7.757384923554902834, -44.79166666666666430, 31.21447844416572792 ) ) ;
#11720=CARTESIAN_POINT ( 'NONE',  ( 2.602106451679912169, -48.47395833381128227, 26.32672608803957459 ) ) ;
#11723=FACE_OUTER_BOUND ( 'NONE', #10526, .T. ) ;
#11734=CARTESIAN_POINT ( 'NONE',  ( 2.507384923554909495, -48.11041666762257307, 32.22484141524756751 ) ) ;
#11763=CARTESIAN_POINT ( 'NONE',  ( 2.602106451679909505, -42.30729166714461087, 32.06077891596451224 ) ) ;
#11773=CARTESIAN_POINT ( 'NONE',  ( 6.007384923554904610, -43.36395833323773275, 32.22484141524757462 ) ) ;
#11777=CARTESIAN_POINT ( 'NONE',  ( 3.766822570234043877, -43.80706347594109218, 25.72612063422284123 ) ) ;
#11779=CARTESIAN_POINT ( 'NONE',  ( 7.567941867304905479, -50.55312500047794799, 29.19375250200204164 ) ) ;
#11781=CARTESIAN_POINT ( 'NONE',  ( 7.757384923554905498, -51.74999999999999289, 29.19375250200204164 ) ) ;
#11788=CARTESIAN_POINT ( 'NONE',  ( 4.257384923554909051, -45.12499999999999289, 25.69375250200204519 ) ) ;
#11795=B_SPLINE_CURVE_WITH_KNOTS ( 'NONE', 3,
 ( #4200, #20796, #8021, #1842, #10792, #36529, #17601, #17394, #30144, #7603, #23776, #13991, #36741, #1022, #37368, #7824, #26966, #27173, #33767, #4621, #39930, #30775, #17802, #4826, #20580, #33556, #18009 ),
 .UNSPECIFIED., .F., .F.,
 ( 4, 2, 2, 2, 2, 2, 2, 2, 2, 1, 2, 2, 2, 4 ),
 ( 0.1650509743181226008, 0.1682276071821757479, 0.1714042400462288951, 0.1745808729102820422, 0.1777575057743351894, 0.1793458222063617491, 0.1801399804223750289, 0.1805370595303816827, 0.1806363293073833531, 0.1807355990843850235, 0.1809341386383883643, 0.1841107715024417613, 0.1872874043664951582, 0.1904640372305485552 ),
 .UNSPECIFIED. ) ;
#11798=CARTESIAN_POINT ( 'NONE',  ( 6.007384923554904610, -43.33333333333332149, 32.22484141524757462 ) ) ;
#11813=CARTESIAN_POINT ( 'NONE',  ( 4.257384923554908163, -49.76562500047794657, 33.01645438728532866 ) ) ;
#11821=EDGE_CURVE ( 'NONE', #30878, #5244, #5033, .T. ) ;
#11823=EDGE_LOOP ( 'NONE', ( #41618, #38342, #4510, #20590 ) ) ;
#11826=CARTESIAN_POINT ( 'NONE',  ( 4.257384923554909051, -50.65562499990439704, 25.15230061767466552 ) ) ;
#11829=ORIENTED_EDGE ( 'NONE', *, *, #30823, .F. ) ;
#11832=CARTESIAN_POINT ( 'NONE',  ( 7.757384923554902834, -47.98541666762257307, 31.21447844416572792 ) ) ;
#11856=B_SPLINE_CURVE_WITH_KNOTS ( 'NONE', 3,
 ( #25610, #19624, #6245, #12631, #6659, #26026, #3262, #29188, #66, #13045, #15620, #32193, #38364, #32597, #38572, #10066, #16453, #41986, #38990, #3057, #28578, #16049, #18802, #9437, #31762, #35595, #22404, #2632, #29403, #3463, #16246, #28989, #12835, #23029, #41565, #26240, #12418, #9873, #22828 ),
 .UNSPECIFIED., .F., .F.,
 ( 4, 2, 1, 1, 1, 2, 2, 2, 2, 2, 2, 1, 1, 2, 2, 1, 1, 2, 2, 2, 2, 2, 4 ),
 ( 0.3174042320821390262, 0.3174546020310364813, 0.3175049719799338810, 0.3176057118777287913, 0.3178071916733185565, 0.3182101512644980867, 0.3190160704468572028, 0.3206279088115753240, 0.3238515855410116218, 0.3270752622704479751, 0.3302989389998842729, 0.3307018985910638031, 0.3307522685399612583, 0.3307774535144099581, 0.3308026384888587135, 0.3309033783866536793, 0.3311048581822437220, 0.3319107773646037263, 0.3335226157293237348, 0.3367462924587639184, 0.3399699691882039909, 0.3415818075529239994, 0.3431936459176440635 ),
 .UNSPECIFIED. ) ;
#11868=CARTESIAN_POINT ( 'NONE',  ( 6.483467197300033291, -48.87481964195697515, 26.46685149917597357 ) ) ;
#11882=VECTOR ( 'NONE', #42056, 1000.000000000000000 ) ;
#11883=CARTESIAN_POINT ( 'NONE',  ( 0.9468279798049125118, -43.80312500047794799, 29.19375250200204164 ) ) ;
#11908=CARTESIAN_POINT ( 'NONE',  ( 2.507384923554911715, -51.58333333333332149, 26.16266358875650866 ) ) ;
#11916=CARTESIAN_POINT ( 'NONE',  ( 7.331839645663885463, -42.40485061181026794, 27.52313662862605881 ) ) ;
#11922=ORIENTED_EDGE ( 'NONE', *, *, #17780, .F. ) ;
#11923=CARTESIAN_POINT ( 'NONE',  ( 0.9468279798049124008, -43.84895833381127517, 31.10510344464368515 ) ) ;
#11924=CARTESIAN_POINT ( 'NONE',  ( 2.602106451679909505, -44.21979166714461940, 32.06077891596451224 ) ) ;
#11932=CARTESIAN_POINT ( 'NONE',  ( 4.257384923554908163, -45.87499999999999289, 33.23520438632941421 ) ) ;
#11933=CARTESIAN_POINT ( 'NONE',  ( 7.567941867304902814, -47.68229166714461087, 31.10510344464368870 ) ) ;
#11945=CARTESIAN_POINT ( 'NONE',  ( 6.007384923554904610, -46.52708333428923737, 32.22484141524757462 ) ) ;
#11962=CARTESIAN_POINT ( 'NONE',  ( 4.257404373735115044, -49.56795750272889478, 32.69375250189725080 ) ) ;
#11963=VERTEX_POINT ( 'NONE', #17983 ) ;
#11965=CARTESIAN_POINT ( 'NONE',  ( 6.393086817769037644, -51.01721833537701656, 31.97434701948635549 ) ) ;
#11971=CARTESIAN_POINT ( 'NONE',  ( 2.507384923554909495, -49.41666666666665719, 32.22484141524756751 ) ) ;
#11976=CARTESIAN_POINT ( 'NONE',  ( 7.567941867304902814, -50.68229166714461087, 31.10510344464368870 ) ) ;
#11984=CARTESIAN_POINT ( 'NONE',  ( 2.507384923554909495, -42.94729166657106845, 32.22484141524756751 ) ) ;
#11988=CARTESIAN_POINT ( 'NONE',  ( 1.326671063194738043, -43.73851479758272376, 27.21936894061798284 ) ) ;
#11990=CARTESIAN_POINT ( 'NONE',  ( 7.567941867304904591, -51.09479166714461940, 31.10510344464368870 ) ) ;
#11992=CARTESIAN_POINT ( 'NONE',  ( 4.257384923554908163, -51.87499999999998579, 33.23520438632941421 ) ) ;
#12023=CARTESIAN_POINT ( 'NONE',  ( 4.257384923554909051, -49.51562500047794657, 25.37105061671875461 ) ) ;
#12025=DIRECTION ( 'NONE',  ( -0.000000000000000000, -1.000000000000000000, -0.000000000000000000 ) ) ;
#12035=CARTESIAN_POINT ( 'NONE',  ( 7.757384923554904610, -51.73895833323773275, 27.17302655983835180 ) ) ;
#12040=CARTESIAN_POINT ( 'NONE',  ( 7.758722357152640470, -42.44489461552163334, 29.24966550351183869 ) ) ;
#12041=CARTESIAN_POINT ( 'NONE',  ( 7.757384923554904610, -46.40208333428924448, 27.17302655983835180 ) ) ;
#12067=CARTESIAN_POINT ( 'NONE',  ( 4.257385064927798446, -48.31875000421112532, 25.69375250200204519 ) ) ;
#12070=CARTESIAN_POINT ( 'NONE',  ( 0.8358061347120296913, -46.21286774301550793, 28.32069558277208188 ) ) ;
#12086=ORIENTED_EDGE ( 'NONE', *, *, #13650, .F. ) ;
#12088=CARTESIAN_POINT ( 'NONE',  ( 5.912663395429907709, -44.46979166714461940, 26.32672608803957459 ) ) ;
#12114=CARTESIAN_POINT ( 'NONE',  ( 0.9268385055368815184, -45.71877540033431586, 28.11391485874483465 ) ) ;
#12124=CARTESIAN_POINT ( 'NONE',  ( 7.567941867304904591, -44.14062500047794657, 29.19375250200204164 ) ) ;
#12126=CARTESIAN_POINT ( 'NONE',  ( 0.9468279798049117346, -45.26145833381127659, 31.10510344464368515 ) ) ;
#12138=CARTESIAN_POINT ( 'NONE',  ( 0.7573849235549120484, -45.95833333333332149, 31.21447844416572792 ) ) ;
#12139=CARTESIAN_POINT ( 'NONE',  ( 4.257384923554908163, -49.26562500047794657, 33.01645438728532866 ) ) ;
#12152=CARTESIAN_POINT ( 'NONE',  ( 6.007384923554907274, -45.36041666762256597, 26.16266358875650866 ) ) ;
#12178=CARTESIAN_POINT ( 'NONE',  ( 2.507384923554909495, -49.91666666666665719, 32.22484141524756751 ) ) ;
#12182=CARTESIAN_POINT ( 'NONE',  ( 4.257384923554909051, -52.75000000000000000, 29.19375250200204164 ) ) ;
#12183=CARTESIAN_POINT ( 'NONE',  ( 7.757384923554902834, -51.29166666666666430, 31.21447844416572792 ) ) ;
#12185=CARTESIAN_POINT ( 'NONE',  ( 0.9468279798049143992, -51.93229166714461797, 27.28240155936039812 ) ) ;
#12187=B_SPLINE_CURVE_WITH_KNOTS ( 'NONE', 3,
 ( #3806, #17214, #37402, #11041, #30177, #20611, #33590, #37607, #17431, #11444, #17633, #1260, #10825, #17835, #23810, #21441, #1052, #18045, #24434, #8462 ),
 .UNSPECIFIED., .F., .F.,
 ( 4, 2, 2, 2, 2, 2, 2, 2, 2, 4 ),
 ( 0.4189741818527615846, 0.4205624339748803564, 0.4221506860969991837, 0.4253271903412367272, 0.4285036945854743262, 0.4316801988297118697, 0.4348567030739494133, 0.4380332073181870123, 0.4412097115624246113, 0.4443862158066621548 ),
 .UNSPECIFIED. ) ;
#12190=CARTESIAN_POINT ( 'NONE',  ( 0.8213820846465974546, -51.17630690253993464, 29.99879261468614899 ) ) ;
#12194=CARTESIAN_POINT ( 'NONE',  ( 2.507384923554911715, -43.61395833323773275, 26.16266358875650866 ) ) ;
#12201=CARTESIAN_POINT ( 'NONE',  ( 0.9468279798049115126, -47.76145833381128369, 31.10510344464368515 ) ) ;
#12206=CARTESIAN_POINT ( 'NONE',  ( 4.257384923554909051, -51.31875000095590167, 25.15230061767466552 ) ) ;
#12231=EDGE_LOOP ( 'NONE', ( #10858, #12686, #35935, #17960 ) ) ;
#12233=CARTESIAN_POINT ( 'NONE',  ( 4.257384923554908163, -49.26562500047793947, 33.01645438728532866 ) ) ;
#12247=CARTESIAN_POINT ( 'NONE',  ( 0.7573849235549129366, -51.03062499990439704, 29.19375250200204164 ) ) ;
#12252=CARTESIAN_POINT ( 'NONE',  ( 5.810016854262419983, -42.53095680055645289, 32.35423014914645279 ) ) ;
#12253=CARTESIAN_POINT ( 'NONE',  ( 7.757384923554905498, -46.44375000095590877, 29.19375250200204164 ) ) ;
#12260=CARTESIAN_POINT ( 'NONE',  ( 0.8193378782107911817, -46.70800951873847850, 28.53794743159250302 ) ) ;
#12270=CARTESIAN_POINT ( 'NONE',  ( 4.257384923554909051, -52.75000000000000000, 29.19375250200204164 ) ) ;
#12283=CARTESIAN_POINT ( 'NONE',  ( 1.158229044483519266, -48.15544404702693271, 30.82060337224095292 ) ) ;
#12288=CARTESIAN_POINT ( 'NONE',  ( 6.007384923554904610, -48.83333333333332860, 32.22484141524757462 ) ) ;
#12301=EDGE_LOOP ( 'NONE', ( #27501, #6812, #10642, #2780 ) ) ;
#12306=CARTESIAN_POINT ( 'NONE',  ( 7.567941867304905479, -44.05312500047794799, 29.19375250200204164 ) ) ;
#12307=CARTESIAN_POINT ( 'NONE',  ( 2.507384923554911715, -42.27708333428924448, 26.16266358875650866 ) ) ;
#12313=EDGE_CURVE ( 'NONE', #29977, #37688, #28701, .T. ) ;
#12320=DIRECTION ( 'NONE',  ( 0.000000000000000000, 1.000000000000000000, 0.000000000000000000 ) ) ;
#12331=CARTESIAN_POINT ( 'NONE',  ( 2.060434156586022691, -45.62078020115231425, 31.97561782964963228 ) ) ;
#12338=CARTESIAN_POINT ( 'NONE',  ( 7.757384923554905498, -42.74999999999999289, 29.19375250200204164 ) ) ;
#12343=CARTESIAN_POINT ( 'NONE',  ( 4.257384923554909051, -45.01562500047794657, 25.37105061671875461 ) ) ;
#12345=CARTESIAN_POINT ( 'NONE',  ( 5.912663395429905044, -46.13645833381128369, 32.06077891596451224 ) ) ;
#12355=CARTESIAN_POINT ( 'NONE',  ( 6.012523041434447713, -46.86149600627152978, 26.14871827263695536 ) ) ;
#12356=CARTESIAN_POINT ( 'NONE',  ( 4.257384923554908163, -43.87499999999999289, 33.23520438632941421 ) ) ;
#12357=CARTESIAN_POINT ( 'NONE',  ( 7.567941867304902814, -45.59895833381128227, 27.28240155936039457 ) ) ;
#12369=ORIENTED_EDGE ( 'NONE', *, *, #41131, .F. ) ;
#12395=CARTESIAN_POINT ( 'NONE',  ( 2.507384923554911715, -50.58333333333332860, 26.16266358875650866 ) ) ;
#12401=CARTESIAN_POINT ( 'NONE',  ( 7.322747159548787188, -50.48564069427749956, 30.94447599966104079 ) ) ;
#12409=CARTESIAN_POINT ( 'NONE',  ( 6.007384923554907274, -51.66666666666665719, 26.16266358875650866 ) ) ;
#12410=CARTESIAN_POINT ( 'NONE',  ( 7.567941867304902814, -52.09895833381127517, 27.28240155936039457 ) ) ;
#12416=CARTESIAN_POINT ( 'NONE',  ( 0.9468279798049125118, -48.80312500047794799, 29.19375250200204164 ) ) ;
#12418=CARTESIAN_POINT ( 'NONE',  ( 3.623388812743331577, -48.58340048156321700, 32.64873868986351368 ) ) ;
#12434=DIRECTION ( 'NONE',  ( -0.000000000000000000, -1.000000000000000000, -0.000000000000000000 ) ) ;
#12452=CARTESIAN_POINT ( 'NONE',  ( 7.567941867304904591, -47.64062500047794657, 29.19375250200204164 ) ) ;
#12465=CARTESIAN_POINT ( 'NONE',  ( 7.757384923554905498, -51.78062499990439704, 29.19375250200204164 ) ) ;
#12471=CARTESIAN_POINT ( 'NONE',  ( 0.7573849235549129366, -45.69375000095590877, 29.19375250200204164 ) ) ;
#12473=ORIENTED_EDGE ( 'NONE', *, *, #32176, .F. ) ;
#12489=CARTESIAN_POINT ( 'NONE',  ( 3.044482980331683741, -42.29615616597446603, 32.27411873898371653 ) ) ;
#12498=CARTESIAN_POINT ( 'NONE',  ( 0.8481136188864848435, -48.21286594238318912, 28.38059477221373328 ) ) ;
#12502=CARTESIAN_POINT ( 'NONE',  ( 4.058227884785847728, -46.31401360703307546, 25.69860947341293311 ) ) ;
#12503=AXIS2_PLACEMENT_3D ( 'NONE', #29382, #251, #13235 ) ;
#12505=CARTESIAN_POINT ( 'NONE',  ( 4.257384923554908163, -44.67812500047794799, 33.01645438728532866 ) ) ;
#12514=CARTESIAN_POINT ( 'NONE',  ( 2.037080718773353283, -42.40270429005899189, 31.91299903367601942 ) ) ;
#12524=DIRECTION ( 'NONE',  ( 0.000000000000000000, 0.000000000000000000, -1.000000000000000000 ) ) ;
#12554=CARTESIAN_POINT ( 'NONE',  ( 4.257406269681411004, -45.56789735307413736, 32.69375250187820825 ) ) ;
#12557=CARTESIAN_POINT ( 'NONE',  ( 0.9468279798049124008, -43.34895833381126806, 31.10510344464368515 ) ) ;
#12558=CARTESIAN_POINT ( 'NONE',  ( 7.567941867304905479, -44.05312500047794799, 29.19375250200204164 ) ) ;
#12561=( BOUNDED_CURVE ( )  B_SPLINE_CURVE ( 2, ( #22224, #32005, #28602, #31584, #24802, #5428, #35192, #34775, #27973 ),
 .UNSPECIFIED., .F., .T. ) 
 B_SPLINE_CURVE_WITH_KNOTS ( ( 3, 2, 2, 2, 3 ),
 ( 0.2375000000000000167, 0.2416666666666666685, 0.2500000000000000000, 0.2583333333333333592, 0.2625000000000000111 ),
 .UNSPECIFIED. ) 
 CURVE ( )  GEOMETRIC_REPRESENTATION_ITEM ( )  RATIONAL_B_SPLINE_CURVE ( ( 0.9330127018922194093, 0.9330127018922196314, 1.000000000000000000, 0.8660254037844387076, 1.000000000000000000, 0.8660254037844387076, 1.000000000000000000, 0.9330127018922194093, 0.9330127018922194093 ) ) 
 REPRESENTATION_ITEM ( '' )  );
#12562=ORIENTED_EDGE ( 'NONE', *, *, #38886, .T. ) ;
#12568=CARTESIAN_POINT ( 'NONE',  ( 7.757384923554905498, -43.24999999999999289, 29.19375250200204164 ) ) ;
#12569=CARTESIAN_POINT ( 'NONE',  ( 7.567941867304902814, -44.68229166714461797, 31.10510344464368870 ) ) ;
#12571=B_SPLINE_CURVE_WITH_KNOTS ( 'NONE', 3,
 ( #23386, #36349, #7221, #33153, #27213, #27622, #11251, #17841, #4861, #34008 ),
 .UNSPECIFIED., .F., .F.,
 ( 4, 2, 2, 2, 4 ),
 ( 0.1719518825728937605, 0.2539639119296701053, 0.3359759412864464778, 0.4179879706432232389, 0.5000000000000000000 ),
 .UNSPECIFIED. ) ;
#12573=CARTESIAN_POINT ( 'NONE',  ( 4.257384923554909051, -52.75000000000000000, 29.19375250200204164 ) ) ;
#12580=EDGE_LOOP ( 'NONE', ( #17120, #38823, #36469, #16639 ) ) ;
#12587=EDGE_CURVE ( 'NONE', #32591, #3034, #16673, .T. ) ;
#12596=CARTESIAN_POINT ( 'NONE',  ( 0.7573849235549129366, -44.49999999999999289, 29.19375250200204164 ) ) ;
#12600=ORIENTED_EDGE ( 'NONE', *, *, #12587, .F. ) ;
#12607=DIRECTION ( 'NONE',  ( -0.000000000000000000, -1.000000000000000000, -0.000000000000000000 ) ) ;
#12608=CARTESIAN_POINT ( 'NONE',  ( 0.7573849235549120484, -48.95833333333332149, 31.21447844416572792 ) ) ;
#12614=CARTESIAN_POINT ( 'NONE',  ( 4.257384923554908163, -51.26562500047794657, 33.01645438728532866 ) ) ;
#12623=CARTESIAN_POINT ( 'NONE',  ( 2.507384923554909495, -51.41666666666665719, 32.22484141524756751 ) ) ;
#12625=ORIENTED_EDGE ( 'NONE', *, *, #22277, .T. ) ;
#12628=CARTESIAN_POINT ( 'NONE',  ( 0.9468279798049115126, -49.76145833381129080, 31.10510344464368515 ) ) ;
#12631=CARTESIAN_POINT ( 'NONE',  ( 4.228994528493347005, -48.81807418969262358, 25.69386040928654324 ) ) ;
#12666=CARTESIAN_POINT ( 'NONE',  ( 0.9468279798049143992, -47.43229166714461087, 27.28240155936039812 ) ) ;
#12667=FACE_OUTER_BOUND ( 'NONE', #18989, .T. ) ;
#12671=CARTESIAN_POINT ( 'NONE',  ( 5.912663395429905044, -49.13645833381128369, 32.06077891596451224 ) ) ;
#12677=CARTESIAN_POINT ( 'NONE',  ( 4.257384923554908163, -48.40562499990439704, 33.23520438632941421 ) ) ;
#12684=CARTESIAN_POINT ( 'NONE',  ( 6.007384923554904610, -48.02708333428923737, 32.22484141524757462 ) ) ;
#12686=ORIENTED_EDGE ( 'NONE', *, *, #18040, .F. ) ;
#12689=CARTESIAN_POINT ( 'NONE',  ( -1.074868669588189274, 7.250000000000000000, 26.54616302712299358 ) ) ;
#12693=EDGE_CURVE ( 'NONE', #36320, #22305, #34838, .T. ) ;
#12698=CARTESIAN_POINT ( 'NONE',  ( 7.757384923554905498, -51.74999999999999289, 29.19375250200204164 ) ) ;
#12704=CARTESIAN_POINT ( 'NONE',  ( 4.257384923554933032, -46.12499999999999289, 25.69375250200204519 ) ) ;
#12708=CARTESIAN_POINT ( 'NONE',  ( 4.257384923554907274, -42.87499999999998579, 32.69375250200203453 ) ) ;
#12713=FACE_OUTER_BOUND ( 'NONE', #33914, .T. ) ;
#12714=CARTESIAN_POINT ( 'NONE',  ( 4.257406270103921919, -48.06789733593042513, 32.69375250187820114 ) ) ;
#12715=ORIENTED_EDGE ( 'NONE', *, *, #37049, .T. ) ;
#12717=CARTESIAN_POINT ( 'NONE',  ( 0.7694743875661853583, -46.18761273873432316, 29.48441395074767257 ) ) ;
#12718=CARTESIAN_POINT ( 'NONE',  ( 2.602106451679909505, -46.71979166714461229, 32.06077891596451224 ) ) ;
#12733=CARTESIAN_POINT ( 'NONE',  ( 3.796794373725280725, -50.58032633976880987, 32.67094870127696993 ) ) ;
#12739=EDGE_CURVE ( 'NONE', #28152, #2420, #16226, .T. ) ;
#12748=FACE_OUTER_BOUND ( 'NONE', #17335, .T. ) ;
#12752=CARTESIAN_POINT ( 'NONE',  ( 4.257384923554909051, -52.75000000000000000, 32.69375250200203453 ) ) ;
#12758=CARTESIAN_POINT ( 'NONE',  ( 4.257384923554909051, -51.12499999999999289, 25.69375250200204519 ) ) ;
#12769=CARTESIAN_POINT ( 'NONE',  ( 4.257384923554908163, -43.76562500047794657, 33.01645438728532866 ) ) ;
#12770=CARTESIAN_POINT ( 'NONE',  ( 7.567941867304905479, -44.51145833381127659, 27.28240155936039457 ) ) ;
#12776=CARTESIAN_POINT ( 'NONE',  ( 4.257440696971988459, -46.81875132889357616, 25.69375250244642572 ) ) ;
#12777=CARTESIAN_POINT ( 'NONE',  ( 7.567941867304902814, -46.59895833381128227, 27.28240155936039457 ) ) ;
#12794=CARTESIAN_POINT ( 'NONE',  ( -1.074868669588189274, 7.250000000000000000, 26.54616302712299358 ) ) ;
#12797=CARTESIAN_POINT ( 'NONE',  ( 4.257397009801616505, -51.06825406007883572, 32.69375250196129912 ) ) ;
#12800=DIRECTION ( 'NONE',  ( -0.000000000000000000, -1.000000000000000000, -0.000000000000000000 ) ) ;
#12803=ORIENTED_EDGE ( 'NONE', *, *, #3311, .F. ) ;
#12805=CARTESIAN_POINT ( 'NONE',  ( 4.257384923554909051, -52.24999999999999289, 25.69375250200204519 ) ) ;
#12813=CARTESIAN_POINT ( 'NONE',  ( 2.507384923554909495, -50.41666666666665719, 32.22484141524756751 ) ) ;
#12820=CARTESIAN_POINT ( 'NONE',  ( 5.912663395429907709, -51.05729166714461797, 26.32672608803957459 ) ) ;
#12823=CARTESIAN_POINT ( 'NONE',  ( 1.138530292825146173, -51.15660238777031310, 30.84510070404542859 ) ) ;
#12826=CARTESIAN_POINT ( 'NONE',  ( 0.7573849235549129366, -49.49999999999998579, 29.19375250200204164 ) ) ;
#12832=CARTESIAN_POINT ( 'NONE',  ( 7.567941867304905479, -49.51145833381128369, 27.28240155936039812 ) ) ;
#12835=CARTESIAN_POINT ( 'NONE',  ( 1.705055767400385003, -48.63422662021439180, 31.62936703901664970 ) ) ;
#12844=DIRECTION ( 'NONE',  ( -0.000000000000000000, -1.000000000000000000, -0.000000000000000000 ) ) ;
#12871=CARTESIAN_POINT ( 'NONE',  ( 5.912663395429904156, -48.22395833381128227, 32.06077891596451224 ) ) ;
#12877=CARTESIAN_POINT ( 'NONE',  ( 7.567941867304905479, -50.05312500047794799, 29.19375250200204164 ) ) ;
#12884=CARTESIAN_POINT ( 'NONE',  ( 2.507384923554909495, -48.44729166657106845, 32.22484141524756751 ) ) ;
#12886=ORIENTED_EDGE ( 'NONE', *, *, #6609, .T. ) ;
#12892=CARTESIAN_POINT ( 'NONE',  ( 7.757384923554905498, -44.94375000095590877, 29.19375250200204164 ) ) ;
#12926=CARTESIAN_POINT ( 'NONE',  ( 5.912663395429905044, -44.63645833381128369, 32.06077891596451224 ) ) ;
#12927=DIRECTION ( 'NONE',  ( -0.000000000000000000, -1.000000000000000000, -0.000000000000000000 ) ) ;
#12929=DIRECTION ( 'NONE',  ( -0.000000000000000000, -1.000000000000000000, -0.000000000000000000 ) ) ;
#12935=CARTESIAN_POINT ( 'NONE',  ( 4.257406270103921919, -48.06789733593042513, 32.69375250187820114 ) ) ;
#12939=DIRECTION ( 'NONE',  ( -0.000000000000000000, -1.000000000000000000, -0.000000000000000000 ) ) ;
#12966=CARTESIAN_POINT ( 'NONE',  ( 7.757384923554905498, -47.24999999999999289, 29.19375250200204164 ) ) ;
#12970=CARTESIAN_POINT ( 'NONE',  ( 0.7518070419428554141, -45.68476137892419331, 29.64309270192013201 ) ) ;
#12981=CARTESIAN_POINT ( 'NONE',  ( 0.9468279798049132889, -42.39062500047794657, 29.19375250200204164 ) ) ;
#12983=CARTESIAN_POINT ( 'NONE',  ( 7.567941867304905479, -43.55312500047794799, 29.19375250200204164 ) ) ;
#12990=CARTESIAN_POINT ( 'NONE',  ( 5.956660446403191145, -47.03036713794099910, 32.27155587563216699 ) ) ;
#12991=CARTESIAN_POINT ( 'NONE',  ( 2.602106451679909505, -44.30729166714461797, 32.06077891596451224 ) ) ;
#12996=ORIENTED_EDGE ( 'NONE', *, *, #17639, .F. ) ;
#13022=CARTESIAN_POINT ( 'NONE',  ( 5.912663395429907709, -49.96979166714461940, 26.32672608803957459 ) ) ;
#13023=CARTESIAN_POINT ( 'NONE',  ( 6.020048928954755851, -47.52629898159199939, 32.25200614385167341 ) ) ;
#13026=CARTESIAN_POINT ( 'NONE',  ( 0.7573849235549138248, -47.04166666666665719, 27.17302655983835180 ) ) ;
#13029=CARTESIAN_POINT ( 'NONE',  ( 4.257384923554907274, -51.87499999999998579, 32.69375250200203453 ) ) ;
#13031=CARTESIAN_POINT ( 'NONE',  ( 4.270766444697928321, -43.31903961768931310, 25.69377162372534329 ) ) ;
#13032=CARTESIAN_POINT ( 'NONE',  ( 4.257384923554909051, -50.51562500047794657, 25.37105061671875461 ) ) ;
#13039=CARTESIAN_POINT ( 'NONE',  ( 4.257384923554909051, -50.62499999999999289, 25.15230061767466552 ) ) ;
#13041=CARTESIAN_POINT ( 'NONE',  ( 7.253348390716708671, -46.40088564259081494, 27.32717798353343852 ) ) ;
#13045=CARTESIAN_POINT ( 'NONE',  ( 3.689161417140196964, -48.80523360438757408, 25.73829104494603826 ) ) ;
#13075=CIRCLE ( 'NONE', #169, 2.999999999999988898 ) ;
#13076=CARTESIAN_POINT ( 'NONE',  ( 4.257384923554908163, -48.76562500047794657, 33.01645438728532866 ) ) ;
#13082=CARTESIAN_POINT ( 'NONE',  ( 7.567941867304905479, -51.01145833381127659, 27.28240155936039457 ) ) ;
#13084=ORIENTED_EDGE ( 'NONE', *, *, #13914, .F. ) ;
#13088=CARTESIAN_POINT ( 'NONE',  ( 7.757384923554905498, -47.78062499990440415, 29.19375250200204164 ) ) ;
#13091=ORIENTED_EDGE ( 'NONE', *, *, #18361, .F. ) ;
#13094=EDGE_CURVE ( 'NONE', #15596, #6132, #36952, .T. ) ;
#13095=CARTESIAN_POINT ( 'NONE',  ( 4.257384923554909051, -45.31875000095590877, 25.15230061767466552 ) ) ;
#13098=CARTESIAN_POINT ( 'NONE',  ( 4.257384923554909051, -43.12499999999999289, 25.69375250200204519 ) ) ;
#13132=CARTESIAN_POINT ( 'NONE',  ( 0.9468279798049125118, -45.80312500047794799, 29.19375250200204164 ) ) ;
#13133=CARTESIAN_POINT ( 'NONE',  ( 3.178668223428115169, -42.40485061181026083, 32.53055490697369123 ) ) ;
#13140=CARTESIAN_POINT ( 'NONE',  ( 6.156273575612109639, -48.02346836918155759, 32.13509106695910589 ) ) ;
#13147=VERTEX_POINT ( 'NONE', #41759 ) ;
#13149=CARTESIAN_POINT ( 'NONE',  ( 0.8378188203511188759, -50.71272993760310044, 28.34140771283698257 ) ) ;
#13162=CARTESIAN_POINT ( 'NONE',  ( 4.257384923554913492, -49.87499999999998579, 32.69375250200203453 ) ) ;
#13173=CARTESIAN_POINT ( 'NONE',  ( 2.507384923554911715, -48.08333333333332860, 26.16266358875650866 ) ) ;
#13184=CARTESIAN_POINT ( 'NONE',  ( 3.649361958902952452, -42.58322672429243028, 32.69375250197767002 ) ) ;
#13193=CARTESIAN_POINT ( 'NONE',  ( 6.895102605304866294, -46.88758535751060208, 26.86050753801149327 ) ) ;
#13194=CARTESIAN_POINT ( 'NONE',  ( 0.9468279798049143992, -44.93229166714461797, 27.28240155936039457 ) ) ;
#13203=CARTESIAN_POINT ( 'NONE',  ( 4.414208897414158450, -46.06491326680936993, 32.69375250041924375 ) ) ;
#13210=B_SPLINE_CURVE_WITH_KNOTS ( 'NONE', 3,
 ( #22925, #28457, #41445, #35058, #31858, #12514, #20574, #19941, #20156, #20362, #29504, #7598, #23348, #374, #32907, #3771, #7818, #29718, #23770, #29929, #13553, #26752, #39715, #26961, #17179, #30139, #13351, #14192, #1016, #33550, #16963, #36310, #33327, #36096, #10372, #26541, #7184, #801, #13774, #26333 ),
 .UNSPECIFIED., .F., .F.,
 ( 4, 2, 2, 2, 2, 2, 2, 2, 2, 2, 2, 2, 2, 2, 2, 2, 2, 2, 2, 4 ),
 ( 0.000000000000000000, 0.03125000000000052736, 0.06250000000000105471, 0.1250000000000011935, 0.1875000000000013323, 0.2500000000000014433, 0.3125000000000016098, 0.3750000000000017764, 0.4375000000000019429, 0.5000000000000021094, 0.5625000000000022204, 0.5937500000000021094, 0.6250000000000019984, 0.6875000000000015543, 0.7500000000000012212, 0.8125000000000007772, 0.8437500000000006661, 0.8750000000000005551, 0.9375000000000002220, 1.000000000000000000 ),
 .UNSPECIFIED. ) ;
#13224=CARTESIAN_POINT ( 'NONE',  ( 7.757384923554905498, -44.24999999999999289, 29.19375250200204164 ) ) ;
#13227=CARTESIAN_POINT ( 'NONE',  ( 7.567941867304904591, -51.59479166714461940, 31.10510344464368870 ) ) ;
#13228=CARTESIAN_POINT ( 'NONE',  ( 2.357285429694124357, -47.11542485743417075, 32.16301691237210747 ) ) ;
#13231=CARTESIAN_POINT ( 'NONE',  ( 0.7573849235549129366, -46.49999999999999289, 29.19375250200204164 ) ) ;
#13234=VECTOR ( 'NONE', #30686, 1000.000000000000000 ) ;
#13235=DIRECTION ( 'NONE',  ( 0.000000000000000000, 0.000000000000000000, -1.000000000000000000 ) ) ;
#13238=DIRECTION ( 'NONE',  ( -0.000000000000000000, -1.000000000000000000, -0.000000000000000000 ) ) ;
#13240=CARTESIAN_POINT ( 'NONE',  ( 6.293009658903947923, -43.36662982934755917, 26.31426885617655742 ) ) ;
#13241=CARTESIAN_POINT ( 'NONE',  ( 0.9468279798049143992, -48.43229166714461087, 27.28240155936039812 ) ) ;
#13247=CARTESIAN_POINT ( 'NONE',  ( 6.007384923554904610, -49.33333333333332860, 32.22484141524757462 ) ) ;
#13249=ORIENTED_EDGE ( 'NONE', *, *, #24946, .F. ) ;
#13250=CARTESIAN_POINT ( 'NONE',  ( 6.443905245930951153, -46.51663064337693498, 31.94568389759649207 ) ) ;
#13257=CARTESIAN_POINT ( 'NONE',  ( 0.7573849235549138248, -50.73541666762258018, 27.17302655983835180 ) ) ;
#13265=EDGE_CURVE ( 'NONE', #18276, #5047, #21382, .T. ) ;
#13270=CARTESIAN_POINT ( 'NONE',  ( 0.7624658562750986635, -44.18543211148538319, 29.54191697212240086 ) ) ;
#13275=CARTESIAN_POINT ( 'NONE',  ( 7.757384923554904610, -42.40208333428923737, 27.17302655983835180 ) ) ;
#13286=CARTESIAN_POINT ( 'NONE',  ( 4.257384923554909051, -44.01562500047795368, 25.37105061671875461 ) ) ;
#13291=CARTESIAN_POINT ( 'NONE',  ( 0.9468279798049125118, -50.30312500047794799, 29.19375250200204164 ) ) ;
#13298=CARTESIAN_POINT ( 'NONE',  ( 2.507384923554909495, -47.44729166657106134, 32.22484141524756751 ) ) ;
#13304=CARTESIAN_POINT ( 'NONE',  ( 0.7573849235549129366, -44.69375000095590877, 29.19375250200204164 ) ) ;
#13305=CARTESIAN_POINT ( 'NONE',  ( 6.007384923554904610, -43.52708333428924448, 32.22484141524757462 ) ) ;
#13318=DIRECTION ( 'NONE',  ( -0.8956692225370904703, 0.000000000000000000, -0.4447208605404111004 ) ) ;
#13319=CARTESIAN_POINT ( 'NONE',  ( 7.757384923554902834, -51.79166666666665719, 31.21447844416572792 ) ) ;
#13331=DIRECTION ( 'NONE',  ( 0.000000000000000000, 1.000000000000000000, 0.000000000000000000 ) ) ;
#13342=CARTESIAN_POINT ( 'NONE',  ( 2.602106451679909505, -42.21979166714461940, 32.06077891596451224 ) ) ;
#13351=CARTESIAN_POINT ( 'NONE',  ( 3.482381198524040933, -42.40338347774257244, 25.76881433544439304 ) ) ;
#13360=CARTESIAN_POINT ( 'NONE',  ( 4.257384923554909051, -43.62499999999998579, 25.15230061767466552 ) ) ;
#13382=CARTESIAN_POINT ( 'NONE',  ( 0.7573849235549120484, -47.95833333333332860, 31.21447844416572792 ) ) ;
#13386=CARTESIAN_POINT ( 'NONE',  ( 4.257384951507396487, -49.81875000160972178, 25.69375250200204519 ) ) ;
#13392=VERTEX_POINT ( 'NONE', #38389 ) ;
#13393=CARTESIAN_POINT ( 'NONE',  ( 2.142542521341825434, -42.62158178309231715, 32.03305195878531464 ) ) ;
#13395=ORIENTED_EDGE ( 'NONE', *, *, #25363, .F. ) ;
#13432=CARTESIAN_POINT ( 'NONE',  ( 2.507384923554911715, -48.08333333333332860, 26.16266358875650866 ) ) ;
#13439=CARTESIAN_POINT ( 'NONE',  ( 5.110701381559501044, -43.33757975153600484, 25.79255424918537543 ) ) ;
#13441=CARTESIAN_POINT ( 'NONE',  ( 5.912663395429907709, -48.55729166714461087, 26.32672608803957459 ) ) ;
#13447=CARTESIAN_POINT ( 'NONE',  ( 4.257384923554908163, -49.87499999999999289, 33.23520438632941421 ) ) ;
#13448=CARTESIAN_POINT ( 'NONE',  ( 4.257384923554908163, -51.76562500047794657, 33.01645438728532866 ) ) ;
#13451=CARTESIAN_POINT ( 'NONE',  ( 1.577481115661631739, -43.13756693596063485, 31.44500239124655039 ) ) ;
#13453=CARTESIAN_POINT ( 'NONE',  ( 2.507384923554909495, -45.91666666666666430, 32.22484141524756751 ) ) ;
#13458=CARTESIAN_POINT ( 'NONE',  ( 7.757384923554902834, -50.48541666762257307, 31.21447844416572792 ) ) ;
#13469=CARTESIAN_POINT ( 'NONE',  ( 0.7716653789176983747, -44.20050440625544041, 28.86910519775949524 ) ) ;
#13474=CARTESIAN_POINT ( 'NONE',  ( 6.007384923554907274, -42.36041666762257307, 26.16266358875650866 ) ) ;
#13486=CARTESIAN_POINT ( 'NONE',  ( 7.567941867304904591, -46.14062500047794657, 29.19375250200204164 ) ) ;
#13490=CARTESIAN_POINT ( 'NONE',  ( 5.912663395429905044, -51.63645833381128369, 32.06077891596451224 ) ) ;
#13496=CARTESIAN_POINT ( 'NONE',  ( 0.7573849235549129366, -48.03062499990440415, 29.19375250200204164 ) ) ;
#13499=ORIENTED_EDGE ( 'NONE', *, *, #24931, .T. ) ;
#13504=CARTESIAN_POINT ( 'NONE',  ( 4.257384923554908163, -43.56875000095590877, 33.23520438632941421 ) ) ;
#13505=CARTESIAN_POINT ( 'NONE',  ( 7.757384923554905498, -43.44375000095590167, 29.19375250200204164 ) ) ;
#13511=CARTESIAN_POINT ( 'NONE',  ( 3.319562750045979005, -42.89732909936924443, 32.69375250200202743 ) ) ;
#13543=CARTESIAN_POINT ( 'NONE',  ( 7.567941867304905479, -43.55312500047794799, 29.19375250200204164 ) ) ;
#13546=CARTESIAN_POINT ( 'NONE',  ( 7.253246892709644733, -43.90088105058985946, 27.32701514452383407 ) ) ;
#13553=CARTESIAN_POINT ( 'NONE',  ( 2.018500134584749972, -42.40557055148732957, 26.48974273222354014 ) ) ;
#13555=ORIENTED_EDGE ( 'NONE', *, *, #32085, .T. ) ;
#13563=ORIENTED_EDGE ( 'NONE', *, *, #17780, .T. ) ;
#13564=CARTESIAN_POINT ( 'NONE',  ( 0.7333630555136090301, -50.69382059178740008, 29.15920040562719961 ) ) ;
#13565=CARTESIAN_POINT ( 'NONE',  ( 0.7573849235549129366, -42.99999999999999289, 29.19375250200204164 ) ) ;
#13566=ORIENTED_EDGE ( 'NONE', *, *, #16803, .T. ) ;
#13589=CARTESIAN_POINT ( 'NONE',  ( 7.387677489837495060, -45.40705635243941174, 27.62759184004299584 ) ) ;
#13600=ORIENTED_EDGE ( 'NONE', *, *, #25909, .F. ) ;
#13604=CARTESIAN_POINT ( 'NONE',  ( 2.602106451679911281, -42.38645833381128369, 26.32672608803957459 ) ) ;
#13607=ORIENTED_EDGE ( 'NONE', *, *, #26535, .F. ) ;
#13610=CARTESIAN_POINT ( 'NONE',  ( 5.912663395429905044, -48.63645833381128369, 32.06077891596451224 ) ) ;
#13642=CARTESIAN_POINT ( 'NONE',  ( 4.257384923554909051, -50.92812500047794799, 25.37105061671875461 ) ) ;
#13647=CARTESIAN_POINT ( 'NONE',  ( 7.757384923554904610, -47.70833333333332149, 27.17302655983835180 ) ) ;
#13650=EDGE_CURVE ( 'NONE', #2260, #28152, #6399, .T. ) ;
#13661=CARTESIAN_POINT ( 'NONE',  ( 4.257384923554908163, -48.37499999999999289, 33.23520438632941421 ) ) ;
#13662=CARTESIAN_POINT ( 'NONE',  ( 7.567941867304904591, -50.14062500047794657, 29.19375250200204164 ) ) ;
#13666=CARTESIAN_POINT ( 'NONE',  ( 4.257403850124284794, -43.06798715535520472, 32.69375250190384463 ) ) ;
#13674=CARTESIAN_POINT ( 'NONE',  ( 4.257384923554909051, -50.81875000095590877, 25.15230061767466552 ) ) ;
#13704=CARTESIAN_POINT ( 'NONE',  ( 2.602106451679909505, -44.30729166714461797, 32.06077891596451224 ) ) ;
#13709=CARTESIAN_POINT ( 'NONE',  ( 5.912663395429907709, -46.46979166714461229, 26.32672608803957459 ) ) ;
#13715=CARTESIAN_POINT ( 'NONE',  ( 0.7573849235549129366, -44.53062499990439704, 29.19375250200204164 ) ) ;
#13722=CARTESIAN_POINT ( 'NONE',  ( 2.507384923554909495, -43.61041666762257307, 32.22484141524756751 ) ) ;
#13736=DIRECTION ( 'NONE',  ( 0.000000000000000000, 0.000000000000000000, -1.000000000000000000 ) ) ;
#13741=CARTESIAN_POINT ( 'NONE',  ( 4.290558595339660108, -51.31953975302815252, 25.69388723502828142 ) ) ;
#13765=CARTESIAN_POINT ( 'NONE',  ( 2.602106451679911281, -43.88645833381129080, 26.32672608803957459 ) ) ;
#13768=DIRECTION ( 'NONE',  ( 0.8329741740894176516, 0.000000000000000000, -0.5533118698347727626 ) ) ;
#13774=CARTESIAN_POINT ( 'NONE',  ( 7.167553491837421298, -42.40437555931063685, 27.22841287014669831 ) ) ;
#13775=ORIENTED_EDGE ( 'NONE', *, *, #41131, .T. ) ;
#13783=CARTESIAN_POINT ( 'NONE',  ( 7.757384923554902834, -42.79166666666665719, 31.21447844416572792 ) ) ;
#13808=CARTESIAN_POINT ( 'NONE',  ( 4.257384923554909051, -52.75000000000000000, 25.69375250200204519 ) ) ;
#13809=VERTEX_POINT ( 'NONE', #30779 ) ;
#13828=ORIENTED_EDGE ( 'NONE', *, *, #10718, .T. ) ;
#13830=CARTESIAN_POINT ( 'NONE',  ( 0.9468279798049125118, -44.80312500047794799, 29.19375250200204164 ) ) ;
#13833=CARTESIAN_POINT ( 'NONE',  ( 4.879019534166787686, -46.05394916177709064, 32.63810770937520545 ) ) ;
#13859=CARTESIAN_POINT ( 'NONE',  ( 0.9468279798049134000, -51.84479166714461229, 27.28240155936039457 ) ) ;
#13863=CARTESIAN_POINT ( 'NONE',  ( 7.757384923554902834, -47.79166666666665719, 31.21447844416572792 ) ) ;
#13867=CARTESIAN_POINT ( 'NONE',  ( 3.599660943495602616, -49.08319440687185420, 32.64619692738686041 ) ) ;
#13868=AXIS2_PLACEMENT_3D ( 'NONE', #37462, #27673, #27877 ) ;
#13871=CARTESIAN_POINT ( 'NONE',  ( 0.9468279798049143992, -48.93229166714461087, 27.28240155936039812 ) ) ;
#13878=CARTESIAN_POINT ( 'NONE',  ( 4.257384923554908163, -47.37499999999999289, 33.23520438632941421 ) ) ;
#13879=CARTESIAN_POINT ( 'NONE',  ( 2.602106451679909505, -51.80729166714461797, 32.06077891596451224 ) ) ;
#13882=CARTESIAN_POINT ( 'NONE',  ( 1.695321029853095185, -43.25547382202357483, 26.76698082676062995 ) ) ;
#13888=CARTESIAN_POINT ( 'NONE',  ( 6.007384923554907274, -50.36041666762257307, 26.16266358875650866 ) ) ;
#13897=DIRECTION ( 'NONE',  ( -0.000000000000000000, -1.000000000000000000, -0.000000000000000000 ) ) ;
#13900=CARTESIAN_POINT ( 'NONE',  ( 3.925745736451821788, -44.81126342932117979, 25.70887367049265393 ) ) ;
#13914=EDGE_CURVE ( 'NONE', #27384, #27947, #19839, .T. ) ;
#13916=CARTESIAN_POINT ( 'NONE',  ( 2.602106451679909505, -46.30729166714461797, 32.06077891596451224 ) ) ;
#13920=CARTESIAN_POINT ( 'NONE',  ( 4.257384923554908163, -47.17812500047795510, 33.01645438728532866 ) ) ;
#13927=CARTESIAN_POINT ( 'NONE',  ( 6.007384923554904610, -44.36395833323773275, 32.22484141524757462 ) ) ;
#13931=ORIENTED_EDGE ( 'NONE', *, *, #2190, .T. ) ;
#13935=CARTESIAN_POINT ( 'NONE',  ( 6.007384923554904610, -43.02708333428924448, 32.22484141524757462 ) ) ;
#13943=CARTESIAN_POINT ( 'NONE',  ( 4.257384923554909051, -52.75000000000000000, 29.19375250200204164 ) ) ;
#13953=CARTESIAN_POINT ( 'NONE',  ( 4.865396705751455109, -51.55427353857958650, 32.69375250245094833 ) ) ;
#13965=CYLINDRICAL_SURFACE ( 'NONE', #37000, 3.499999999999996003 ) ;
#13976=CARTESIAN_POINT ( 'NONE',  ( 7.567941867304905479, -43.05312500047794799, 29.19375250200204164 ) ) ;
#13985=CARTESIAN_POINT ( 'NONE',  ( 5.054861093502212022, -48.54974463217318714, 32.60215417614575273 ) ) ;
#13990=CARTESIAN_POINT ( 'NONE',  ( 0.8809096544469218193, -44.21430663708844122, 28.26410196334070335 ) ) ;
#13991=CARTESIAN_POINT ( 'NONE',  ( 0.8293030845324208533, -50.17821961377931217, 29.91199059682945816 ) ) ;
#13999=CARTESIAN_POINT ( 'NONE',  ( 0.7573849235549120484, -49.15208333428923737, 31.21447844416572792 ) ) ;
#14000=CARTESIAN_POINT ( 'NONE',  ( 4.257384923554908163, -43.26562500047795368, 33.01645438728532866 ) ) ;
#14027=CARTESIAN_POINT ( 'NONE',  ( 0.7573849235549138248, -45.54166666666666430, 27.17302655983835180 ) ) ;
#14028=ORIENTED_EDGE ( 'NONE', *, *, #20395, .T. ) ;
#14033=CARTESIAN_POINT ( 'NONE',  ( 5.173503040601140412, -50.04608394400447935, 32.60265672674164961 ) ) ;
#14044=DIRECTION ( 'NONE',  ( -0.000000000000000000, -1.000000000000000000, -0.000000000000000000 ) ) ;
#14050=CARTESIAN_POINT ( 'NONE',  ( 0.9468279798049115126, -47.26145833381127659, 31.10510344464368515 ) ) ;
#14056=EDGE_LOOP ( 'NONE', ( #31548, #24564, #25871, #41300 ) ) ;
#14072=CARTESIAN_POINT ( 'NONE',  ( 4.257384923554909051, -45.62499999999999289, 25.69375250200204519 ) ) ;
#14079=CARTESIAN_POINT ( 'NONE',  ( 5.912663395429905044, -49.63645833381128369, 32.06077891596451224 ) ) ;
#14083=CARTESIAN_POINT ( 'NONE',  ( 4.257384923554908163, -43.37499999999999289, 33.23520438632941421 ) ) ;
#14089=CARTESIAN_POINT ( 'NONE',  ( 2.602106451679912169, -45.47395833381128227, 26.32672608803957459 ) ) ;
#14094=CARTESIAN_POINT ( 'NONE',  ( 7.757384923554905498, -47.74999999999999289, 29.19375250200204164 ) ) ;
#14095=CARTESIAN_POINT ( 'NONE',  ( 0.9468279798049143992, -51.43229166714461797, 27.28240155936039457 ) ) ;
#14105=CARTESIAN_POINT ( 'NONE',  ( 4.257384923554908163, -48.56875000095589456, 33.23520438632941421 ) ) ;
#14117=CARTESIAN_POINT ( 'NONE',  ( 6.955504822719134950, -42.00450905097582677, 34.01771537441437943 ) ) ;
#14129=CARTESIAN_POINT ( 'NONE',  ( 7.567941867304904591, -45.59895833381128227, 27.28240155936039812 ) ) ;
#14138=CARTESIAN_POINT ( 'NONE',  ( 4.257384923554908163, -46.90562499990439704, 33.23520438632941421 ) ) ;
#14144=CARTESIAN_POINT ( 'NONE',  ( 0.7573849235549138248, -42.73541666762258018, 27.17302655983835180 ) ) ;
#14161=CARTESIAN_POINT ( 'NONE',  ( 7.757384923554904610, -48.20833333333333570, 27.17302655983835180 ) ) ;
#14169=DIRECTION ( 'NONE',  ( -0.000000000000000000, -1.000000000000000000, -0.000000000000000000 ) ) ;
#14170=CARTESIAN_POINT ( 'NONE',  ( 5.723227194887511082, -51.03383662981508451, 32.37336304907700679 ) ) ;
#14181=CARTESIAN_POINT ( 'NONE',  ( 7.567941867304904591, -43.59479166714461229, 31.10510344464368870 ) ) ;
#14187=( BOUNDED_CURVE ( )  B_SPLINE_CURVE ( 2, ( #27359, #11195, #33530, #8001, #4804, #24379, #37348, #21175, #34151 ),
 .UNSPECIFIED., .F., .T. ) 
 B_SPLINE_CURVE_WITH_KNOTS ( ( 3, 2, 2, 2, 3 ),
 ( 0.2625000000000000111, 0.2666666666666666630, 0.2750000000000000222, 0.2833333333333333259, 0.2875000000000000333 ),
 .UNSPECIFIED. ) 
 CURVE ( )  GEOMETRIC_REPRESENTATION_ITEM ( )  RATIONAL_B_SPLINE_CURVE ( ( 0.9330127018922194093, 0.9330127018922194093, 1.000000000000000000, 0.8660254037844387076, 1.000000000000000000, 0.8660254037844387076, 1.000000000000000000, 0.9330127018922189652, 0.9330127018922194093 ) ) 
 REPRESENTATION_ITEM ( '' )  );
#14192=CARTESIAN_POINT ( 'NONE',  ( 4.045319806307197119, -42.40413158257847215, 25.68863330223127051 ) ) ;
#14196=CARTESIAN_POINT ( 'NONE',  ( 3.718381546859108155, -44.30597553098011332, 25.73264222577477867 ) ) ;
#14199=ORIENTED_EDGE ( 'NONE', *, *, #3947, .T. ) ;
#14203=CARTESIAN_POINT ( 'NONE',  ( 0.7573849235549138248, -50.23541666762257307, 27.17302655983835180 ) ) ;
#14204=CARTESIAN_POINT ( 'NONE',  ( 0.9468279798049143992, -43.43229166714461797, 27.28240155936039457 ) ) ;
#14208=DIRECTION ( 'NONE',  ( -0.000000000000000000, -1.000000000000000000, -0.000000000000000000 ) ) ;
#14224=CARTESIAN_POINT ( 'NONE',  ( 5.127826097248761705, -43.04746757639636456, 32.61647084861933621 ) ) ;
#14228=VECTOR ( 'NONE', #31260, 1000.000000000000000 ) ;
#14232=AXIS2_PLACEMENT_3D ( 'NONE', #39293, #32138, #2793 ) ;
#14237=CARTESIAN_POINT ( 'NONE',  ( 7.315637474420465303, -49.98323120263950869, 30.95641859431201937 ) ) ;
#14253=CARTESIAN_POINT ( 'NONE',  ( 5.912663395429905044, -47.13645833381128369, 32.06077891596451224 ) ) ;
#14261=EDGE_LOOP ( 'NONE', ( #28369, #13566, #41822, #38287 ) ) ;
#14286=CARTESIAN_POINT ( 'NONE',  ( 0.9468279798049134000, -48.84479166714461229, 27.28240155936039457 ) ) ;
#14290=CARTESIAN_POINT ( 'NONE',  ( 0.7573849235549129366, -45.49999999999999289, 29.19375250200204164 ) ) ;
#14291=ORIENTED_EDGE ( 'NONE', *, *, #16240, .F. ) ;
#14295=CARTESIAN_POINT ( 'NONE',  ( 1.366514976402122716, -49.24050471453161748, 27.17926297769722410 ) ) ;
#14298=CARTESIAN_POINT ( 'NONE',  ( 4.257384923554908163, -47.76562500047794657, 33.01645438728532866 ) ) ;
#14302=CARTESIAN_POINT ( 'NONE',  ( 7.757384923554905498, -47.24999999999999289, 29.19375250200204164 ) ) ;
#14303=CARTESIAN_POINT ( 'NONE',  ( 0.9468279798049132889, -50.89062500047794657, 29.19375250200204164 ) ) ;
#14307=CARTESIAN_POINT ( 'NONE',  ( 1.606918670950999495, -43.13650068732244591, 31.47967097773539535 ) ) ;
#14315=CARTESIAN_POINT ( 'NONE',  ( 7.757384923554902834, -46.98541666762256597, 31.21447844416572792 ) ) ;
#14324=CARTESIAN_POINT ( 'NONE',  ( 6.408295534151669415, -45.01587498771841922, 31.99258855846528959 ) ) ;
#14327=CARTESIAN_POINT ( 'NONE',  ( 2.274659669032305320, -44.77170999717656485, 26.26399533730382529 ) ) ;
#14343=CARTESIAN_POINT ( 'NONE',  ( 0.9468279798049143992, -43.93229166714461087, 27.28240155936039812 ) ) ;
#14351=CARTESIAN_POINT ( 'NONE',  ( 6.007384923554907274, -45.69729166657106845, 26.16266358875650866 ) ) ;
#14354=ORIENTED_EDGE ( 'NONE', *, *, #10796, .F. ) ;
#14358=CARTESIAN_POINT ( 'NONE',  ( 5.912663395429907709, -50.96979166714461940, 26.32672608803957459 ) ) ;
#14373=CARTESIAN_POINT ( 'NONE',  ( 6.749072665410328575, -51.38301154348381061, 26.69347430428500090 ) ) ;
#14374=CIRCLE ( 'NONE', #10301, 5.000000000000004441 ) ;
#14376=DIRECTION ( 'NONE',  ( -0.000000000000000000, 1.000000000000000000, -0.000000000000000000 ) ) ;
#14384=CARTESIAN_POINT ( 'NONE',  ( 5.848086763065961868, -51.03087679668490750, 32.31173612233266113 ) ) ;
#14393=CARTESIAN_POINT ( 'NONE',  ( 0.9468279798049143992, -51.93229166714461797, 27.28240155936039812 ) ) ;
#14396=CARTESIAN_POINT ( 'NONE',  ( 1.196164697370689645, -45.15190157074073340, 30.95144641820654741 ) ) ;
#14400=DIRECTION ( 'NONE',  ( 0.000000000000000000, 0.000000000000000000, -1.000000000000000000 ) ) ;
#14413=CARTESIAN_POINT ( 'NONE',  ( 2.507384923554911715, -49.77708333428924448, 26.16266358875650866 ) ) ;
#14429=CARTESIAN_POINT ( 'NONE',  ( 4.257384923554907274, -43.87499999999999289, 32.69375250200203453 ) ) ;
#14437=CARTESIAN_POINT ( 'NONE',  ( 7.701077676605128097, -42.95731928283520062, 29.81930176444853942 ) ) ;
#14444=ORIENTED_EDGE ( 'NONE', *, *, #2276, .F. ) ;
#14464=CARTESIAN_POINT ( 'NONE',  ( 4.257384923554908163, -46.67812500047794799, 33.01645438728532866 ) ) ;
#14498=CARTESIAN_POINT ( 'NONE',  ( 0.9468279798049134000, -48.34479166714461940, 27.28240155936039457 ) ) ;
#14502=CARTESIAN_POINT ( 'NONE',  ( 7.757384923554905498, -44.24999999999999289, 29.19375250200204164 ) ) ;
#14504=CARTESIAN_POINT ( 'NONE',  ( 7.736462770932773125, -49.43354815989309969, 28.74848346525752163 ) ) ;
#14508=CARTESIAN_POINT ( 'NONE',  ( 4.257384923554909051, -46.51562500047795368, 25.37105061671875461 ) ) ;
#14518=CARTESIAN_POINT ( 'NONE',  ( 0.7573849235549120484, -48.95833333333332149, 31.21447844416572792 ) ) ;
#14519=CARTESIAN_POINT ( 'NONE',  ( 2.602106451679912169, -47.97395833381128227, 26.32672608803957459 ) ) ;
#14526=CARTESIAN_POINT ( 'NONE',  ( 7.567941867304904591, -52.14062500047794657, 29.19375250200204164 ) ) ;
#14530=CARTESIAN_POINT ( 'NONE',  ( 0.7573849235549129366, -47.69375000095590877, 29.19375250200204164 ) ) ;
#14539=DIRECTION ( 'NONE',  ( 0.000000000000000000, 0.000000000000000000, -1.000000000000000000 ) ) ;
#14552=ORIENTED_EDGE ( 'NONE', *, *, #5578, .F. ) ;
#14554=CARTESIAN_POINT ( 'NONE',  ( 5.904305490310028048, -44.03119053920807602, 32.29885441545587810 ) ) ;
#14558=CARTESIAN_POINT ( 'NONE',  ( 0.9468279798049124008, -42.34895833381128227, 31.10510344464368515 ) ) ;
#14565=CARTESIAN_POINT ( 'NONE',  ( 6.007384923554904610, -46.86395833323773275, 32.22484141524757462 ) ) ;
#14567=ORIENTED_EDGE ( 'NONE', *, *, #30560, .F. ) ;
#14568=VERTEX_POINT ( 'NONE', #22196 ) ;
#14571=CARTESIAN_POINT ( 'NONE',  ( 2.602106451679911281, -51.88645833381128369, 26.32672608803957459 ) ) ;
#14574=EDGE_CURVE ( 'NONE', #28413, #15596, #15086, .T. ) ;
#14597=LINE ( 'NONE', #27571, #29898 ) ;
#14605=CARTESIAN_POINT ( 'NONE',  ( 7.567941867304902814, -50.68229166714461087, 31.10510344464368870 ) ) ;
#14610=CARTESIAN_POINT ( 'NONE',  ( 6.007384923554904610, -46.33333333333332149, 32.22484141524757462 ) ) ;
#14614=EDGE_LOOP ( 'NONE', ( #26691, #8218, #8056, #5024 ) ) ;
#14623=CARTESIAN_POINT ( 'NONE',  ( 7.757384923554905498, -50.24999999999998579, 29.19375250200204164 ) ) ;
#14625=CARTESIAN_POINT ( 'NONE',  ( 4.257384923554909051, -48.81875000095590167, 25.15230061767466552 ) ) ;
#14626=CARTESIAN_POINT ( 'NONE',  ( 7.567941867304904591, -42.64062500047794657, 29.19375250200204164 ) ) ;
#14644=CARTESIAN_POINT ( 'NONE',  ( 4.257384923554909051, -44.12499999999999289, 25.69375250200204519 ) ) ;
#14651=CARTESIAN_POINT ( 'NONE',  ( 6.047613445485506389, -42.86153037716380254, 26.16258216914170376 ) ) ;
#14663=CARTESIAN_POINT ( 'NONE',  ( 7.791602725366442606, -48.94417426152391926, 29.13997155634423919 ) ) ;
#14676=CARTESIAN_POINT ( 'NONE',  ( 2.602106451679911281, -46.88645833381128369, 26.32672608803957459 ) ) ;
#14685=EDGE_CURVE ( 'NONE', #34914, #679, #20133, .T. ) ;
#14707=CARTESIAN_POINT ( 'NONE',  ( 5.912663395429905044, -47.63645833381128369, 32.06077891596451224 ) ) ;
#14708=LINE ( 'NONE', #27666, #2092 ) ;
#14713=CARTESIAN_POINT ( 'NONE',  ( 7.757384923554904610, -45.70833333333332149, 27.17302655983835180 ) ) ;
#14716=CARTESIAN_POINT ( 'NONE',  ( 4.257384923554909051, -52.75000000000000000, 19.03247289836684786 ) ) ;
#14717=ORIENTED_EDGE ( 'NONE', *, *, #32604, .T. ) ;
#14718=CARTESIAN_POINT ( 'NONE',  ( 7.567941867304902814, -46.68229166714461087, 31.10510344464368870 ) ) ;
#14719=CARTESIAN_POINT ( 'NONE',  ( 0.9468279798049134000, -48.34479166714460519, 27.28240155936039102 ) ) ;
#14727=CARTESIAN_POINT ( 'NONE',  ( 7.757384923554904610, -43.70833333333331439, 27.17302655983835180 ) ) ;
#14728=CARTESIAN_POINT ( 'NONE',  ( 7.567941867304902814, -48.18229166714460376, 31.10510344464368870 ) ) ;
#14738=CARTESIAN_POINT ( 'NONE',  ( 7.757384923554905498, -48.44375000095590167, 29.19375250200204164 ) ) ;
#14756=EDGE_CURVE ( 'NONE', #34930, #37688, #15122, .T. ) ;
#14765=CARTESIAN_POINT ( 'NONE',  ( 7.632785701200944573, -43.92178927066061078, 28.16100524816936357 ) ) ;
#14774=CARTESIAN_POINT ( 'NONE',  ( 6.007384923554904610, -43.86395833323773275, 32.22484141524757462 ) ) ;
#14779=CARTESIAN_POINT ( 'NONE',  ( 4.257384923554909051, -51.42812500047794799, 25.37105061671875461 ) ) ;
#14810=CARTESIAN_POINT ( 'NONE',  ( 5.912663395429904156, -51.72395833381127517, 32.06077891596451224 ) ) ;
#14816=CARTESIAN_POINT ( 'NONE',  ( 5.195207097063847534, -46.14732909936925154, 25.69375250200204874 ) ) ;
#14827=CARTESIAN_POINT ( 'NONE',  ( 7.737111592484803957, -42.45202030341407351, 29.58884305679245585 ) ) ;
#14828=CARTESIAN_POINT ( 'NONE',  ( 2.507384923554909495, -48.61041666762257307, 32.22484141524756751 ) ) ;
#14829=CARTESIAN_POINT ( 'NONE',  ( 0.9468279798049132889, -43.39062500047794657, 29.19375250200204164 ) ) ;
#14843=DIRECTION ( 'NONE',  ( -0.000000000000000000, -1.000000000000000000, -0.000000000000000000 ) ) ;
#14849=CARTESIAN_POINT ( 'NONE',  ( 7.124667301592310764, -42.89478843769994398, 27.16628720921863049 ) ) ;
#14856=CARTESIAN_POINT ( 'NONE',  ( 4.257384923554909051, -49.12499999999998579, 25.69375250200204519 ) ) ;
#14863=CARTESIAN_POINT ( 'NONE',  ( 7.071476277146852674, -48.99580517798322177, 31.29180711805380000 ) ) ;
#14875=CARTESIAN_POINT ( 'NONE',  ( 7.567941867304904591, -44.09479166714461940, 31.10510344464368870 ) ) ;
#14888=CYLINDRICAL_SURFACE ( 'NONE', #810, 3.499999999999996003 ) ;
#14901=CARTESIAN_POINT ( 'NONE',  ( 4.257384923554908163, -45.17812500047794799, 33.01645438728532866 ) ) ;
#14906=CARTESIAN_POINT ( 'NONE',  ( 0.7573849235549120484, -43.95833333333332149, 31.21447844416572792 ) ) ;
#14912=CARTESIAN_POINT ( 'NONE',  ( 5.912663395429904156, -46.22395833381128227, 32.06077891596451224 ) ) ;
#14914=CARTESIAN_POINT ( 'NONE',  ( 5.912663395429905044, -46.63645833381128369, 32.06077891596451224 ) ) ;
#14924=CARTESIAN_POINT ( 'NONE',  ( 2.507384923554911715, -45.08333333333332149, 26.16266358875650866 ) ) ;
#14925=CARTESIAN_POINT ( 'NONE',  ( 0.9468279798049124008, -47.84895833381128227, 31.10510344464368515 ) ) ;
#14929=PLANE ( 'NONE',  #7198 ) ;
#14935=VERTEX_POINT ( 'NONE', #33668 ) ;
#14936=CARTESIAN_POINT ( 'NONE',  ( 2.507384923554909495, -46.61041666762257307, 32.22484141524756751 ) ) ;
#14976=ORIENTED_EDGE ( 'NONE', *, *, #22040, .F. ) ;
#14977=CARTESIAN_POINT ( 'NONE',  ( 4.257384923554909051, -44.15562499990440415, 25.15230061767466552 ) ) ;
#14979=ORIENTED_EDGE ( 'NONE', *, *, #8321, .F. ) ;
#14985=CARTESIAN_POINT ( 'NONE',  ( 0.9468279798049134000, -51.34479166714461940, 27.28240155936039457 ) ) ;
#15001=CARTESIAN_POINT ( 'NONE',  ( 4.257384923554931255, -43.37499999999999289, 32.69375250200203453 ) ) ;
#15017=CARTESIAN_POINT ( 'NONE',  ( 4.257384923554909051, -50.51562500047794657, 25.37105061671875461 ) ) ;
#15019=FACE_OUTER_BOUND ( 'NONE', #28748, .T. ) ;
#15020=CARTESIAN_POINT ( 'NONE',  ( 4.257384923554909051, -52.75000000000000000, 29.19375250200204164 ) ) ;
#15026=ORIENTED_EDGE ( 'NONE', *, *, #28074, .F. ) ;
#15029=CARTESIAN_POINT ( 'NONE',  ( 7.757384923554904610, -49.73895833323773275, 27.17302655983835180 ) ) ;
#15035=ADVANCED_FACE ( 'NONE', ( #11723 ), #24929, .T. ) ;
#15037=CARTESIAN_POINT ( 'NONE',  ( 6.007384923554907274, -46.36041666762257307, 26.16266358875650866 ) ) ;
#15043=CARTESIAN_POINT ( 'NONE',  ( 1.862562961008580320, -46.62798354932460398, 31.80581087231889370 ) ) ;
#15062=CARTESIAN_POINT ( 'NONE',  ( 4.257384923554896616, -48.12499999999998579, 25.69375250200204519 ) ) ;
#15066=CARTESIAN_POINT ( 'NONE',  ( 1.002747364484114723, -48.22340083344367656, 27.90563144571163789 ) ) ;
#15067=VERTEX_POINT ( 'NONE', #34281 ) ;
#15069=DIRECTION ( 'NONE',  ( 0.000000000000000000, 0.000000000000000000, -1.000000000000000000 ) ) ;
#15086=B_SPLINE_CURVE_WITH_KNOTS ( 'NONE', 3,
 ( #18172, #28572, #28153, #2628, #35164, #18590, #28363, #25191, #38151, #11777, #6028, #19005, #31971, #1999, #31758, #11988, #37942, #5826, #2840, #27739, #40709, #11565, #24773, #24559, #8381, #21360, #9867, #25814, #9432, #480, #35793, #32593, #3459, #3051 ),
 .UNSPECIFIED., .F., .F.,
 ( 4, 2, 1, 1, 1, 1, 2, 2, 2, 2, 2, 2, 2, 2, 2, 2, 1, 1, 2, 4 ),
 ( 0.8252512867581911493, 0.8252774937230057395, 0.8253037006878203297, 0.8253561146174493990, 0.8254609424767076487, 0.8256705981952241480, 0.8260899096322572577, 0.8269285325063233660, 0.8286057782544554717, 0.8319602697507197941, 0.8353147612469842276, 0.8386692527432485500, 0.8420237442395128724, 0.8453782357357771948, 0.8470554814839094115, 0.8472651372024259109, 0.8474747929209424102, 0.8478941043579755199, 0.8487327272320415172, 0.8520872187283060617 ),
 .UNSPECIFIED. ) ;
#15088=CARTESIAN_POINT ( 'NONE',  ( 2.602106451679911281, -43.88645833381129080, 26.32672608803957459 ) ) ;
#15109=CARTESIAN_POINT ( 'NONE',  ( 6.891126468185495568, -45.50330001549879455, 31.54102876720484616 ) ) ;
#15114=CARTESIAN_POINT ( 'NONE',  ( 0.7573849235549138248, -51.54166666666665719, 27.17302655983835180 ) ) ;
#15117=CARTESIAN_POINT ( 'NONE',  ( 5.912663395429907709, -46.96979166714461229, 26.32672608803957459 ) ) ;
#15122=CIRCLE ( 'NONE', #38889, 5.499999999999994671 ) ;
#15128=CARTESIAN_POINT ( 'NONE',  ( 7.567941867304902814, -43.18229166714461087, 31.10510344464368870 ) ) ;
#15129=CARTESIAN_POINT ( 'NONE',  ( 2.602106451679911281, -48.88645833381128369, 26.32672608803957459 ) ) ;
#15136=CARTESIAN_POINT ( 'NONE',  ( 6.007384923554907274, -44.16666666666665719, 26.16266358875650866 ) ) ;
#15137=CARTESIAN_POINT ( 'NONE',  ( 7.567941867304904591, -48.64062500047794657, 29.19375250200204164 ) ) ;
#15149=CARTESIAN_POINT ( 'NONE',  ( 7.757384923554904610, -47.90208333428924448, 27.17302655983835180 ) ) ;
#15164=CARTESIAN_POINT ( 'NONE',  ( 1.197689415489127773, -49.73658875364228749, 27.43350171975244933 ) ) ;
#15177=CARTESIAN_POINT ( 'NONE',  ( 4.257384923554908163, -43.26562500047793947, 33.01645438728532866 ) ) ;
#15182=CARTESIAN_POINT ( 'NONE',  ( 7.148879964610586057, -44.49362263921505445, 31.19088385935765828 ) ) ;
#15186=CARTESIAN_POINT ( 'NONE',  ( 4.257384923554909051, -43.15562499990439704, 25.15230061767466552 ) ) ;
#15193=CARTESIAN_POINT ( 'NONE',  ( 0.9468279798049125118, -50.30312500047794799, 29.19375250200204164 ) ) ;
#15195=CARTESIAN_POINT ( 'NONE',  ( 6.007384923554904610, -51.83333333333332149, 32.22484141524757462 ) ) ;
#15204=FACE_OUTER_BOUND ( 'NONE', #32232, .T. ) ;
#15230=CARTESIAN_POINT ( 'NONE',  ( 4.257384923554909051, -51.01562500047795368, 25.37105061671875461 ) ) ;
#15244=CARTESIAN_POINT ( 'NONE',  ( 0.7573849235549138248, -52.07229166657106845, 27.17302655983835180 ) ) ;
#15253=CARTESIAN_POINT ( 'NONE',  ( 6.007384923554907274, -46.86041666762257307, 26.16266358875650866 ) ) ;
#15257=CARTESIAN_POINT ( 'NONE',  ( 4.257384923554915268, -50.62499999999999289, 25.69375250200204519 ) ) ;
#15306=CARTESIAN_POINT ( 'NONE',  ( 0.9468279798049115126, -43.26145833381128369, 31.10510344464368515 ) ) ;
#15309=VECTOR ( 'NONE', #14376, 1000.000000000000000 ) ;
#15321=DIRECTION ( 'NONE',  ( 8.659560562354932858E-17, 0.7071067811865474617, -0.7071067811865474617 ) ) ;
#15327=CARTESIAN_POINT ( 'NONE',  ( 4.704965835571067956, -45.55695089492635219, 32.69375236535156404 ) ) ;
#15332=CARTESIAN_POINT ( 'NONE',  ( 2.510907866148289536, -45.60860063502410355, 32.26504739212718675 ) ) ;
#15341=VERTEX_POINT ( 'NONE', #19782 ) ;
#15342=FACE_OUTER_BOUND ( 'NONE', #23349, .T. ) ;
#15344=DIRECTION ( 'NONE',  ( -0.000000000000000000, -1.000000000000000000, -0.000000000000000000 ) ) ;
#15347=CARTESIAN_POINT ( 'NONE',  ( 7.567941867304904591, -42.64062500047794657, 29.19375250200204164 ) ) ;
#15350=CARTESIAN_POINT ( 'NONE',  ( 4.257384923554909051, -43.92812500047795510, 25.37105061671875106 ) ) ;
#15358=CARTESIAN_POINT ( 'NONE',  ( 2.507384923554911715, -44.08333333333332149, 26.16266358875650866 ) ) ;
#15359=CARTESIAN_POINT ( 'NONE',  ( 4.257384923554909051, -48.01562500047794657, 25.37105061671875106 ) ) ;
#15360=VERTEX_POINT ( 'NONE', #22144 ) ;
#15367=CARTESIAN_POINT ( 'NONE',  ( 4.257385003886612118, -45.31875000283309163, 25.69375250200204874 ) ) ;
#15371=CARTESIAN_POINT ( 'NONE',  ( 4.257384923554909051, -45.31875000095590877, 25.15230061767466552 ) ) ;
#15393=CARTESIAN_POINT ( 'NONE',  ( 4.257384923554908163, -49.37499999999998579, 33.23520438632941421 ) ) ;
#15399=CARTESIAN_POINT ( 'NONE',  ( 5.381673916920405532, -50.34354696738387247, 25.87138610505315128 ) ) ;
#15406=CARTESIAN_POINT ( 'NONE',  ( 0.7573849235549129366, -51.99999999999999289, 29.19375250200204164 ) ) ;
#15412=CARTESIAN_POINT ( 'NONE',  ( 7.567941867304905479, -48.01145833381128369, 27.28240155936039812 ) ) ;
#15413=CARTESIAN_POINT ( 'NONE',  ( 4.257384923554909051, 7.250000000000000000, 29.19375250200204164 ) ) ;
#15418=CARTESIAN_POINT ( 'NONE',  ( 0.7573849235549120484, -44.95833333333332149, 31.21447844416572792 ) ) ;
#15443=CARTESIAN_POINT ( 'NONE',  ( 5.912663395429907709, -48.55729166714461087, 26.32672608803957459 ) ) ;
#15444=CARTESIAN_POINT ( 'NONE',  ( 4.257384923554907274, -48.37499999999998579, 32.69375250200203453 ) ) ;
#15445=LINE ( 'NONE', #25647, #975 ) ;
#15448=CARTESIAN_POINT ( 'NONE',  ( 9.589638516698011372, 7.250000000000000000, 31.84134197688108614 ) ) ;
#15455=CARTESIAN_POINT ( 'NONE',  ( 0.7573849235549120484, -50.48895833323773275, 31.21447844416572792 ) ) ;
#15461=DIRECTION ( 'NONE',  ( 0.000000000000000000, 0.000000000000000000, -1.000000000000000000 ) ) ;
#15463=CARTESIAN_POINT ( 'NONE',  ( 2.507384923554909495, -46.61041666762257307, 32.22484141524756751 ) ) ;
#15468=CARTESIAN_POINT ( 'NONE',  ( 4.257384923554909939, 0.8500000000000035305, 39.35503210563723542 ) ) ;
#15491=CARTESIAN_POINT ( 'NONE',  ( 0.9268306642545129925, -48.21877478731359901, 28.11393890399381235 ) ) ;
#15496=CARTESIAN_POINT ( 'NONE',  ( 4.257384923554909051, -52.75000000000000000, 25.69375250200204519 ) ) ;
#15497=CARTESIAN_POINT ( 'NONE',  ( 5.195207097063841317, -48.85267090063072715, 32.69375250200202743 ) ) ;
#15509=ORIENTED_EDGE ( 'NONE', *, *, #25959, .F. ) ;
#15510=CARTESIAN_POINT ( 'NONE',  ( 7.567941867304905479, -44.51145833381129080, 27.28240155936039812 ) ) ;
#15525=DIRECTION ( 'NONE',  ( 0.9980327303751835855, 0.000000000000000000, -0.06269504844767276319 ) ) ;
#15532=DIRECTION ( 'NONE',  ( -0.000000000000000000, -1.000000000000000000, -0.000000000000000000 ) ) ;
#15536=CARTESIAN_POINT ( 'NONE',  ( 2.565389344933217242, -45.77717661627633561, 26.09935396029751686 ) ) ;
#15543=CARTESIAN_POINT ( 'NONE',  ( 6.007384923554907274, -42.66666666666665719, 26.16266358875650866 ) ) ;
#15545=CARTESIAN_POINT ( 'NONE',  ( 5.226271311602193492, -49.34190356823144441, 25.82178539275060558 ) ) ;
#15546=LINE ( 'NONE', #14716, #11537 ) ;
#15548=CARTESIAN_POINT ( 'NONE',  ( 0.9468279798049143992, -44.93229166714461797, 27.28240155936039812 ) ) ;
#15549=CARTESIAN_POINT ( 'NONE',  ( 4.257384923554909051, -45.92812500047796220, 25.37105061671875106 ) ) ;
#15555=VERTEX_POINT ( 'NONE', #40196 ) ;
#15558=CARTESIAN_POINT ( 'NONE',  ( 4.257384923554909051, -45.62499999999999289, 25.15230061767466552 ) ) ;
#15559=CARTESIAN_POINT ( 'NONE',  ( 5.912663395429907709, -44.05729166714461797, 26.32672608803957459 ) ) ;
#15561=DIRECTION ( 'NONE',  ( -0.000000000000000000, -1.000000000000000000, -0.000000000000000000 ) ) ;
#15595=CARTESIAN_POINT ( 'NONE',  ( 4.257384923554908163, -49.87499999999999289, 33.23520438632941421 ) ) ;
#15596=VERTEX_POINT ( 'NONE', #3832 ) ;
#15598=VECTOR ( 'NONE', #38424, 1000.000000000000114 ) ;
#15602=CARTESIAN_POINT ( 'NONE',  ( 7.567941867304904591, -52.14062500047794657, 29.19375250200204164 ) ) ;
#15606=( BOUNDED_CURVE ( )  B_SPLINE_CURVE ( 2, ( #4819, #1629, #14610, #27583, #8215, #37982, #5866, #14816, #5656 ),
 .UNSPECIFIED., .F., .T. ) 
 B_SPLINE_CURVE_WITH_KNOTS ( ( 3, 2, 2, 2, 3 ),
 ( 0.5875000000000000222, 0.5916666666666666741, 0.5999999999999999778, 0.6083333333333332815, 0.6124999999999999334 ),
 .UNSPECIFIED. ) 
 CURVE ( )  GEOMETRIC_REPRESENTATION_ITEM ( )  RATIONAL_B_SPLINE_CURVE ( ( 0.9330127018922194093, 0.9330127018922194093, 1.000000000000000000, 0.8660254037844387076, 1.000000000000000000, 0.8660254037844387076, 1.000000000000000000, 0.9330127018922202975, 0.9330127018922194093 ) ) 
 REPRESENTATION_ITEM ( '' )  );
#15610=CARTESIAN_POINT ( 'NONE',  ( 7.757384923554905498, -51.74999999999999289, 29.19375250200204164 ) ) ;
#15614=AXIS2_PLACEMENT_3D ( 'NONE', #15694, #35243, #38227 ) ;
#15617=CARTESIAN_POINT ( 'NONE',  ( 2.602106451679911281, -49.88645833381128369, 26.32672608803957459 ) ) ;
#15618=DIRECTION ( 'NONE',  ( 0.000000000000000000, 0.000000000000000000, 1.000000000000000000 ) ) ;
#15620=CARTESIAN_POINT ( 'NONE',  ( 3.352452488000560393, -48.79715768487822913, 25.80502639550580923 ) ) ;
#15651=CARTESIAN_POINT ( 'NONE',  ( 4.257384923554909051, -49.01562500047793947, 25.37105061671875461 ) ) ;
#15652=DIRECTION ( 'NONE',  ( 0.8329741740894176516, 0.000000000000000000, -0.5533118698347727626 ) ) ;
#15665=CARTESIAN_POINT ( 'NONE',  ( 6.007384923554904610, -49.86395833323773275, 32.22484141524757462 ) ) ;
#15670=CARTESIAN_POINT ( 'NONE',  ( 4.679965312749212458, -42.55868857278844075, 32.69375250201897387 ) ) ;
#15671=CARTESIAN_POINT ( 'NONE',  ( 0.7573849235549120484, -47.15208333428923737, 31.21447844416572792 ) ) ;
#15677=CARTESIAN_POINT ( 'NONE',  ( 4.229829917954948115, -46.81809420038812419, 25.69384524017633709 ) ) ;
#15694=CARTESIAN_POINT ( 'NONE',  ( 4.257384923554909051, 5.249999999999997335, 29.19375250200204164 ) ) ;
#15701=EDGE_CURVE ( 'NONE', #38516, #16189, #5508, .T. ) ;
#15704=DIRECTION ( 'NONE',  ( -0.000000000000000000, -1.000000000000000000, -0.000000000000000000 ) ) ;
#15711=CARTESIAN_POINT ( 'NONE',  ( 6.595757437628482656, -48.01206338924518491, 31.82289736963684490 ) ) ;
#15721=CARTESIAN_POINT ( 'NONE',  ( 0.9468279798049134000, -42.34479166714461940, 27.28240155936039457 ) ) ;
#15743=CARTESIAN_POINT ( 'NONE',  ( 7.558581467624073014, -45.41722474197759851, 28.02109436123814135 ) ) ;
#15753=CARTESIAN_POINT ( 'NONE',  ( 7.757384923554902834, -42.79166666666665719, 31.21447844416572792 ) ) ;
#15757=CARTESIAN_POINT ( 'NONE',  ( 5.912663395429907709, -45.05729166714461797, 26.32672608803957459 ) ) ;
#15758=CARTESIAN_POINT ( 'NONE',  ( 5.912663395429907709, -44.46979166714461940, 26.32672608803957459 ) ) ;
#15766=CARTESIAN_POINT ( 'NONE',  ( 6.317863118539786882, -46.86968173906446822, 26.33787851343121034 ) ) ;
#15767=CARTESIAN_POINT ( 'NONE',  ( 6.007384923554904610, -51.02708333428923737, 32.22484141524757462 ) ) ;
#15768=CARTESIAN_POINT ( 'NONE',  ( 4.257384923554909051, -46.51562500047795368, 25.37105061671875106 ) ) ;
#15770=ADVANCED_FACE ( 'NONE', ( #18484, #37426 ), #37630, .T. ) ;
#15806=CARTESIAN_POINT ( 'NONE',  ( 2.722807162759138588, -47.10612055722910441, 32.36495752999819331 ) ) ;
#15807=( BOUNDED_CURVE ( )  B_SPLINE_CURVE ( 2, ( #28522, #39730, #23363, #7404, #39512, #29519, #2580, #22350, #23581 ),
 .UNSPECIFIED., .F., .F. ) 
 B_SPLINE_CURVE_WITH_KNOTS ( ( 3, 2, 2, 2, 3 ),
 ( 0.01250000000000000243, 0.01666666666666666644, 0.02500000000000000139, 0.03333333333333333287, 0.03749999999999999861 ),
 .UNSPECIFIED. ) 
 CURVE ( )  GEOMETRIC_REPRESENTATION_ITEM ( )  RATIONAL_B_SPLINE_CURVE ( ( 0.9330127018922194093, 0.9330127018922194093, 1.000000000000000000, 0.8660254037844387076, 1.000000000000000000, 0.8660254037844387076, 1.000000000000000000, 0.9330127018922194093, 0.9330127018922194093 ) ) 
 REPRESENTATION_ITEM ( '' )  );
#15809=CARTESIAN_POINT ( 'NONE',  ( 7.757384923554905498, -49.24999999999998579, 29.19375250200204164 ) ) ;
#15815=CARTESIAN_POINT ( 'NONE',  ( 4.526053432582991753, -43.32458953733280538, 25.70366498296531077 ) ) ;
#15817=CARTESIAN_POINT ( 'NONE',  ( 5.912663395429907709, -51.55729166714461797, 26.32672608803957459 ) ) ;
#15824=CARTESIAN_POINT ( 'NONE',  ( 6.007384923554907274, -50.66666666666665719, 26.16266358875650866 ) ) ;
#15830=CARTESIAN_POINT ( 'NONE',  ( 7.087903831510641517, -46.49564367575952417, 31.27518496280760374 ) ) ;
#15833=CARTESIAN_POINT ( 'NONE',  ( 4.257384923554909051, -49.42812500047794799, 25.37105061671875461 ) ) ;
#15834=CARTESIAN_POINT ( 'NONE',  ( 2.507384923554911715, -46.08333333333332149, 26.16266358875650866 ) ) ;
#15839=LINE ( 'NONE', #41778, #17657 ) ;
#15862=AXIS2_PLACEMENT_3D ( 'NONE', #35070, #5930, #12524 ) ;
#15869=CARTESIAN_POINT ( 'NONE',  ( 7.567941867304904591, -49.09895833381128227, 27.28240155936039812 ) ) ;
#15874=CARTESIAN_POINT ( 'NONE',  ( 5.912663395429905044, -49.63645833381128369, 32.06077891596451224 ) ) ;
#15881=CARTESIAN_POINT ( 'NONE',  ( 7.757384923554904610, -51.23895833323773275, 27.17302655983835180 ) ) ;
#15888=CARTESIAN_POINT ( 'NONE',  ( 4.257384923554908163, -47.56875000095590877, 33.23520438632941421 ) ) ;
#15894=CARTESIAN_POINT ( 'NONE',  ( 1.296425106312324438, -46.73832029726629855, 27.27900400513847856 ) ) ;
#15903=CARTESIAN_POINT ( 'NONE',  ( 4.257384924376430568, -51.81875000097547002, 25.69375250200204519 ) ) ;
#15913=DIRECTION ( 'NONE',  ( 0.000000000000000000, 0.000000000000000000, -1.000000000000000000 ) ) ;
#15916=CARTESIAN_POINT ( 'NONE',  ( 3.170302522513056775, -48.29317881804618651, 25.85979247468966591 ) ) ;
#15921=CARTESIAN_POINT ( 'NONE',  ( 4.257384923554909051, -46.92812500047795510, 25.37105061671875461 ) ) ;
#15935=ADVANCED_FACE ( 'NONE', ( #172 ), #26138, .T. ) ;
#15943=DIRECTION ( 'NONE',  ( -0.000000000000000000, -1.000000000000000000, -0.000000000000000000 ) ) ;
#15964=CARTESIAN_POINT ( 'NONE',  ( 4.037193678478864456, -45.81388164294964582, 25.69895105699555771 ) ) ;
#15976=CARTESIAN_POINT ( 'NONE',  ( 2.602106451679909505, -43.30729166714461797, 32.06077891596451224 ) ) ;
#15977=CARTESIAN_POINT ( 'NONE',  ( 7.567941867304905479, -46.05312500047794799, 29.19375250200204164 ) ) ;
#15988=LINE ( 'NONE', #32340, #6806 ) ;
#15989=CARTESIAN_POINT ( 'NONE',  ( 7.567941867304902814, -46.09895833381128227, 27.28240155936039457 ) ) ;
#16017=VERTEX_POINT ( 'NONE', #25927 ) ;
#16023=CARTESIAN_POINT ( 'NONE',  ( 2.969868793495920034, -47.28911517217845528, 25.92902108495795588 ) ) ;
#16026=CARTESIAN_POINT ( 'NONE',  ( 0.7573849235549138248, -49.04166666666665009, 27.17302655983835180 ) ) ;
#16033=CARTESIAN_POINT ( 'NONE',  ( 2.602106451679909505, -51.30729166714461797, 32.06077891596451224 ) ) ;
#16037=CARTESIAN_POINT ( 'NONE',  ( 0.7712042165907809776, -51.20546035091972215, 28.64685322309688331 ) ) ;
#16040=CARTESIAN_POINT ( 'NONE',  ( 2.507384923554911715, -50.58333333333332860, 26.16266358875650866 ) ) ;
#16043=CARTESIAN_POINT ( 'NONE',  ( 4.707335199593570607, -46.32939083886152787, 25.71220708268069188 ) ) ;
#16045=CARTESIAN_POINT ( 'NONE',  ( 2.602106451679909505, -49.21979166714461940, 32.06077891596451224 ) ) ;
#16047=AXIS2_PLACEMENT_3D ( 'NONE', #18123, #34697, #5563 ) ;
#16049=CARTESIAN_POINT ( 'NONE',  ( 0.7684730838774413986, -48.68787772272541758, 29.47215482281801968 ) ) ;
#16057=EDGE_CURVE ( 'NONE', #26970, #9447, #31124, .T. ) ;
#16084=CARTESIAN_POINT ( 'NONE',  ( 0.9468279798049143992, -46.93229166714461087, 27.28240155936039812 ) ) ;
#16085=CARTESIAN_POINT ( 'NONE',  ( 4.257384923554909051, 5.249999999999997335, 19.03247289836684786 ) ) ;
#16089=CARTESIAN_POINT ( 'NONE',  ( 2.602106451679911281, -51.38645833381127659, 26.32672608803957459 ) ) ;
#16093=PRODUCT_CONTEXT ( 'NONE', #25552, 'mechanical' ) ;
#16096=CARTESIAN_POINT ( 'NONE',  ( 2.507384923554911715, -49.61395833323773275, 26.16266358875650866 ) ) ;
#16101=CARTESIAN_POINT ( 'NONE',  ( 7.757384923554902834, -44.48541666762257307, 31.21447844416572792 ) ) ;
#16118=CARTESIAN_POINT ( 'NONE',  ( 3.649380331186591331, -51.58322629214500665, 32.69375250155312784 ) ) ;
#16127=DIRECTION ( 'NONE',  ( -0.000000000000000000, -1.000000000000000000, -0.000000000000000000 ) ) ;
#16133=ORIENTED_EDGE ( 'NONE', *, *, #19953, .F. ) ;
#16135=CARTESIAN_POINT ( 'NONE',  ( 0.7593285874961362980, -46.19106856474823530, 29.32449512433518279 ) ) ;
#16136=CARTESIAN_POINT ( 'NONE',  ( 0.9468279798049134000, -45.84479166714461229, 27.28240155936039457 ) ) ;
#16140=CARTESIAN_POINT ( 'NONE',  ( 0.7573849235549120484, -49.95833333333332860, 31.21447844416572792 ) ) ;
#16153=PLANE ( 'NONE',  #16726 ) ;
#16177=DIRECTION ( 'NONE',  ( 0.06269504844767277707, 0.000000000000000000, 0.9980327303751835855 ) ) ;
#16186=CARTESIAN_POINT ( 'NONE',  ( 0.9468279798049124008, -42.34895833381128227, 31.10510344464368515 ) ) ;
#16187=CARTESIAN_POINT ( 'NONE',  ( 0.9468279798049117346, -44.76145833381129080, 31.10510344464368515 ) ) ;
#16189=VERTEX_POINT ( 'NONE', #24505 ) ;
#16193=CARTESIAN_POINT ( 'NONE',  ( 2.602106451679909505, -45.30729166714461797, 32.06077891596451224 ) ) ;
#16215=ORIENTED_EDGE ( 'NONE', *, *, #29750, .F. ) ;
#16220=CARTESIAN_POINT ( 'NONE',  ( 7.567941867304904591, -51.09479166714461940, 31.10510344464368870 ) ) ;
#16221=CARTESIAN_POINT ( 'NONE',  ( 4.715533434895189835, -47.55760065792828328, 32.69375245562657284 ) ) ;
#16224=CARTESIAN_POINT ( 'NONE',  ( 4.257384923554909051, -46.12500000000000000, 25.15230061767466552 ) ) ;
#16225=ORIENTED_EDGE ( 'NONE', *, *, #18124, .F. ) ;
#16226=( BOUNDED_CURVE ( )  B_SPLINE_CURVE ( 2, ( #19098, #28873, #25493, #42074, #9318, #16140, #35688, #22285, #38663 ),
 .UNSPECIFIED., .F., .T. ) 
 B_SPLINE_CURVE_WITH_KNOTS ( ( 3, 2, 2, 2, 3 ),
 ( 0.2124999999999999944, 0.2166666666666666741, 0.2250000000000000056, 0.2333333333333333370, 0.2375000000000000167 ),
 .UNSPECIFIED. ) 
 CURVE ( )  GEOMETRIC_REPRESENTATION_ITEM ( )  RATIONAL_B_SPLINE_CURVE ( ( 0.9330127018922194093, 0.9330127018922191873, 1.000000000000000000, 0.8660254037844387076, 1.000000000000000000, 0.8660254037844387076, 1.000000000000000000, 0.9330127018922191873, 0.9330127018922194093 ) ) 
 REPRESENTATION_ITEM ( '' )  );
#16232=CARTESIAN_POINT ( 'NONE',  ( 4.257337177015303453, -43.31874891592651977, 25.69375250232772245 ) ) ;
#16233=CARTESIAN_POINT ( 'NONE',  ( 7.567941867304904591, -48.59895833381128227, 27.28240155936039812 ) ) ;
#16236=CARTESIAN_POINT ( 'NONE',  ( 2.799664999047590364, -51.10346044585850933, 32.37578816141000004 ) ) ;
#16238=CARTESIAN_POINT ( 'NONE',  ( 2.507384923554909495, -50.41666666666665719, 32.22484141524756751 ) ) ;
#16239=CARTESIAN_POINT ( 'NONE',  ( 7.757384923554905498, -45.24999999999999289, 29.19375250200204164 ) ) ;
#16240=EDGE_CURVE ( 'NONE', #9447, #16017, #37883, .T. ) ;
#16241=EDGE_LOOP ( 'NONE', ( #25849, #8227, #1951, #22091 ) ) ;
#16246=CARTESIAN_POINT ( 'NONE',  ( 1.014090813125490653, -48.66334322452244976, 30.55303934225188556 ) ) ;
#16250=CARTESIAN_POINT ( 'NONE',  ( 6.007384923554907274, -51.86041666762257307, 26.16266358875650866 ) ) ;
#16263=CARTESIAN_POINT ( 'NONE',  ( 1.862529241339832220, -44.12798434721139529, 31.80578232064003430 ) ) ;
#16281=CARTESIAN_POINT ( 'NONE',  ( 5.912663395429904156, -47.72395833381128227, 32.06077891596451224 ) ) ;
#16284=CARTESIAN_POINT ( 'NONE',  ( 4.257384923554909051, -50.92812500047794799, 25.37105061671875106 ) ) ;
#16292=CARTESIAN_POINT ( 'NONE',  ( 0.7573849235549138248, -48.07229166657106845, 27.17302655983835180 ) ) ;
#16299=CARTESIAN_POINT ( 'NONE',  ( 4.257384923554908163, -43.56875000095590877, 33.23520438632941421 ) ) ;
#16321=LINE ( 'NONE', #39255, #11882 ) ;
#16336=CARTESIAN_POINT ( 'NONE',  ( 4.257384923554909051, -45.92812500047794799, 25.37105061671875461 ) ) ;
#16369=CARTESIAN_POINT ( 'NONE',  ( 6.007384923554907274, -52.16666666666665719, 26.16266358875650866 ) ) ;
#16375=LINE ( 'NONE', #12752, #29763 ) ;
#16378=CARTESIAN_POINT ( 'NONE',  ( 4.739764703921419908, -45.32930553300766263, 25.69375250707629021 ) ) ;
#16382=DIRECTION ( 'NONE',  ( -0.9980327303751835855, 0.000000000000000000, 0.06269504844767277707 ) ) ;
#16394=ORIENTED_EDGE ( 'NONE', *, *, #13914, .T. ) ;
#16400=CARTESIAN_POINT ( 'NONE',  ( 5.912663395429904156, -44.22395833381127517, 32.06077891596451224 ) ) ;
#16429=CARTESIAN_POINT ( 'NONE',  ( 2.602106451679909505, -51.21979166714461940, 32.06077891596451224 ) ) ;
#16430=CARTESIAN_POINT ( 'NONE',  ( 3.481432367832919539, -47.08792997467101316, 32.63022858438433360 ) ) ;
#16432=CARTESIAN_POINT ( 'NONE',  ( 6.007384923554904610, -47.33333333333332149, 32.22484141524757462 ) ) ;
#16434=PLANE ( 'NONE',  #12503 ) ;
#16436=ORIENTED_EDGE ( 'NONE', *, *, #37687, .F. ) ;
#16438=CARTESIAN_POINT ( 'NONE',  ( 7.567941867304904591, -48.09895833381128227, 27.28240155936039812 ) ) ;
#16445=CARTESIAN_POINT ( 'NONE',  ( 4.257384923554909051, -51.62499999999999289, 25.15230061767466552 ) ) ;
#16453=CARTESIAN_POINT ( 'NONE',  ( 0.8357940588222394496, -48.71286678597664377, 28.32074073763388000 ) ) ;
#16457=CARTESIAN_POINT ( 'NONE',  ( 7.757384923554904610, -51.40208333428923027, 27.17302655983835180 ) ) ;
#16473=CARTESIAN_POINT ( 'NONE',  ( 0.7573849235549138248, -42.73541666762258018, 27.17302655983835180 ) ) ;
#16485=CARTESIAN_POINT ( 'NONE',  ( 7.567941867304904591, -44.14062500047794657, 29.19375250200204164 ) ) ;
#16491=CARTESIAN_POINT ( 'NONE',  ( 2.602106451679909505, -51.21979166714461940, 32.06077891596451224 ) ) ;
#16498=CARTESIAN_POINT ( 'NONE',  ( 6.007384923554907274, -47.69729166657106845, 26.16266358875650866 ) ) ;
#16504=CARTESIAN_POINT ( 'NONE',  ( 6.007384923554904610, -43.52708333428924448, 32.22484141524757462 ) ) ;
#16505=CARTESIAN_POINT ( 'NONE',  ( 0.7573849235549138248, -43.73541666762257307, 27.17302655983835180 ) ) ;
#16543=CARTESIAN_POINT ( 'NONE',  ( 4.257384923554908163, -43.67812500047794799, 33.01645438728532866 ) ) ;
#16546=CARTESIAN_POINT ( 'NONE',  ( 4.611024687279486223, -44.06168471479399784, 32.69375256036362032 ) ) ;
#16553=CARTESIAN_POINT ( 'NONE',  ( 7.022015372733203087, -48.38858039930481425, 27.00064690223579689 ) ) ;
#16562=CARTESIAN_POINT ( 'NONE',  ( 2.507384923554909495, -42.91666666666665719, 32.22484141524756751 ) ) ;
#16569=EDGE_CURVE ( 'NONE', #6171, #37984, #15988, .T. ) ;
#16575=EDGE_CURVE ( 'NONE', #10524, #10651, #19118, .T. ) ;
#16585=CARTESIAN_POINT ( 'NONE',  ( 0.7573849235549138248, -48.04166666666665719, 27.17302655983835180 ) ) ;
#16601=CARTESIAN_POINT ( 'NONE',  ( 7.567941867304905479, -43.05312500047794799, 29.19375250200204164 ) ) ;
#16610=CARTESIAN_POINT ( 'NONE',  ( 4.889406927138391978, -46.05370173170800996, 32.63622221452869354 ) ) ;
#16634=FACE_OUTER_BOUND ( 'NONE', #14261, .T. ) ;
#16635=CARTESIAN_POINT ( 'NONE',  ( 0.8451499254546688267, -47.17417678362879485, 30.09738622103246541 ) ) ;
#16638=CARTESIAN_POINT ( 'NONE',  ( 2.507384923554911715, -47.58333333333332149, 26.16266358875650866 ) ) ;
#16639=ORIENTED_EDGE ( 'NONE', *, *, #1083, .T. ) ;
#16645=CARTESIAN_POINT ( 'NONE',  ( 6.086168908141100786, -43.52748871755736104, 32.20936235694947669 ) ) ;
#16646=CARTESIAN_POINT ( 'NONE',  ( 7.567941867304904591, -49.59895833381128227, 27.28240155936039812 ) ) ;
#16650=DIRECTION ( 'NONE',  ( 0.000000000000000000, 0.000000000000000000, -1.000000000000000000 ) ) ;
#16652=CARTESIAN_POINT ( 'NONE',  ( 0.7573849235549129366, -51.49999999999999289, 29.19375250200204164 ) ) ;
#16653=CARTESIAN_POINT ( 'NONE',  ( 0.9468279798049124008, -51.34895833381127517, 31.10510344464368515 ) ) ;
#16655=CARTESIAN_POINT ( 'NONE',  ( 4.956464721733225609, -46.55389097732946624, 32.63984723290977286 ) ) ;
#16662=( BOUNDED_CURVE ( )  B_SPLINE_CURVE ( 2, ( #12708, #41427, #2290, #28025, #19085, #9089, #34615, #38443, #9305 ),
 .UNSPECIFIED., .F., .F. ) 
 B_SPLINE_CURVE_WITH_KNOTS ( ( 3, 2, 2, 2, 3 ),
 ( 0.9375000000000000000, 0.9416666666666666519, 0.9499999999999999556, 0.9583333333333333703, 0.9625000000000000222 ),
 .UNSPECIFIED. ) 
 CURVE ( )  GEOMETRIC_REPRESENTATION_ITEM ( )  RATIONAL_B_SPLINE_CURVE ( ( 0.9330127018922194093, 0.9330127018922194093, 1.000000000000000000, 0.8660254037844387076, 1.000000000000000000, 0.8660254037844387076, 1.000000000000000000, 0.9330127018922194093, 0.9330127018922194093 ) ) 
 REPRESENTATION_ITEM ( '' )  );
#16663=CARTESIAN_POINT ( 'NONE',  ( 6.007384923554904610, -50.02708333428924448, 32.22484141524757462 ) ) ;
#16671=ORIENTED_EDGE ( 'NONE', *, *, #41194, .T. ) ;
#16673=B_SPLINE_CURVE_WITH_KNOTS ( 'NONE', 3,
 ( #7866, #2088, #1880, #18467, #28244, #34627, #4864, #27830, #40393, #17844, #34012, #8677, #14863, #8471, #34423, #14663, #11451, #30817, #21650, #21448, #11868, #30606, #5492, #40595, #28035, #41017 ),
 .UNSPECIFIED., .F., .F.,
 ( 4, 2, 2, 2, 2, 2, 2, 2, 2, 2, 2, 2, 4 ),
 ( 0.2936963628370675705, 0.2966598464927014955, 0.2974007174066099490, 0.2975859351350870763, 0.2977711528635642035, 0.2981415883205184580, 0.2996233301483354206, 0.3025868138039693456, 0.3055502974596032706, 0.3085137811152371956, 0.3114772647708711761, 0.3144407484265051012, 0.3174042320821390262 ),
 .UNSPECIFIED. ) ;
#16676=CARTESIAN_POINT ( 'NONE',  ( 4.257373630597665937, -44.06920056960389331, 32.69375250196740978 ) ) ;
#16679=CARTESIAN_POINT ( 'NONE',  ( 2.722808792670202038, -44.60612035451349300, 32.36495826875209758 ) ) ;
#16693=CARTESIAN_POINT ( 'NONE',  ( 4.257384923554908163, -45.76562500047795368, 33.01645438728532866 ) ) ;
#16697=CARTESIAN_POINT ( 'NONE',  ( 7.567941867304902814, -51.59479166714461940, 31.10510344464368870 ) ) ;
#16702=CARTESIAN_POINT ( 'NONE',  ( 7.757384923554902834, -49.32229166657106845, 31.21447844416572792 ) ) ;
#16707=CARTESIAN_POINT ( 'NONE',  ( 6.007384923554904610, -44.02708333428924448, 32.22484141524757462 ) ) ;
#16708=CARTESIAN_POINT ( 'NONE',  ( 4.257384923554908163, -45.06875000095590877, 33.23520438632941421 ) ) ;
#16723=CARTESIAN_POINT ( 'NONE',  ( 4.257384923554909939, -52.75000000000000000, 39.35503210563723542 ) ) ;
#16726=AXIS2_PLACEMENT_3D ( 'NONE', #811, #40563, #1642 ) ;
#16727=CARTESIAN_POINT ( 'NONE',  ( 2.142597841376364887, -51.76591979834516621, 26.35441391374854092 ) ) ;
#16736=CARTESIAN_POINT ( 'NONE',  ( 4.257404126188692572, -50.06796725373735057, 32.69375250189985138 ) ) ;
#16742=DIRECTION ( 'NONE',  ( 1.000000000000000000, 0.000000000000000000, -0.000000000000000000 ) ) ;
#16746=CARTESIAN_POINT ( 'NONE',  ( 0.9468279798049125118, -44.30312500047794799, 29.19375250200204164 ) ) ;
#16747=CARTESIAN_POINT ( 'NONE',  ( 4.257384923554909051, -42.40485061181025372, 32.69375250200203453 ) ) ;
#16756=CARTESIAN_POINT ( 'NONE',  ( 4.775657658050108445, -48.55640513467545816, 32.65540673540338901 ) ) ;
#16766=CARTESIAN_POINT ( 'NONE',  ( 4.257387527570275054, -50.81875003717480155, 25.69375250200301508 ) ) ;
#16767=B_SPLINE_CURVE_WITH_KNOTS ( 'NONE', 3,
 ( #12067, #2927, #35250, #5486, #25061, #41646, #15916, #25692, #5700, #2505, #34416, #5276, #8886, #38022, #15066, #28030, #15491, #12498, #2295, #28445, #18462, #32057, #25485, #9311, #21644, #22276, #41432, #28863, #38655, #12283, #25267, #6111, #38234, #41863, #34620, #22074, #12714 ),
 .UNSPECIFIED., .F., .F.,
 ( 4, 2, 2, 2, 2, 2, 2, 2, 2, 2, 2, 2, 2, 2, 1, 2, 2, 2, 4 ),
 ( 0.3681897126842696988, 0.3689425091585314398, 0.3696953056327931253, 0.3712008985813165518, 0.3742120844783634048, 0.3772232703754102578, 0.3775996686125411284, 0.3779760668496719989, 0.3787288633239337399, 0.3802344562724572774, 0.3832456421695042970, 0.3839984386437660380, 0.3843748368808969085, 0.3844689364401796539, 0.3845630359994623992, 0.3847512351180278345, 0.3862568280665515386, 0.3892680139635988912, 0.3922791998606462993 ),
 .UNSPECIFIED. ) ;
#16768=CARTESIAN_POINT ( 'NONE',  ( 0.7573849235549120484, -43.45833333333332149, 31.21447844416572792 ) ) ;
#16772=EDGE_CURVE ( 'NONE', #13809, #321, #34105, .T. ) ;
#16791=CARTESIAN_POINT ( 'NONE',  ( 7.407476139744110455, -45.40812920926124008, 27.66825174283231803 ) ) ;
#16800=VERTEX_POINT ( 'NONE', #9220 ) ;
#16803=EDGE_CURVE ( 'NONE', #40970, #3008, #38461, .T. ) ;
#16804=ORIENTED_EDGE ( 'NONE', *, *, #39924, .F. ) ;
#16805=CARTESIAN_POINT ( 'NONE',  ( 5.912663395429905044, -42.63645833381128369, 32.06077891596451224 ) ) ;
#16810=CARTESIAN_POINT ( 'NONE',  ( 7.567941867304905479, -49.01145833381127659, 27.28240155936039812 ) ) ;
#16842=CARTESIAN_POINT ( 'NONE',  ( 5.912663395429907709, -50.46979166714461940, 26.32672608803957459 ) ) ;
#16845=CARTESIAN_POINT ( 'NONE',  ( 0.7573849235549120484, -48.45833333333332860, 31.21447844416572792 ) ) ;
#16848=( BOUNDED_CURVE ( )  B_SPLINE_CURVE ( 2, ( #37608, #36777, #17432, #14027, #7638, #28654, #31846, #37815, #2714 ),
 .UNSPECIFIED., .F., .F. ) 
 B_SPLINE_CURVE_WITH_KNOTS ( ( 3, 2, 2, 2, 3 ),
 ( 0.6624999999999999778, 0.6666666666666666297, 0.6750000000000000444, 0.6833333333333333481, 0.6875000000000000000 ),
 .UNSPECIFIED. ) 
 CURVE ( )  GEOMETRIC_REPRESENTATION_ITEM ( )  RATIONAL_B_SPLINE_CURVE ( ( 0.9330127018922194093, 0.9330127018922194093, 1.000000000000000000, 0.8660254037844387076, 1.000000000000000000, 0.8660254037844387076, 1.000000000000000000, 0.9330127018922194093, 0.9330127018922194093 ) ) 
 REPRESENTATION_ITEM ( '' )  );
#16854=CARTESIAN_POINT ( 'NONE',  ( 7.567941867304902814, -49.68229166714461797, 31.10510344464368870 ) ) ;
#16862=CARTESIAN_POINT ( 'NONE',  ( 2.507384923554909495, -48.91666666666665719, 32.22484141524756751 ) ) ;
#16863=CARTESIAN_POINT ( 'NONE',  ( 5.912663395429907709, -50.55729166714461797, 26.32672608803957459 ) ) ;
#16871=CARTESIAN_POINT ( 'NONE',  ( 2.507384923554909495, -51.11041666762257307, 32.22484141524756751 ) ) ;
#16887=CARTESIAN_POINT ( 'NONE',  ( 2.975060292544088991, -42.09928153978950149, 32.45038320576673385 ) ) ;
#16895=ORIENTED_EDGE ( 'NONE', *, *, #7499, .T. ) ;
#16897=CARTESIAN_POINT ( 'NONE',  ( 0.9468279798049132889, -45.89062500047794657, 29.19375250200204164 ) ) ;
#16902=CARTESIAN_POINT ( 'NONE',  ( 4.257384923554908163, -46.67812500047796220, 33.01645438728532866 ) ) ;
#16908=CARTESIAN_POINT ( 'NONE',  ( 4.257384923554909051, -48.65562499990440415, 25.15230061767466552 ) ) ;
#16913=CIRCLE ( 'NONE', #27087, 2.000000000000001776 ) ;
#16916=CARTESIAN_POINT ( 'NONE',  ( 2.507384923554911715, -43.77708333428924448, 26.16266358875650866 ) ) ;
#16919=EDGE_LOOP ( 'NONE', ( #19122, #39505, #34068, #32909, #32498, #39032, #32239, #29235, #36723, #22143, #29663, #23773, #32752, #1327, #20994, #26380, #4089, #38199, #13828, #12562, #39268, #37171, #13775, #24283, #37936, #34280, #26339, #21909, #19265, #1533, #8023, #32116, #36158, #36189, #14717, #31133, #31232, #5909, #6326, #10260, #3446, #18953, #3559 ) ) ;
#16931=CARTESIAN_POINT ( 'NONE',  ( 4.993779605986802039, -51.33633701436628627, 25.76912581695707516 ) ) ;
#16953=CARTESIAN_POINT ( 'NONE',  ( 7.567941867304905479, -42.51145833381128369, 27.28240155936039812 ) ) ;
#16956=DIRECTION ( 'NONE',  ( -0.000000000000000000, -1.000000000000000000, -0.000000000000000000 ) ) ;
#16962=AXIS2_PLACEMENT_3D ( 'NONE', #40367, #17408, #24006 ) ;
#16963=CARTESIAN_POINT ( 'NONE',  ( 5.178944950686976689, -42.40581226674584769, 25.80588562437470301 ) ) ;
#16967=CARTESIAN_POINT ( 'NONE',  ( 2.797696106033661589, -44.28379444243795149, 25.99126114642119489 ) ) ;
#16974=CARTESIAN_POINT ( 'NONE',  ( 0.7573849235549138248, -43.54166666666665719, 27.17302655983835180 ) ) ;
#16978=FACE_OUTER_BOUND ( 'NONE', #3883, .T. ) ;
#16990=CARTESIAN_POINT ( 'NONE',  ( 4.257384923554909051, -52.75000000000000000, 29.19375250200204164 ) ) ;
#17001=CARTESIAN_POINT ( 'NONE',  ( 3.319562750045975452, -48.10267090063072004, 25.69375250200204519 ) ) ;
#17004=CARTESIAN_POINT ( 'NONE',  ( 4.257404126188692572, -50.06796725373735057, 32.69375250189985138 ) ) ;
#17011=ORIENTED_EDGE ( 'NONE', *, *, #33401, .F. ) ;
#17022=CARTESIAN_POINT ( 'NONE',  ( 0.9468279798049134000, -44.84479166714461940, 27.28240155936039457 ) ) ;
#17025=CARTESIAN_POINT ( 'NONE',  ( 4.866650383396064150, -46.05424367296411248, 32.64031920267535725 ) ) ;
#17053=CARTESIAN_POINT ( 'NONE',  ( 5.912663395429907709, -51.96979166714461940, 26.32672608803957459 ) ) ;
#17056=CARTESIAN_POINT ( 'NONE',  ( 6.007384923554904610, -46.33333333333332149, 32.22484141524757462 ) ) ;
#17059=CARTESIAN_POINT ( 'NONE',  ( 2.697319420846179483, -49.10451515202854011, 32.34178364494799496 ) ) ;
#17062=CARTESIAN_POINT ( 'NONE',  ( 4.257384923554908163, -49.76562500047794657, 33.01645438728532866 ) ) ;
#17071=CARTESIAN_POINT ( 'NONE',  ( 6.007384923554904610, -46.83333333333332149, 32.22484141524757462 ) ) ;
#17072=CARTESIAN_POINT ( 'NONE',  ( 0.9468279798049132889, -50.39062500047794657, 29.19375250200204164 ) ) ;
#17075=CARTESIAN_POINT ( 'NONE',  ( 2.240470916522819600, -43.11621117806984671, 32.07551745261009302 ) ) ;
#17082=CARTESIAN_POINT ( 'NONE',  ( 7.757384923554904610, -50.40208333428924448, 27.17302655983835180 ) ) ;
#17093=CARTESIAN_POINT ( 'NONE',  ( 7.315643298427244368, -44.90153327204530598, 27.43109671079633927 ) ) ;
#17096=CARTESIAN_POINT ( 'NONE',  ( 0.7275300035338608806, -44.69487529891586064, 29.18866941669331183 ) ) ;
#17104=CARTESIAN_POINT ( 'NONE',  ( 4.257384923554933032, -44.62499999999999289, 25.69375250200204519 ) ) ;
#17111=CARTESIAN_POINT ( 'NONE',  ( 2.602106451679912169, -45.47395833381128227, 26.32672608803957459 ) ) ;
#17116=CARTESIAN_POINT ( 'NONE',  ( 7.567941867304902814, -48.59479166714461229, 31.10510344464368870 ) ) ;
#17120=ORIENTED_EDGE ( 'NONE', *, *, #33721, .F. ) ;
#17122=ORIENTED_EDGE ( 'NONE', *, *, #23306, .F. ) ;
#17123=CARTESIAN_POINT ( 'NONE',  ( 0.7573849235549129366, -46.53062499990440415, 29.19375250200204164 ) ) ;
#17129=CARTESIAN_POINT ( 'NONE',  ( 0.7573849235549129366, -45.19375000095590877, 29.19375250200204164 ) ) ;
#17144=CARTESIAN_POINT ( 'NONE',  ( 4.266838237385764288, -51.31897507244583068, 25.69376205134561530 ) ) ;
#17156=FACE_OUTER_BOUND ( 'NONE', #12231, .T. ) ;
#17169=CARTESIAN_POINT ( 'NONE',  ( 5.912663395429905044, -44.13645833381129080, 32.06077891596451224 ) ) ;
#17179=CARTESIAN_POINT ( 'NONE',  ( 2.825111381773371733, -42.40355319057812267, 25.99726070350407880 ) ) ;
#17185=ORIENTED_EDGE ( 'NONE', *, *, #22820, .F. ) ;
#17187=CARTESIAN_POINT ( 'NONE',  ( 5.195207097063839541, -50.14732909936925154, 25.69375250200204874 ) ) ;
#17189=CARTESIAN_POINT ( 'NONE',  ( 0.7573849235549138248, -51.73541666762258018, 27.17302655983835180 ) ) ;
#17191=CARTESIAN_POINT ( 'NONE',  ( 4.257384923554909051, -43.01562500047794657, 25.37105061671875106 ) ) ;
#17193=VECTOR ( 'NONE', #2320, 1000.000000000000000 ) ;
#17214=CARTESIAN_POINT ( 'NONE',  ( 4.027787496314825688, -47.81372590936857847, 25.69375250065493432 ) ) ;
#17234=CARTESIAN_POINT ( 'NONE',  ( 0.9468279798049125118, -43.30312500047794799, 29.19375250200204164 ) ) ;
#17239=CARTESIAN_POINT ( 'NONE',  ( 2.602106451679909505, -45.71979166714461229, 32.06077891596451224 ) ) ;
#17242=CLOSED_SHELL ( 'NONE', ( #1819, #3895, #27542, #2513, #15035, #35497, #19891, #9539, #18218, #24976, #3567, #10056, #26228, #39906, #18568, #35788, #11315, #35756, #37057, #390, #28629, #41226, #32231, #10557, #21337, #30353, #39091, #39669, #36350, #11120, #29812, #9075, #27002, #37146, #19975, #23884, #4374, #17346, #36066, #25289, #24579, #195, #22247, #36503, #25874, #689, #4370, #29568, #15770, #15935, #29141, #1556, #21952, #20550, #1171, #10023, #7507, #7457, #4935, #9752, #17254, #19948, #29126, #29863, #25097, #35594, #2321, #36855 ) ) ;
#17243=CARTESIAN_POINT ( 'NONE',  ( 4.775653861276124346, -46.05640522773727241, 32.65540730014851789 ) ) ;
#17246=ORIENTED_EDGE ( 'NONE', *, *, #20395, .F. ) ;
#17254=ADVANCED_FACE ( 'NONE', ( #28628 ), #6139, .T. ) ;
#17269=CARTESIAN_POINT ( 'NONE',  ( 0.9468279798049115126, -47.26145833381127659, 31.10510344464368515 ) ) ;
#17273=CARTESIAN_POINT ( 'NONE',  ( 0.7573849235549138248, -44.04166666666665719, 27.17302655983835180 ) ) ;
#17280=CARTESIAN_POINT ( 'NONE',  ( 0.9468279798049143992, -46.43229166714461087, 27.28240155936039812 ) ) ;
#17288=CARTESIAN_POINT ( 'NONE',  ( 4.257384923554909051, -48.12499999999998579, 25.15230061767466552 ) ) ;
#17289=CARTESIAN_POINT ( 'NONE',  ( 2.602106451679912169, -50.47395833381128227, 26.32672608803957459 ) ) ;
#17292=CARTESIAN_POINT ( 'NONE',  ( 4.257384923554931255, -43.37499999999999289, 32.69375250200203453 ) ) ;
#17299=CARTESIAN_POINT ( 'NONE',  ( 7.757384923554905498, -48.94375000095590167, 29.19375250200204164 ) ) ;
#17314=CARTESIAN_POINT ( 'NONE',  ( 0.7573849235549129366, -42.19375000095590167, 29.19375250200204164 ) ) ;
#17320=CARTESIAN_POINT ( 'NONE',  ( 4.257403850124284794, -43.06798715535520472, 32.69375250190384463 ) ) ;
#17325=CARTESIAN_POINT ( 'NONE',  ( 4.257384923554931255, -43.37499999999999289, 32.69375250200203453 ) ) ;
#17327=CARTESIAN_POINT ( 'NONE',  ( 0.9468279798049143992, -46.43229166714461087, 27.28240155936039812 ) ) ;
#17335=EDGE_LOOP ( 'NONE', ( #21843, #23771, #30405, #13084, #16225 ) ) ;
#17336=CARTESIAN_POINT ( 'NONE',  ( 6.007384923554907274, -46.19729166657106845, 26.16266358875650866 ) ) ;
#17342=CARTESIAN_POINT ( 'NONE',  ( 0.7573849235549138248, -44.73541666762258018, 27.17302655983835180 ) ) ;
#17344=LINE ( 'NONE', #37324, #9583 ) ;
#17346=ADVANCED_FACE ( 'NONE', ( #26290 ), #29242, .T. ) ;
#17381=CARTESIAN_POINT ( 'NONE',  ( 4.257384923554908163, -42.67812500047794799, 33.01645438728532866 ) ) ;
#17389=CARTESIAN_POINT ( 'NONE',  ( 4.910181181136407780, -48.55320664656201757, 32.63238650312012368 ) ) ;
#17390=ORIENTED_EDGE ( 'NONE', *, *, #17548, .F. ) ;
#17394=CARTESIAN_POINT ( 'NONE',  ( 0.9319271095403495186, -50.22280438673409719, 28.00235999796277397 ) ) ;
#17402=CARTESIAN_POINT ( 'NONE',  ( 7.757384923554904610, -48.40208333428923737, 27.17302655983835180 ) ) ;
#17405=ORIENTED_EDGE ( 'NONE', *, *, #8851, .T. ) ;
#17408=DIRECTION ( 'NONE',  ( -0.000000000000000000, -1.000000000000000000, -0.000000000000000000 ) ) ;
#17431=CARTESIAN_POINT ( 'NONE',  ( 1.204823857811940346, -47.73607277547826300, 27.42106328382752167 ) ) ;
#17432=CARTESIAN_POINT ( 'NONE',  ( 2.507384923554911715, -45.58333333333332149, 26.16266358875650866 ) ) ;
#17438=DIRECTION ( 'NONE',  ( 0.000000000000000000, 0.000000000000000000, -1.000000000000000000 ) ) ;
#17452=ORIENTED_EDGE ( 'NONE', *, *, #3315, .F. ) ;
#17454=CARTESIAN_POINT ( 'NONE',  ( 7.567941867304905479, -46.51145833381128369, 27.28240155936039812 ) ) ;
#17461=EDGE_LOOP ( 'NONE', ( #14444, #26818, #19216, #30770 ) ) ;
#17482=CARTESIAN_POINT ( 'NONE',  ( 0.9468279798049115126, -49.26145833381128369, 31.10510344464368515 ) ) ;
#17486=CARTESIAN_POINT ( 'NONE',  ( 4.257384923554909051, -45.62499999999999289, 25.15230061767466552 ) ) ;
#17493=CARTESIAN_POINT ( 'NONE',  ( 0.9468279798049143992, -46.93229166714461087, 27.28240155936039812 ) ) ;
#17498=CARTESIAN_POINT ( 'NONE',  ( 4.257384923554909051, -47.12499999999999289, 25.15230061767466552 ) ) ;
#17499=CARTESIAN_POINT ( 'NONE',  ( 2.602106451679912169, -49.47395833381128227, 26.32672608803957459 ) ) ;
#17508=CARTESIAN_POINT ( 'NONE',  ( 7.757384923554905498, -46.94375000095590877, 29.19375250200204164 ) ) ;
#17516=CARTESIAN_POINT ( 'NONE',  ( 7.757386103033468316, -44.93265859128980821, 28.73561336441095548 ) ) ;
#17533=CARTESIAN_POINT ( 'NONE',  ( 6.415323780099212669, -50.51768454959326249, 31.98745583173668550 ) ) ;
#17537=CARTESIAN_POINT ( 'NONE',  ( 7.779217216655366585, -44.45355210293071480, 29.54642497685722091 ) ) ;
#17541=CARTESIAN_POINT ( 'NONE',  ( 0.7573849235549138248, -45.57229166657107555, 27.17302655983835180 ) ) ;
#17547=CARTESIAN_POINT ( 'NONE',  ( 5.195207097063837764, -50.85267090063073425, 32.69375250200203453 ) ) ;
#17548=EDGE_CURVE ( 'NONE', #13147, #34930, #21151, .T. ) ;
#17549=CARTESIAN_POINT ( 'NONE',  ( 7.567941867304904591, -51.59479166714461940, 31.10510344464368870 ) ) ;
#17557=AXIS2_PLACEMENT_3D ( 'NONE', #27103, #30925, #11353 ) ;
#17566=CARTESIAN_POINT ( 'NONE',  ( 4.632038606075823850, -51.32766984582223557, 25.71308297382691066 ) ) ;
#17569=CARTESIAN_POINT ( 'NONE',  ( 5.195207097063831547, -48.14732909936925154, 25.69375250200204164 ) ) ;
#17586=CARTESIAN_POINT ( 'NONE',  ( 2.602106451679912169, -51.47395833381127517, 26.32672608803957459 ) ) ;
#17595=FACE_OUTER_BOUND ( 'NONE', #41593, .T. ) ;
#17601=CARTESIAN_POINT ( 'NONE',  ( 1.372692075071819451, -50.24462996302281681, 27.15497028180735484 ) ) ;
#17608=EDGE_CURVE ( 'NONE', #37126, #30827, #24354, .T. ) ;
#17609=CARTESIAN_POINT ( 'NONE',  ( 6.007384923554907274, -50.36041666762257307, 26.16266358875650866 ) ) ;
#17610=CARTESIAN_POINT ( 'NONE',  ( 7.567941867304902814, -43.09895833381128227, 27.28240155936039457 ) ) ;
#17628=CARTESIAN_POINT ( 'NONE',  ( 4.560670012418957420, -42.82584505446858714, 25.69807864655268048 ) ) ;
#17633=CARTESIAN_POINT ( 'NONE',  ( 0.7585202976687700493, -47.70447161036407380, 28.72631004132002630 ) ) ;
#17639=EDGE_CURVE ( 'NONE', #41408, #28413, #17344, .T. ) ;
#17655=CARTESIAN_POINT ( 'NONE',  ( 4.257384923554909051, -47.42812500047794799, 25.37105061671875461 ) ) ;
#17657=VECTOR ( 'NONE', #25615, 1000.000000000000000 ) ;
#17658=EDGE_LOOP ( 'NONE', ( #29647, #12886, #18933, #23878 ) ) ;
#17686=CARTESIAN_POINT ( 'NONE',  ( 5.912663395429907709, -49.46979166714461940, 26.32672608803957459 ) ) ;
#17690=CARTESIAN_POINT ( 'NONE',  ( 7.757384923554905498, -43.74999999999999289, 29.19375250200204164 ) ) ;
#17702=CARTESIAN_POINT ( 'NONE',  ( 6.007384923554904610, -46.33333333333332149, 32.22484141524757462 ) ) ;
#17703=CARTESIAN_POINT ( 'NONE',  ( 5.912663395429907709, -48.55729166714461087, 26.32672608803957459 ) ) ;
#17713=CARTESIAN_POINT ( 'NONE',  ( 2.507384923554911715, -48.27708333428923737, 26.16266358875650866 ) ) ;
#17723=CARTESIAN_POINT ( 'NONE',  ( 6.020064644314659930, -44.86010142892099140, 26.13550791927527683 ) ) ;
#17738=CARTESIAN_POINT ( 'NONE',  ( 7.753280596255371471, -43.93292809180421443, 28.64643166545664243 ) ) ;
#17741=CARTESIAN_POINT ( 'NONE',  ( 0.9468279798049124008, -42.84895833381128227, 31.10510344464368515 ) ) ;
#17750=ORIENTED_EDGE ( 'NONE', *, *, #33663, .F. ) ;
#17751=CARTESIAN_POINT ( 'NONE',  ( 2.507384923554909495, -46.44729166657106845, 32.22484141524756751 ) ) ;
#17758=CARTESIAN_POINT ( 'NONE',  ( 2.507384923554911715, -42.27708333428924448, 26.16266358875650866 ) ) ;
#17772=CARTESIAN_POINT ( 'NONE',  ( 7.716709722723441800, -51.43002001426882686, 28.53806490422757491 ) ) ;
#17780=EDGE_CURVE ( 'NONE', #7238, #15341, #21776, .T. ) ;
#17783=CARTESIAN_POINT ( 'NONE',  ( 7.307774966076294731, -42.40391780584809567, 27.47736923338838011 ) ) ;
#17790=CARTESIAN_POINT ( 'NONE',  ( 5.912663395429904156, -51.22395833381127517, 32.06077891596451224 ) ) ;
#17802=CARTESIAN_POINT ( 'NONE',  ( 2.103395109276308794, -50.12030546550250421, 31.99034297650314684 ) ) ;
#17811=CARTESIAN_POINT ( 'NONE',  ( 0.7573849235549129366, -49.19375000095590167, 29.19375250200204164 ) ) ;
#17824=CARTESIAN_POINT ( 'NONE',  ( 2.507384923554909495, -43.91666666666665719, 32.22484141524756751 ) ) ;
#17835=CARTESIAN_POINT ( 'NONE',  ( 1.196169441440665615, -47.65190129272988884, 30.95145438127327964 ) ) ;
#17841=CARTESIAN_POINT ( 'NONE',  ( 5.459046503238084824, -42.40485061181025372, 32.53552244146850114 ) ) ;
#17844=CARTESIAN_POINT ( 'NONE',  ( 6.602477018248971596, -49.01111519826702079, 31.79286654198001827 ) ) ;
#17858=CARTESIAN_POINT ( 'NONE',  ( 4.257384923554908163, -45.67812500047795510, 33.01645438728532866 ) ) ;
#17863=CARTESIAN_POINT ( 'NONE',  ( 4.257384923554933032, -44.62499999999999289, 25.69375250200204519 ) ) ;
#17866=ORIENTED_EDGE ( 'NONE', *, *, #3315, .T. ) ;
#17876=DIRECTION ( 'NONE',  ( -0.000000000000000000, -1.000000000000000000, -0.000000000000000000 ) ) ;
#17891=CARTESIAN_POINT ( 'NONE',  ( 2.602106451679909505, -48.21979166714461229, 32.06077891596451224 ) ) ;
#17892=CARTESIAN_POINT ( 'NONE',  ( 4.257467766145297539, -43.81875197339704897, 25.69375250298245916 ) ) ;
#17896=CARTESIAN_POINT ( 'NONE',  ( 0.7573849235549129366, -44.49999999999999289, 29.19375250200204164 ) ) ;
#17900=CARTESIAN_POINT ( 'NONE',  ( 4.257384923554908163, -46.76562500047794657, 33.01645438728532866 ) ) ;
#17902=CARTESIAN_POINT ( 'NONE',  ( 2.602106451679911281, -46.88645833381128369, 26.32672608803957459 ) ) ;
#17908=CARTESIAN_POINT ( 'NONE',  ( 6.007384923554904610, -43.83333333333332149, 32.22484141524757462 ) ) ;
#17909=CARTESIAN_POINT ( 'NONE',  ( 7.567941867304902814, -48.09895833381128227, 27.28240155936039457 ) ) ;
#17913=DIRECTION ( 'NONE',  ( -0.5533118698347725406, 0.000000000000000000, -0.8329741740894178736 ) ) ;
#17920=ORIENTED_EDGE ( 'NONE', *, *, #7499, .F. ) ;
#17921=CARTESIAN_POINT ( 'NONE',  ( 4.257384923554909051, -47.81875000095592299, 25.15230061767466552 ) ) ;
#17927=EDGE_CURVE ( 'NONE', #38516, #18276, #35592, .T. ) ;
#17937=CARTESIAN_POINT ( 'NONE',  ( 1.462158283685268678, -49.64173990296366412, 31.34942581913036008 ) ) ;
#17946=CARTESIAN_POINT ( 'NONE',  ( 4.257467766145297539, -43.81875197339704897, 25.69375250298245916 ) ) ;
#17950=CARTESIAN_POINT ( 'NONE',  ( 7.567941867304902814, -43.18229166714461087, 31.10510344464368870 ) ) ;
#17957=CARTESIAN_POINT ( 'NONE',  ( 0.7573849235549138248, -46.07229166657106845, 27.17302655983835180 ) ) ;
#17960=ORIENTED_EDGE ( 'NONE', *, *, #11153, .T. ) ;
#17963=CARTESIAN_POINT ( 'NONE',  ( 4.257384923554908163, -50.67812500047794799, 33.01645438728532866 ) ) ;
#17964=VECTOR ( 'NONE', #10421, 1000.000000000000000 ) ;
#17974=LINE ( 'NONE', #34347, #2066 ) ;
#17983=CARTESIAN_POINT ( 'NONE',  ( 4.257404373735115044, -49.56795750272889478, 32.69375250189725080 ) ) ;
#17990=CARTESIAN_POINT ( 'NONE',  ( 4.257384923554909051, -52.75000000000000000, 29.19375250200204164 ) ) ;
#17997=CARTESIAN_POINT ( 'NONE',  ( 5.912663395429907709, -51.55729166714461797, 26.32672608803957459 ) ) ;
#18000=CARTESIAN_POINT ( 'NONE',  ( 4.027785755371767529, -45.31372586545636238, 25.69375249958685004 ) ) ;
#18002=CARTESIAN_POINT ( 'NONE',  ( 2.602106451679911281, -51.88645833381128369, 26.32672608803957459 ) ) ;
#18009=CARTESIAN_POINT ( 'NONE',  ( 4.257404126188692572, -50.06796725373735057, 32.69375250189985138 ) ) ;
#18013=CARTESIAN_POINT ( 'NONE',  ( 4.257384923554907274, -50.37499999999998579, 32.69375250200203453 ) ) ;
#18014=CARTESIAN_POINT ( 'NONE',  ( 7.711105262912270497, -42.43061216113024869, 28.57001118150609287 ) ) ;
#18015=CARTESIAN_POINT ( 'NONE',  ( 7.757384923554902834, -48.48541666762256597, 31.21447844416572792 ) ) ;
#18040=EDGE_CURVE ( 'NONE', #2991, #41285, #507, .T. ) ;
#18045=CARTESIAN_POINT ( 'NONE',  ( 3.339839038092423440, -47.58897909153638039, 32.60236888880887562 ) ) ;
#18050=CARTESIAN_POINT ( 'NONE',  ( 6.007384923554904610, -49.33333333333332860, 32.22484141524757462 ) ) ;
#18063=VERTEX_POINT ( 'NONE', #28777 ) ;
#18068=CARTESIAN_POINT ( 'NONE',  ( 7.567941867304905479, -43.55312500047794799, 29.19375250200204164 ) ) ;
#18083=FACE_OUTER_BOUND ( 'NONE', #35825, .T. ) ;
#18099=CARTESIAN_POINT ( 'NONE',  ( 7.567941867304904591, -48.59479166714461940, 31.10510344464368870 ) ) ;
#18104=CARTESIAN_POINT ( 'NONE',  ( 2.507384923554909495, -44.41666666666665719, 32.22484141524756751 ) ) ;
#18106=CARTESIAN_POINT ( 'NONE',  ( 7.104627408622158136, -49.39484185763559765, 27.10932692453258142 ) ) ;
#18109=CARTESIAN_POINT ( 'NONE',  ( 0.9468279798049143992, -45.93229166714461087, 27.28240155936039812 ) ) ;
#18111=CARTESIAN_POINT ( 'NONE',  ( 2.602106451679911281, -47.88645833381128369, 26.32672608803957459 ) ) ;
#18118=CARTESIAN_POINT ( 'NONE',  ( 4.257384923554908163, -45.37499999999999289, 33.23520438632941421 ) ) ;
#18119=CARTESIAN_POINT ( 'NONE',  ( 0.9468279798049143992, -47.93229166714461087, 27.28240155936039457 ) ) ;
#18123=CARTESIAN_POINT ( 'NONE',  ( 4.257384923554909051, -52.75000000000000000, 29.19375250200204164 ) ) ;
#18124=EDGE_CURVE ( 'NONE', #18585, #27384, #7351, .T. ) ;
#18131=CARTESIAN_POINT ( 'NONE',  ( 7.757384923554904610, -46.90208333428923027, 27.17302655983835180 ) ) ;
#18167=CARTESIAN_POINT ( 'NONE',  ( 7.757384923554904610, -43.73895833323772564, 27.17302655983835180 ) ) ;
#18172=CARTESIAN_POINT ( 'NONE',  ( 4.257467766145297539, -43.81875197339704897, 25.69375250298245916 ) ) ;
#18174=CARTESIAN_POINT ( 'NONE',  ( 0.9468279798049115126, -51.26145833381129080, 31.10510344464368515 ) ) ;
#18206=CARTESIAN_POINT ( 'NONE',  ( 7.567941867304904591, -51.09895833381128227, 27.28240155936039812 ) ) ;
#18207=DIRECTION ( 'NONE',  ( 0.000000000000000000, -1.000000000000000000, -0.000000000000000000 ) ) ;
#18217=CARTESIAN_POINT ( 'NONE',  ( 2.507384923554911715, -52.11395833323773275, 26.16266358875650866 ) ) ;
#18218=ADVANCED_FACE ( 'NONE', ( #10125 ), #32659, .T. ) ;
#18223=CARTESIAN_POINT ( 'NONE',  ( 7.281634078944689392, -42.48431629580117175, 30.98330804292861984 ) ) ;
#18224=CARTESIAN_POINT ( 'NONE',  ( 2.507384923554909495, -50.61041666762257307, 32.22484141524756751 ) ) ;
#18229=CARTESIAN_POINT ( 'NONE',  ( 0.7833283242627300247, -46.70303563019047743, 28.75679378155784605 ) ) ;
#18234=ORIENTED_EDGE ( 'NONE', *, *, #17927, .F. ) ;
#18253=CARTESIAN_POINT ( 'NONE',  ( 4.157907407854070314, -46.31638304700847186, 25.69496350073779922 ) ) ;
#18265=ORIENTED_EDGE ( 'NONE', *, *, #29003, .F. ) ;
#18266=ORIENTED_EDGE ( 'NONE', *, *, #36844, .F. ) ;
#18269=CARTESIAN_POINT ( 'NONE',  ( 0.9468279798049134000, -43.84479166714461940, 27.28240155936039457 ) ) ;
#18273=CARTESIAN_POINT ( 'NONE',  ( 4.257384923554931255, -45.87499999999999289, 32.69375250200203453 ) ) ;
#18276=VERTEX_POINT ( 'NONE', #10750 ) ;
#18277=VECTOR ( 'NONE', #14208, 1000.000000000000000 ) ;
#18284=CARTESIAN_POINT ( 'NONE',  ( 4.257384923554909051, -52.75000000000000000, 26.19375250200205230 ) ) ;
#18297=CARTESIAN_POINT ( 'NONE',  ( 7.567941867304904591, -44.59479166714461940, 31.10510344464368870 ) ) ;
#18305=CARTESIAN_POINT ( 'NONE',  ( 6.104647974681401301, -49.36399588568571772, 26.18350227275256614 ) ) ;
#18308=CARTESIAN_POINT ( 'NONE',  ( 0.9468279798049132889, -42.89062500047794657, 29.19375250200204164 ) ) ;
#18309=CARTESIAN_POINT ( 'NONE',  ( 5.912663395429907709, -47.46979166714461229, 26.32672608803957459 ) ) ;
#18317=CARTESIAN_POINT ( 'NONE',  ( 4.257384923554908163, -44.37499999999999289, 33.23520438632941421 ) ) ;
#18318=CARTESIAN_POINT ( 'NONE',  ( 0.9468279798049143992, -47.43229166714461087, 27.28240155936039457 ) ) ;
#18327=ORIENTED_EDGE ( 'NONE', *, *, #25931, .T. ) ;
#18332=CARTESIAN_POINT ( 'NONE',  ( 2.507384923554911715, -46.77708333428923737, 26.16266358875650866 ) ) ;
#18354=CARTESIAN_POINT ( 'NONE',  ( 4.257384923554907274, -50.37499999999998579, 32.69375250200203453 ) ) ;
#18361=EDGE_CURVE ( 'NONE', #34951, #8688, #17974, .T. ) ;
#18365=CARTESIAN_POINT ( 'NONE',  ( 5.912663395429904156, -43.22395833381127517, 32.06077891596451224 ) ) ;
#18369=CARTESIAN_POINT ( 'NONE',  ( 4.257364759755165373, -44.56955858896998279, 32.69375250189113302 ) ) ;
#18373=CARTESIAN_POINT ( 'NONE',  ( 4.257384923554909051, -42.65562499990439704, 25.15230061767466552 ) ) ;
#18381=CARTESIAN_POINT ( 'NONE',  ( 4.257384923554909051, -50.42812500047794799, 25.37105061671875461 ) ) ;
#18397=CARTESIAN_POINT ( 'NONE',  ( 7.757384923554905498, -43.24999999999999289, 29.19375250200204164 ) ) ;
#18399=CARTESIAN_POINT ( 'NONE',  ( 0.7573849235549138248, -46.54166666666665719, 27.17302655983835180 ) ) ;
#18415=CARTESIAN_POINT ( 'NONE',  ( 0.9468279798049143992, -49.43229166714461797, 27.28240155936039812 ) ) ;
#18416=DIRECTION ( 'NONE',  ( 0.5533118698347727626, 0.000000000000000000, 0.8329741740894176516 ) ) ;
#18426=CARTESIAN_POINT ( 'NONE',  ( 7.757384923554904610, -50.73895833323773985, 27.17302655983835180 ) ) ;
#18432=CARTESIAN_POINT ( 'NONE',  ( 7.748022612349314109, -42.44956337252566669, 29.47292738127782386 ) ) ;
#18433=CARTESIAN_POINT ( 'NONE',  ( 2.507384923554911715, -47.77708333428923737, 26.16266358875650866 ) ) ;
#18438=CARTESIAN_POINT ( 'NONE',  ( 3.252690536537945043, -46.59224857966543709, 32.58724403798436242 ) ) ;
#18462=CARTESIAN_POINT ( 'NONE',  ( 0.7518121276228710848, -48.18476069298282738, 29.64312138438439348 ) ) ;
#18465=CARTESIAN_POINT ( 'NONE',  ( 3.972865654299906790, -46.31198540363738658, 25.70486921022052229 ) ) ;
#18466=CARTESIAN_POINT ( 'NONE',  ( -0.7016216170541935693, 3.250000000000000444, 32.48782483564529855 ) ) ;
#18467=CARTESIAN_POINT ( 'NONE',  ( 6.118325136139532106, -49.02469819937434181, 32.16209055562107721 ) ) ;
#18482=CARTESIAN_POINT ( 'NONE',  ( 0.9468279798049115126, -44.26145833381128369, 31.10510344464368515 ) ) ;
#18484=FACE_OUTER_BOUND ( 'NONE', #33607, .T. ) ;
#18503=DIRECTION ( 'NONE',  ( 0.000000000000000000, 0.000000000000000000, -1.000000000000000000 ) ) ;
#18508=CARTESIAN_POINT ( 'NONE',  ( 1.490420712370577494, -45.64058454871335613, 31.35540716855688004 ) ) ;
#18517=CARTESIAN_POINT ( 'NONE',  ( 4.257384923554909051, -43.12499999999999289, 25.15230061767466552 ) ) ;
#18519=CARTESIAN_POINT ( 'NONE',  ( 3.882851339416273806, -42.80983302217806852, 25.71307002722200608 ) ) ;
#18522=CARTESIAN_POINT ( 'NONE',  ( 0.9468279798049143992, -43.43229166714461797, 27.28240155936039812 ) ) ;
#18523=CARTESIAN_POINT ( 'NONE',  ( 7.567941867304905479, -44.01145833381129080, 27.28240155936039457 ) ) ;
#18532=CARTESIAN_POINT ( 'NONE',  ( 7.757384923554904610, -45.20833333333332149, 27.17302655983835180 ) ) ;
#18533=CARTESIAN_POINT ( 'NONE',  ( 7.567941867304902814, -48.68229166714461087, 31.10510344464368870 ) ) ;
#18536=CYLINDRICAL_SURFACE ( 'NONE', #16047, 3.499999999999996003 ) ;
#18546=CARTESIAN_POINT ( 'NONE',  ( 4.257384923554908163, -45.56875000095590877, 33.23520438632941421 ) ) ;
#18562=CARTESIAN_POINT ( 'NONE',  ( 6.228309098867199189, -51.02156414445331478, 32.09277250805516246 ) ) ;
#18568=ADVANCED_FACE ( 'NONE', ( #15204 ), #19229, .T. ) ;
#18569=CARTESIAN_POINT ( 'NONE',  ( 7.757384923554904610, -50.70833333333332860, 27.17302655983835180 ) ) ;
#18575=CARTESIAN_POINT ( 'NONE',  ( 6.007384923554904610, -51.33333333333332149, 32.22484141524757462 ) ) ;
#18577=CARTESIAN_POINT ( 'NONE',  ( 4.271641082492189767, -50.31905671966664784, 25.69377426149561217 ) ) ;
#18585=VERTEX_POINT ( 'NONE', #28169 ) ;
#18586=CARTESIAN_POINT ( 'NONE',  ( 7.757384923554904610, -52.20833333333332149, 27.17302655983835180 ) ) ;
#18590=CARTESIAN_POINT ( 'NONE',  ( 4.203733311638682579, -43.81747283271217697, 25.69410451607043555 ) ) ;
#18591=CARTESIAN_POINT ( 'NONE',  ( 5.195207097063835988, -43.85267090063073425, 32.69375250200204164 ) ) ;
#18592=CARTESIAN_POINT ( 'NONE',  ( 7.567941867304905479, -48.05312500047795510, 29.19375250200204164 ) ) ;
#18627=CARTESIAN_POINT ( 'NONE',  ( 5.912663395429907709, -48.05729166714461087, 26.32672608803957459 ) ) ;
#18641=CARTESIAN_POINT ( 'NONE',  ( 7.757384923554902834, -50.32229166657106134, 31.21447844416572792 ) ) ;
#18647=CARTESIAN_POINT ( 'NONE',  ( 2.507384923554909495, -46.11041666762257307, 32.22484141524756751 ) ) ;
#18654=CARTESIAN_POINT ( 'NONE',  ( 0.7716549171134656770, -46.70050188413667058, 28.86921795579420902 ) ) ;
#18667=CARTESIAN_POINT ( 'NONE',  ( 0.7573849235549129366, -51.99999999999999289, 29.19375250200204164 ) ) ;
#18690=EDGE_CURVE ( 'NONE', #26379, #14935, #175, .T. ) ;
#18699=CARTESIAN_POINT ( 'NONE',  ( 0.9468279798049125118, -42.80312500047794799, 29.19375250200204164 ) ) ;
#18720=CARTESIAN_POINT ( 'NONE',  ( 5.746188576823219485, -45.53326393658586824, 32.36492241908970158 ) ) ;
#18725=CARTESIAN_POINT ( 'NONE',  ( 1.017373798032094490, -45.72421344913539798, 27.86888731199303493 ) ) ;
#18732=CARTESIAN_POINT ( 'NONE',  ( 4.125083166729221595, -42.81560116176900976, 25.69589778585174145 ) ) ;
#18735=CARTESIAN_POINT ( 'NONE',  ( 5.912663395429904156, -43.72395833381127517, 32.06077891596451224 ) ) ;
#18736=CARTESIAN_POINT ( 'NONE',  ( 0.9468279798049134000, -44.34479166714461940, 27.28240155936039102 ) ) ;
#18744=CARTESIAN_POINT ( 'NONE',  ( 2.507384923554911715, -45.58333333333332149, 26.16266358875650866 ) ) ;
#18745=CARTESIAN_POINT ( 'NONE',  ( 5.912663395429904156, -46.22395833381128227, 32.06077891596451224 ) ) ;
#18751=FACE_OUTER_BOUND ( 'NONE', #23842, .T. ) ;
#18758=ORIENTED_EDGE ( 'NONE', *, *, #21287, .T. ) ;
#18782=CARTESIAN_POINT ( 'NONE',  ( 6.007384923554907274, -50.66666666666665719, 26.16266358875650866 ) ) ;
#18785=DIRECTION ( 'NONE',  ( 0.000000000000000000, 0.000000000000000000, -1.000000000000000000 ) ) ;
#18788=CARTESIAN_POINT ( 'NONE',  ( 4.357264200515069241, -50.32090047452125248, 25.69497413807381747 ) ) ;
#18791=CARTESIAN_POINT ( 'NONE',  ( 3.357395576508412915, -51.29743235121178913, 25.78163088665665015 ) ) ;
#18794=CARTESIAN_POINT ( 'NONE',  ( 7.757384923554902834, -51.79166666666665719, 31.21447844416572792 ) ) ;
#18800=CARTESIAN_POINT ( 'NONE',  ( 5.912663395429905044, -47.63645833381128369, 32.06077891596451224 ) ) ;
#18802=CARTESIAN_POINT ( 'NONE',  ( 0.7690692225104893698, -48.68771836623270133, 29.47952732091425787 ) ) ;
#18832=CARTESIAN_POINT ( 'NONE',  ( 7.567941867304904591, -48.09895833381128227, 27.28240155936039812 ) ) ;
#18833=PLANE ( 'NONE',  #55 ) ;
#18838=LINE ( 'NONE', #40751, #21876 ) ;
#18845=CARTESIAN_POINT ( 'NONE',  ( 6.007384923554907274, -50.19729166657106845, 26.16266358875650866 ) ) ;
#18851=CARTESIAN_POINT ( 'NONE',  ( 7.757384923554905498, -45.94375000095590877, 29.19375250200204164 ) ) ;
#18856=EDGE_CURVE ( 'NONE', #18063, #27686, #21791, .T. ) ;
#18857=CARTESIAN_POINT ( 'NONE',  ( 0.8005292408247836056, -46.70558112752276969, 28.64458517434834306 ) ) ;
#18867=CARTESIAN_POINT ( 'NONE',  ( 7.567941867304905479, -52.05312500047794799, 29.19375250200204164 ) ) ;
#18871=CARTESIAN_POINT ( 'NONE',  ( 2.507384923554909495, -51.91666666666665719, 32.22484141524756751 ) ) ;
#18879=DIRECTION ( 'NONE',  ( 0.000000000000000000, 0.000000000000000000, -1.000000000000000000 ) ) ;
#18884=CARTESIAN_POINT ( 'NONE',  ( 4.257384923554909051, -52.75000000000000000, 32.69375250200203453 ) ) ;
#18891=CARTESIAN_POINT ( 'NONE',  ( 5.946165192286296808, -48.02853971940316313, 32.25958641765839729 ) ) ;
#18899=ORIENTED_EDGE ( 'NONE', *, *, #8714, .F. ) ;
#18901=CARTESIAN_POINT ( 'NONE',  ( 5.912663395429907709, -42.46979166714461940, 26.32672608803957459 ) ) ;
#18925=CARTESIAN_POINT ( 'NONE',  ( 4.148861628609099128, -45.81637106524696179, 25.69375242907101153 ) ) ;
#18932=CARTESIAN_POINT ( 'NONE',  ( 2.975075972702347471, -42.40553116549648394, 32.45038937991203909 ) ) ;
#18933=ORIENTED_EDGE ( 'NONE', *, *, #13094, .T. ) ;
#18934=CARTESIAN_POINT ( 'NONE',  ( 4.264946699334307034, -49.31893003541803466, 25.69375851398777755 ) ) ;
#18938=CARTESIAN_POINT ( 'NONE',  ( 7.567941867304904591, -44.59895833381127517, 27.28240155936039812 ) ) ;
#18939=CARTESIAN_POINT ( 'NONE',  ( 2.602106451679909505, -44.71979166714461940, 32.06077891596451224 ) ) ;
#18951=CARTESIAN_POINT ( 'NONE',  ( 6.007384923554907274, -51.36041666762257307, 26.16266358875650866 ) ) ;
#18952=CARTESIAN_POINT ( 'NONE',  ( 2.602106451679909505, -44.80729166714461797, 32.06077891596451224 ) ) ;
#18953=ORIENTED_EDGE ( 'NONE', *, *, #2802, .T. ) ;
#18959=DIRECTION ( 'NONE',  ( -0.000000000000000000, -1.000000000000000000, -0.000000000000000000 ) ) ;
#18978=CARTESIAN_POINT ( 'NONE',  ( 4.257384923554909051, -52.75000000000000000, 29.19375250200204164 ) ) ;
#18987=DIRECTION ( 'NONE',  ( 0.000000000000000000, 0.000000000000000000, -1.000000000000000000 ) ) ;
#18988=CARTESIAN_POINT ( 'NONE',  ( 6.007384923554907274, -49.66666666666665719, 26.16266358875650866 ) ) ;
#18989=EDGE_LOOP ( 'NONE', ( #29726, #14028 ) ) ;
#18995=CARTESIAN_POINT ( 'NONE',  ( 2.602106451679912169, -51.97395833381127517, 26.32672608803957459 ) ) ;
#19001=CARTESIAN_POINT ( 'NONE',  ( 0.7573849235549129366, -50.99999999999999289, 29.19375250200204164 ) ) ;
#19005=CARTESIAN_POINT ( 'NONE',  ( 3.285047394825686418, -43.79544424032977901, 25.82256864068008539 ) ) ;
#19007=CARTESIAN_POINT ( 'NONE',  ( 7.567941867304904591, -48.09479166714461229, 31.10510344464368870 ) ) ;
#19043=CARTESIAN_POINT ( 'NONE',  ( 2.602106451679909505, -47.80729166714461087, 32.06077891596451224 ) ) ;
#19045=DIRECTION ( 'NONE',  ( 0.06269504844767277707, 0.000000000000000000, 0.9980327303751835855 ) ) ;
#19048=CARTESIAN_POINT ( 'NONE',  ( 5.912663395429907709, -49.96979166714461940, 26.32672608803957459 ) ) ;
#19054=CARTESIAN_POINT ( 'NONE',  ( 7.757384923554905498, -50.78062499990439704, 29.19375250200204164 ) ) ;
#19058=DIRECTION ( 'NONE',  ( 0.000000000000000000, 1.000000000000000000, 0.000000000000000000 ) ) ;
#19060=CARTESIAN_POINT ( 'NONE',  ( 7.757384923554905498, -45.44375000095590877, 29.19375250200204164 ) ) ;
#19085=CARTESIAN_POINT ( 'NONE',  ( 7.757384923554905498, -42.74999999999999289, 29.19375250200204164 ) ) ;
#19095=CARTESIAN_POINT ( 'NONE',  ( 2.602106451679911281, -46.88645833381128369, 26.32672608803957459 ) ) ;
#19098=CARTESIAN_POINT ( 'NONE',  ( 4.257384923554915268, -50.12499999999997868, 25.69375250200204519 ) ) ;
#19105=CARTESIAN_POINT ( 'NONE',  ( 6.996206350243394212, -47.88966090603650372, 27.00125865633196298 ) ) ;
#19113=ORIENTED_EDGE ( 'NONE', *, *, #19689, .F. ) ;
#19116=CARTESIAN_POINT ( 'NONE',  ( 4.630631976088899648, 7.250000000000000000, 35.13541431052434660 ) ) ;
#19118=B_SPLINE_CURVE_WITH_KNOTS ( 'NONE', 3,
 ( #3207, #9165, #31914, #2573, #12990, #28514, #38725, #32541, #28931, #38299, #212, #41503, #35111, #41928, #13193, #15766, #12355, #26181, #35533, #22972, #20371, #12776 ),
 .UNSPECIFIED., .F., .F.,
 ( 4, 2, 2, 2, 2, 2, 2, 2, 2, 2, 4 ),
 ( 0.4871832794823670043, 0.4892682418778427356, 0.4913532042733184668, 0.4934381666687941981, 0.4955231290642699293, 0.4996930538552213918, 0.5038629786461727988, 0.5080329034371242614, 0.5122028282280757239, 0.5163727530190271864, 0.5205426778099786489 ),
 .UNSPECIFIED. ) ;
#19122=ORIENTED_EDGE ( 'NONE', *, *, #35809, .T. ) ;
#19141=CARTESIAN_POINT ( 'NONE',  ( 1.059967215642415805, -45.72644936159947093, 27.76916137949113761 ) ) ;
#19150=CARTESIAN_POINT ( 'NONE',  ( 4.257384923554909051, -44.51562500047793947, 25.37105061671875461 ) ) ;
#19151=CARTESIAN_POINT ( 'NONE',  ( 5.912663395429907709, -45.46979166714461229, 26.32672608803957459 ) ) ;
#19154=VECTOR ( 'NONE', #19307, 1000.000000000000000 ) ;
#19161=CARTESIAN_POINT ( 'NONE',  ( 7.567941867304902814, -45.18229166714461797, 31.10510344464368870 ) ) ;
#19164=VECTOR ( 'NONE', #33524, 1000.000000000000000 ) ;
#19195=CARTESIAN_POINT ( 'NONE',  ( 5.173501322207794573, -47.54716186659237565, 32.60265708822004171 ) ) ;
#19196=CARTESIAN_POINT ( 'NONE',  ( 4.257384971216501057, -47.81875000207092086, 25.69375250200204519 ) ) ;
#19197=CARTESIAN_POINT ( 'NONE',  ( 6.007384923554907274, -48.66666666666665719, 26.16266358875650866 ) ) ;
#19202=CARTESIAN_POINT ( 'NONE',  ( 4.257384923554909051, -51.12499999999999289, 25.69375250200204519 ) ) ;
#19204=CARTESIAN_POINT ( 'NONE',  ( 5.912663395429907709, -52.05729166714461797, 26.32672608803957459 ) ) ;
#19212=CARTESIAN_POINT ( 'NONE',  ( 0.7573849235549138248, -51.04166666666665719, 27.17302655983835180 ) ) ;
#19216=ORIENTED_EDGE ( 'NONE', *, *, #24296, .T. ) ;
#19219=CARTESIAN_POINT ( 'NONE',  ( 5.912663395429907709, -47.46979166714461229, 26.32672608803957459 ) ) ;
#19229=CYLINDRICAL_SURFACE ( 'NONE', #6860, 3.499999999999996003 ) ;
#19251=VERTEX_POINT ( 'NONE', #25624 ) ;
#19253=CARTESIAN_POINT ( 'NONE',  ( 7.567941867304904591, -47.09895833381128938, 27.28240155936039812 ) ) ;
#19258=CARTESIAN_POINT ( 'NONE',  ( 5.912663395429907709, -49.46979166714461940, 26.32672608803957459 ) ) ;
#19263=CARTESIAN_POINT ( 'NONE',  ( 7.757384923554905498, -48.28062499990439704, 29.19375250200204164 ) ) ;
#19265=ORIENTED_EDGE ( 'NONE', *, *, #985, .T. ) ;
#19269=CARTESIAN_POINT ( 'NONE',  ( 2.507384923554909495, -47.11041666762257307, 32.22484141524756751 ) ) ;
#19284=CARTESIAN_POINT ( 'NONE',  ( 9.216391464164017222, 3.250000000000000444, 25.89968016835878828 ) ) ;
#19297=CARTESIAN_POINT ( 'NONE',  ( 9.589638516698011372, 3.250000000000000444, 31.84134197688108614 ) ) ;
#19303=CARTESIAN_POINT ( 'NONE',  ( 0.7690633520481234831, -46.18771991487935935, 29.47945565263848877 ) ) ;
#19304=CARTESIAN_POINT ( 'NONE',  ( 7.567941867304905479, -45.05312500047794799, 29.19375250200204164 ) ) ;
#19307=DIRECTION ( 'NONE',  ( -0.000000000000000000, -1.000000000000000000, -0.000000000000000000 ) ) ;
#19312=CARTESIAN_POINT ( 'NONE',  ( 7.781342189264628395, -47.93513637306280373, 28.74637256839532284 ) ) ;
#19320=CARTESIAN_POINT ( 'NONE',  ( 3.011430212699131026, -50.59841665820681555, 32.46463687355288386 ) ) ;
#19356=CONICAL_SURFACE ( 'NONE', #39732, 2.999999999999988898, 0.7853981633974482790 ) ;
#19358=CARTESIAN_POINT ( 'NONE',  ( 5.912663395429907709, -42.55729166714461087, 26.32672608803957459 ) ) ;
#19359=CARTESIAN_POINT ( 'NONE',  ( 5.912663395429907709, -45.96979166714461229, 26.32672608803957459 ) ) ;
#19370=CARTESIAN_POINT ( 'NONE',  ( 0.9468279798049143992, -45.43229166714461797, 27.28240155936039457 ) ) ;
#19395=CARTESIAN_POINT ( 'NONE',  ( 2.992427724609936224, -42.37818741561596170, 32.40632171968005082 ) ) ;
#19401=CARTESIAN_POINT ( 'NONE',  ( 0.9468279798049125118, -50.80312500047794799, 29.19375250200204164 ) ) ;
#19402=CARTESIAN_POINT ( 'NONE',  ( 3.728822002920322287, -47.30679459398075437, 25.73137163227809054 ) ) ;
#19405=CARTESIAN_POINT ( 'NONE',  ( 0.7573849235549138248, -48.54166666666665719, 27.17302655983835180 ) ) ;
#19410=CARTESIAN_POINT ( 'NONE',  ( 6.767324126933612405, -43.50765372690876376, 31.67136402418985242 ) ) ;
#19411=CARTESIAN_POINT ( 'NONE',  ( 0.9468279798049124008, -51.84895833381127517, 31.10510344464368515 ) ) ;
#19420=CARTESIAN_POINT ( 'NONE',  ( 7.757384923554905498, -49.74999999999998579, 29.19375250200204164 ) ) ;
#19424=CARTESIAN_POINT ( 'NONE',  ( -0.7016216170541935693, 3.250000000000000444, 32.48782483564529855 ) ) ;
#19425=AXIS2_PLACEMENT_3D ( 'NONE', #36752, #30575, #4425 ) ;
#19443=CARTESIAN_POINT ( 'NONE',  ( 1.171936686702267805, -44.15292240405341317, 30.93675069184469706 ) ) ;
#19461=CARTESIAN_POINT ( 'NONE',  ( 7.567941867304902814, -46.68229166714461087, 31.10510344464368870 ) ) ;
#19466=CARTESIAN_POINT ( 'NONE',  ( 2.602106451679909505, -49.71979166714461940, 32.06077891596451224 ) ) ;
#19473=CARTESIAN_POINT ( 'NONE',  ( 7.757384923554902834, -48.32229166657106134, 31.21447844416572792 ) ) ;
#19479=CARTESIAN_POINT ( 'NONE',  ( 2.507384923554911715, -43.77708333428924448, 26.16266358875650866 ) ) ;
#19482=CARTESIAN_POINT ( 'NONE',  ( 0.7573849235549138248, -43.04166666666666430, 27.17302655983835180 ) ) ;
#19497=CARTESIAN_POINT ( 'NONE',  ( 4.257384923554909051, -52.75000000000000000, 29.19375250200204164 ) ) ;
#19510=VERTEX_POINT ( 'NONE', #12794 ) ;
#19512=CARTESIAN_POINT ( 'NONE',  ( 7.567941867304905479, -47.05312500047795510, 29.19375250200204164 ) ) ;
#19520=CARTESIAN_POINT ( 'NONE',  ( 4.865387480305788159, -51.83322625228183966, 25.69375250200204874 ) ) ;
#19530=CARTESIAN_POINT ( 'NONE',  ( 1.980572215027825322, -50.76375655303291978, 26.50649014946537463 ) ) ;
#19540=CYLINDRICAL_SURFACE ( 'NONE', #31528, 5.499999999999994671 ) ;
#19570=CARTESIAN_POINT ( 'NONE',  ( 0.9468279798049124008, -44.34895833381127517, 31.10510344464368515 ) ) ;
#19572=DIRECTION ( 'NONE',  ( -0.000000000000000000, -1.000000000000000000, -0.000000000000000000 ) ) ;
#19597=CARTESIAN_POINT ( 'NONE',  ( 4.257384923554909051, -49.92812500047795510, 25.37105061671875461 ) ) ;
#19598=CARTESIAN_POINT ( 'NONE',  ( 4.249084420889739810, -47.31856287306275988, 25.69375986671302670 ) ) ;
#19601=CARTESIAN_POINT ( 'NONE',  ( 2.507384923554909495, -45.91666666666666430, 32.22484141524756751 ) ) ;
#19609=CARTESIAN_POINT ( 'NONE',  ( 2.602106451679912169, -47.97395833381128227, 26.32672608803957459 ) ) ;
#19614=DIRECTION ( 'NONE',  ( 0.8329741740894176516, 0.000000000000000000, -0.5533118698347727626 ) ) ;
#19617=CARTESIAN_POINT ( 'NONE',  ( 7.757384923554905498, -51.24999999999999289, 29.19375250200204164 ) ) ;
#19624=CARTESIAN_POINT ( 'NONE',  ( 4.252382527332392748, -48.81863089642496334, 25.69375241780392471 ) ) ;
#19628=CARTESIAN_POINT ( 'NONE',  ( 2.507384923554909495, -51.61041666762257307, 32.22484141524756751 ) ) ;
#19659=CARTESIAN_POINT ( 'NONE',  ( 7.567941867304904591, -45.64062500047794657, 29.19375250200204164 ) ) ;
#19663=CARTESIAN_POINT ( 'NONE',  ( 5.912663395429905044, -50.63645833381128369, 32.06077891596451224 ) ) ;
#19670=CARTESIAN_POINT ( 'NONE',  ( 2.507384923554911715, -47.61395833323773275, 26.16266358875650866 ) ) ;
#19678=CARTESIAN_POINT ( 'NONE',  ( 0.7573849235549138248, -44.73541666762258018, 27.17302655983835180 ) ) ;
#19689=EDGE_CURVE ( 'NONE', #16189, #5047, #33632, .T. ) ;
#19701=DIRECTION ( 'NONE',  ( 0.000000000000000000, 0.000000000000000000, -1.000000000000000000 ) ) ;
#19702=FACE_OUTER_BOUND ( 'NONE', #39880, .T. ) ;
#19708=CARTESIAN_POINT ( 'NONE',  ( 4.257384923554909051, -52.75000000000000000, 29.19375250200204164 ) ) ;
#19719=CARTESIAN_POINT ( 'NONE',  ( 0.9468279798049134000, -46.34479166714461229, 27.28240155936039457 ) ) ;
#19736=CARTESIAN_POINT ( 'NONE',  ( 4.257369266595627977, -50.56937335658698629, 32.69375250193562721 ) ) ;
#19737=CARTESIAN_POINT ( 'NONE',  ( 4.257384923554909051, -51.81875000095590877, 25.15230061767466552 ) ) ;
#19752=CARTESIAN_POINT ( 'NONE',  ( 7.757384923554904610, -52.20833333333332149, 27.17302655983835180 ) ) ;
#19761=CARTESIAN_POINT ( 'NONE',  ( 7.757384923554902834, -47.29166666666665719, 31.21447844416572792 ) ) ;
#19782=CARTESIAN_POINT ( 'NONE',  ( 4.257384923554909051, 7.250000000000000000, 37.35503210563722831 ) ) ;
#19807=CARTESIAN_POINT ( 'NONE',  ( 5.195207097063835988, -44.35267090063073425, 32.69375250200204164 ) ) ;
#19810=CARTESIAN_POINT ( 'NONE',  ( 2.602106451679911281, -50.88645833381127659, 26.32672608803957459 ) ) ;
#19811=CARTESIAN_POINT ( 'NONE',  ( 4.257403086791381241, -47.31875042192206848, 25.69375250204917194 ) ) ;
#19814=CARTESIAN_POINT ( 'NONE',  ( 4.257384923554909051, -47.62499999999999289, 25.15230061767466552 ) ) ;
#19820=CARTESIAN_POINT ( 'NONE',  ( 5.713749997039577089, -43.53685368173783132, 32.40016375215834188 ) ) ;
#19821=CARTESIAN_POINT ( 'NONE',  ( 0.9468279798049132889, -49.39062500047794657, 29.19375250200204164 ) ) ;
#19826=AXIS2_PLACEMENT_3D ( 'NONE', #15020, #40964, #24193 ) ;
#19828=CARTESIAN_POINT ( 'NONE',  ( 0.7573849235549138248, -49.04166666666665009, 27.17302655983835180 ) ) ;
#19839=CIRCLE ( 'NONE', #5615, 3.499999999999996003 ) ;
#19840=CARTESIAN_POINT ( 'NONE',  ( 2.507384923554909495, -48.61041666762257307, 32.22484141524756751 ) ) ;
#19848=EDGE_CURVE ( 'NONE', #41285, #10374, #34967, .T. ) ;
#19869=CARTESIAN_POINT ( 'NONE',  ( 0.9468279798049124008, -45.84895833381127517, 31.10510344464368515 ) ) ;
#19875=CARTESIAN_POINT ( 'NONE',  ( 7.567941867304905479, -50.51145833381129080, 27.28240155936039457 ) ) ;
#19883=CARTESIAN_POINT ( 'NONE',  ( 6.007384923554907274, -47.19729166657106134, 26.16266358875650866 ) ) ;
#19891=ADVANCED_FACE ( 'NONE', ( #18083 ), #34450, .T. ) ;
#19892=CARTESIAN_POINT ( 'NONE',  ( 7.757384923554905498, -44.94375000095590877, 29.19375250200204164 ) ) ;
#19893=CARTESIAN_POINT ( 'NONE',  ( 0.7573849235549120484, -44.15208333428923737, 31.21447844416572792 ) ) ;
#19932=CARTESIAN_POINT ( 'NONE',  ( 0.9468279798049115126, -42.26145833381129080, 31.10510344464368515 ) ) ;
#19941=CARTESIAN_POINT ( 'NONE',  ( 1.450703344183503551, -42.40326249313397966, 31.30385622266625845 ) ) ;
#19948=ADVANCED_FACE ( 'NONE', ( #8089 ), #21891, .F. ) ;
#19952=CARTESIAN_POINT ( 'NONE',  ( 3.585388404569898491, -50.80385627191245135, 25.75644694802884871 ) ) ;
#19953=EDGE_CURVE ( 'NONE', #21757, #40028, #5311, .T. ) ;
#19954=CARTESIAN_POINT ( 'NONE',  ( 7.757384923554902834, -43.29166666666666430, 31.21447844416572792 ) ) ;
#19975=ADVANCED_FACE ( 'NONE', ( #21066 ), #14888, .T. ) ;
#19994=CARTESIAN_POINT ( 'NONE',  ( 4.257384923554908163, -43.17812500047794799, 33.01645438728532866 ) ) ;
#20000=CARTESIAN_POINT ( 'NONE',  ( 2.602106451679911281, -48.88645833381128369, 26.32672608803957459 ) ) ;
#20005=CARTESIAN_POINT ( 'NONE',  ( 4.707824882563185653, -45.82862408102098328, 25.69375280470764622 ) ) ;
#20019=CARTESIAN_POINT ( 'NONE',  ( 4.257384923554909051, -48.62499999999998579, 25.69375250200204519 ) ) ;
#20035=CARTESIAN_POINT ( 'NONE',  ( 4.257384923554909051, -46.62499999999999289, 25.15230061767466552 ) ) ;
#20043=CARTESIAN_POINT ( 'NONE',  ( 7.567941867304904591, -48.64062500047794657, 29.19375250200204164 ) ) ;
#20050=CARTESIAN_POINT ( 'NONE',  ( 2.507384923554909495, -47.91666666666665719, 32.22484141524756751 ) ) ;
#20051=CARTESIAN_POINT ( 'NONE',  ( 5.912663395429907709, -51.05729166714461797, 26.32672608803957459 ) ) ;
#20054=AXIS2_PLACEMENT_3D ( 'NONE', #40094, #29889, #4576 ) ;
#20060=CARTESIAN_POINT ( 'NONE',  ( 2.507384923554911715, -50.77708333428923737, 26.16266358875650866 ) ) ;
#20061=CARTESIAN_POINT ( 'NONE',  ( 4.257384923554909051, -52.75000000000000000, 23.69375250200204519 ) ) ;
#20062=( GEOMETRIC_REPRESENTATION_CONTEXT ( 3 ) GLOBAL_UNCERTAINTY_ASSIGNED_CONTEXT ( ( #23318 ) ) GLOBAL_UNIT_ASSIGNED_CONTEXT ( ( #8968, #34293, #24313 ) ) REPRESENTATION_CONTEXT ( 'NONE', 'WORKASPACE' ) );
#20076=CARTESIAN_POINT ( 'NONE',  ( 4.257384923554909051, -42.31875000095590167, 25.15230061767466552 ) ) ;
#20081=FACE_OUTER_BOUND ( 'NONE', #5380, .T. ) ;
#20085=ORIENTED_EDGE ( 'NONE', *, *, #24934, .T. ) ;
#20087=CARTESIAN_POINT ( 'NONE',  ( 0.9468279798049143992, -45.43229166714461797, 27.28240155936039812 ) ) ;
#20091=CARTESIAN_POINT ( 'NONE',  ( 4.257384923554909051, -46.92812500047795510, 25.37105061671875106 ) ) ;
#20094=ORIENTED_EDGE ( 'NONE', *, *, #24946, .T. ) ;
#20098=CARTESIAN_POINT ( 'NONE',  ( 0.7573849235549138248, -49.07229166657106134, 27.17302655983835180 ) ) ;
#20104=CARTESIAN_POINT ( 'NONE',  ( 0.7573849235549129366, -43.69375000095590877, 29.19375250200204164 ) ) ;
#20105=CARTESIAN_POINT ( 'NONE',  ( 4.257384923554908163, -44.06875000095590877, 33.23520438632941421 ) ) ;
#20124=CARTESIAN_POINT ( 'NONE',  ( 7.757384923554905498, -48.24999999999998579, 29.19375250200204164 ) ) ;
#20133=B_SPLINE_CURVE_WITH_KNOTS ( 'NONE', 3,
 ( #29399, #268, #16655, #39183, #22399, #13250, #35376, #15830, #41769, #10268, #23025, #7075, #10063, #13041, #28774, #26022, #36202, #41981, #38986, #16043, #35994, #22822 ),
 .UNSPECIFIED., .F., .F.,
 ( 4, 2, 2, 2, 2, 2, 2, 2, 2, 2, 4 ),
 ( 0.5414319103264134680, 0.5433003748494472651, 0.5451688393724810622, 0.5470373038955149703, 0.5489057684185487673, 0.5526426974646163615, 0.5563796265106840666, 0.5601165555567516607, 0.5638534846028193659, 0.5675904136488869600, 0.5713273426949546652 ),
 .UNSPECIFIED. ) ;
#20146=CARTESIAN_POINT ( 'NONE',  ( 5.912663395429905044, -42.63645833381128369, 32.06077891596451224 ) ) ;
#20152=( BOUNDED_CURVE ( )  B_SPLINE_CURVE ( 2, ( #9530, #15497, #12288, #8892, #22490, #32485, #2509, #28871, #38872 ),
 .UNSPECIFIED., .F., .F. ) 
 B_SPLINE_CURVE_WITH_KNOTS ( ( 3, 2, 2, 2, 3 ),
 ( 0.3375000000000000222, 0.3416666666666666741, 0.3499999999999999778, 0.3583333333333333370, 0.3624999999999999889 ),
 .UNSPECIFIED. ) 
 CURVE ( )  GEOMETRIC_REPRESENTATION_ITEM ( )  RATIONAL_B_SPLINE_CURVE ( ( 0.9330127018922194093, 0.9330127018922198534, 1.000000000000000000, 0.8660254037844387076, 1.000000000000000000, 0.8660254037844387076, 1.000000000000000000, 0.9330127018922194093, 0.9330127018922194093 ) ) 
 REPRESENTATION_ITEM ( '' )  );
#20156=CARTESIAN_POINT ( 'NONE',  ( 1.286798421057948616, -42.40378032087074445, 31.06650128501637909 ) ) ;
#20157=ORIENTED_EDGE ( 'NONE', *, *, #18690, .F. ) ;
#20160=CARTESIAN_POINT ( 'NONE',  ( 4.201982084410235352, -44.31743184351945075, 25.69412726318273243 ) ) ;
#20166=CARTESIAN_POINT ( 'NONE',  ( 2.329384073493019791, -50.77368622224567218, 26.23421896831290567 ) ) ;
#20168=CARTESIAN_POINT ( 'NONE',  ( 2.507384923554911715, -51.77708333428923737, 26.16266358875650866 ) ) ;
#20194=CARTESIAN_POINT ( 'NONE',  ( 5.195207097063847534, -47.14732909936924443, 25.69375250200204874 ) ) ;
#20211=CARTESIAN_POINT ( 'NONE',  ( 5.912663395429907709, -44.96979166714461940, 26.32672608803957459 ) ) ;
#20217=CARTESIAN_POINT ( 'NONE',  ( 6.152631310697794120, -46.02215077734707194, 32.17048479926999249 ) ) ;
#20240=CARTESIAN_POINT ( 'NONE',  ( 6.007384923554904610, -44.33333333333332149, 32.22484141524757462 ) ) ;
#20243=CARTESIAN_POINT ( 'NONE',  ( 2.602106451679911281, -51.88645833381128369, 26.32672608803957459 ) ) ;
#20246=CARTESIAN_POINT ( 'NONE',  ( 2.507384923554909495, -47.41666666666665719, 32.22484141524756751 ) ) ;
#20247=ORIENTED_EDGE ( 'NONE', *, *, #38528, .F. ) ;
#20252=CARTESIAN_POINT ( 'NONE',  ( 4.257384923554909051, -49.51562500047794657, 25.37105061671875461 ) ) ;
#20255=VERTEX_POINT ( 'NONE', #41634 ) ;
#20258=CARTESIAN_POINT ( 'NONE',  ( 0.7573849235549138248, -48.54166666666665719, 27.17302655983835180 ) ) ;
#20259=CARTESIAN_POINT ( 'NONE',  ( 4.257384923554909051, -52.01562500047794657, 25.37105061671875106 ) ) ;
#20262=CARTESIAN_POINT ( 'NONE',  ( 1.842423516487604163, -43.12841693280324051, 31.73315976314671616 ) ) ;
#20268=CARTESIAN_POINT ( 'NONE',  ( 6.007384923554907274, -49.86041666762257307, 26.16266358875650866 ) ) ;
#20279=CARTESIAN_POINT ( 'NONE',  ( 5.173518856654212072, -44.83941489987380891, 25.78485262926021093 ) ) ;
#20282=CARTESIAN_POINT ( 'NONE',  ( 1.014225569120269954, -44.72696841158080616, 27.79397663064076340 ) ) ;
#20299=CARTESIAN_POINT ( 'NONE',  ( 7.567941867304905479, -46.51145833381128369, 27.28240155936039457 ) ) ;
#20305=CARTESIAN_POINT ( 'NONE',  ( 0.7573849235549120484, -44.48895833323773275, 31.21447844416572792 ) ) ;
#20313=CARTESIAN_POINT ( 'NONE',  ( 7.757384923554904610, -43.40208333428924448, 27.17302655983835180 ) ) ;
#20329=CARTESIAN_POINT ( 'NONE',  ( 4.323710921731753309, -51.32032883149125979, 25.69429138085894948 ) ) ;
#20352=CARTESIAN_POINT ( 'NONE',  ( 2.602106451679911281, -44.38645833381128369, 26.32672608803957459 ) ) ;
#20355=CARTESIAN_POINT ( 'NONE',  ( 4.257373630597665937, -44.06920056960389331, 32.69375250196740978 ) ) ;
#20358=CARTESIAN_POINT ( 'NONE',  ( 4.257387320252103535, -45.81875005579910720, 25.69375250200286587 ) ) ;
#20360=CARTESIAN_POINT ( 'NONE',  ( 5.221907364133830498, -47.84002526000101341, 25.79487257707605607 ) ) ;
#20362=CARTESIAN_POINT ( 'NONE',  ( 1.022478885060276843, -42.40471323084106103, 30.56011815409148369 ) ) ;
#20371=CARTESIAN_POINT ( 'NONE',  ( 4.440365877136021489, -46.82310667953520777, 25.69375541740710389 ) ) ;
#20373=CARTESIAN_POINT ( 'NONE',  ( 6.007384923554904610, -43.33333333333332149, 32.22484141524757462 ) ) ;
#20374=CARTESIAN_POINT ( 'NONE',  ( 5.912663395429907709, -42.55729166714461087, 26.32672608803957459 ) ) ;
#20395=EDGE_CURVE ( 'NONE', #29977, #36911, #14374, .T. ) ;
#20404=CARTESIAN_POINT ( 'NONE',  ( 4.257384923554909051, -52.75000000000000000, 25.69375250200204519 ) ) ;
#20418=CARTESIAN_POINT ( 'NONE',  ( 4.257384923554909051, -43.42812500047794799, 25.37105061671875106 ) ) ;
#20425=CARTESIAN_POINT ( 'NONE',  ( 2.602106451679911281, -45.88645833381128369, 26.32672608803957459 ) ) ;
#20440=CARTESIAN_POINT ( 'NONE',  ( 4.257384923554909051, -52.75000000000000000, 29.19375250200204164 ) ) ;
#20446=AXIS2_PLACEMENT_3D ( 'NONE', #29892, #23092, #13736 ) ;
#20456=CARTESIAN_POINT ( 'NONE',  ( 0.9468279798049134000, -47.34479166714461940, 27.28240155936039457 ) ) ;
#20460=CARTESIAN_POINT ( 'NONE',  ( 7.757384923554904610, -46.70833333333332149, 27.17302655983835180 ) ) ;
#20463=CARTESIAN_POINT ( 'NONE',  ( 3.727113663785146080, -49.30620146789480884, 25.72087592056918126 ) ) ;
#20468=CARTESIAN_POINT ( 'NONE',  ( 7.567941867304902814, -50.18229166714461797, 31.10510344464368870 ) ) ;
#20475=CARTESIAN_POINT ( 'NONE',  ( 7.757384923554902834, -48.29166666666665009, 31.21447844416572792 ) ) ;
#20476=CARTESIAN_POINT ( 'NONE',  ( 4.257384923554909051, -50.01562500047794657, 25.37105061671875106 ) ) ;
#20481=CARTESIAN_POINT ( 'NONE',  ( 0.7573849235549120484, -43.45833333333332149, 31.21447844416572792 ) ) ;
#20487=CARTESIAN_POINT ( 'NONE',  ( 7.757384923554904610, -49.40208333428924448, 27.17302655983835180 ) ) ;
#20507=ORIENTED_EDGE ( 'NONE', *, *, #9575, .T. ) ;
#20512=CARTESIAN_POINT ( 'NONE',  ( 4.257384923554908163, -44.76562500047793947, 33.01645438728532866 ) ) ;
#20520=CARTESIAN_POINT ( 'NONE',  ( 6.007384923554907274, -46.69729166657106134, 26.16266358875650866 ) ) ;
#20529=CARTESIAN_POINT ( 'NONE',  ( 6.007384923554907274, -42.86041666762257307, 26.16266358875650866 ) ) ;
#20534=DIRECTION ( 'NONE',  ( -0.000000000000000000, -1.000000000000000000, -0.000000000000000000 ) ) ;
#20548=LINE ( 'NONE', #7792, #19164 ) ;
#20550=ADVANCED_FACE ( 'NONE', ( #19702 ), #5529, .T. ) ;
#20555=CARTESIAN_POINT ( 'NONE',  ( 7.400097147136390774, -50.90772945599078270, 27.65290599698193219 ) ) ;
#20566=CARTESIAN_POINT ( 'NONE',  ( 7.567941867304904591, -43.09479166714462650, 31.10510344464368870 ) ) ;
#20567=CARTESIAN_POINT ( 'NONE',  ( 3.319562750045979005, -48.39732909936924443, 32.69375250200202743 ) ) ;
#20574=CARTESIAN_POINT ( 'NONE',  ( 1.825953643544445670, -42.40272209678187920, 31.72715754867942195 ) ) ;
#20579=CARTESIAN_POINT ( 'NONE',  ( 4.255660974076588943, -44.31870884124778343, 25.69375246902105658 ) ) ;
#20580=CARTESIAN_POINT ( 'NONE',  ( 3.339764640347642644, -50.08837478974248825, 32.60235388936703771 ) ) ;
#20587=CARTESIAN_POINT ( 'NONE',  ( 0.7573849235549138248, -49.23541666762258018, 27.17302655983835180 ) ) ;
#20590=ORIENTED_EDGE ( 'NONE', *, *, #22474, .T. ) ;
#20606=CARTESIAN_POINT ( 'NONE',  ( 6.957267128835243675, -42.88870693365972642, 26.95208760938039561 ) ) ;
#20611=CARTESIAN_POINT ( 'NONE',  ( 2.503696200896709190, -47.77814708276503808, 26.13072067749811467 ) ) ;
#20626=CARTESIAN_POINT ( 'NONE',  ( 4.257384923554909051, -52.75000000000000000, 25.69375250200204519 ) ) ;
#20630=DIRECTION ( 'NONE',  ( 0.000000000000000000, 0.000000000000000000, -1.000000000000000000 ) ) ;
#20633=VERTEX_POINT ( 'NONE', #35453 ) ;
#20636=CARTESIAN_POINT ( 'NONE',  ( 2.602106451679909505, -46.21979166714461229, 32.06077891596451224 ) ) ;
#20641=CARTESIAN_POINT ( 'NONE',  ( 0.7573849235549129366, -51.49999999999999289, 29.19375250200204164 ) ) ;
#20652=CARTESIAN_POINT ( 'NONE',  ( 0.8628958791522070015, -46.17477097081946624, 30.06357964096892843 ) ) ;
#20668=CARTESIAN_POINT ( 'NONE',  ( 0.9468279798049134000, -49.84479166714461940, 27.28240155936039457 ) ) ;
#20673=CARTESIAN_POINT ( 'NONE',  ( 0.7573849235549138248, -45.04166666666665719, 27.17302655983835180 ) ) ;
#20681=CARTESIAN_POINT ( 'NONE',  ( 2.602106451679909505, -47.30729166714461087, 32.06077891596451224 ) ) ;
#20687=CARTESIAN_POINT ( 'NONE',  ( 6.007384923554904610, -48.83333333333332860, 32.22484141524757462 ) ) ;
#20688=CARTESIAN_POINT ( 'NONE',  ( 5.912663395429907709, -50.05729166714461087, 26.32672608803957459 ) ) ;
#20691=CARTESIAN_POINT ( 'NONE',  ( 2.777484378203061599, -43.28534887756380556, 25.99699512701728210 ) ) ;
#20698=CARTESIAN_POINT ( 'NONE',  ( 2.507384923554909495, -50.61041666762257307, 32.22484141524756751 ) ) ;
#20701=VECTOR ( 'NONE', #40787, 1000.000000000000000 ) ;
#20710=CARTESIAN_POINT ( 'NONE',  ( 4.715533426023096553, -45.05760075599271630, 32.69375245563277588 ) ) ;
#20729=CARTESIAN_POINT ( 'NONE',  ( 2.815360438258434961, -42.30192363818449763, 32.18390116252139421 ) ) ;
#20734=VECTOR ( 'NONE', #8198, 1000.000000000000000 ) ;
#20738=CARTESIAN_POINT ( 'NONE',  ( 7.757384923554902834, -44.82229166657106845, 31.21447844416572792 ) ) ;
#20744=CARTESIAN_POINT ( 'NONE',  ( 2.507384923554911715, -44.27708333428923737, 26.16266358875650866 ) ) ;
#20747=CARTESIAN_POINT ( 'NONE',  ( 7.757384923554904610, -51.70833333333332149, 27.17302655983835180 ) ) ;
#20751=DIRECTION ( 'NONE',  ( -0.000000000000000000, -1.000000000000000000, -0.000000000000000000 ) ) ;
#20781=ORIENTED_EDGE ( 'NONE', *, *, #10621, .F. ) ;
#20784=CARTESIAN_POINT ( 'NONE',  ( 7.567941867304905479, -44.01145833381129080, 27.28240155936039812 ) ) ;
#20786=CARTESIAN_POINT ( 'NONE',  ( 7.757384923554904610, -47.70833333333332149, 27.17302655983835180 ) ) ;
#20792=CARTESIAN_POINT ( 'NONE',  ( 4.876775967520497801, -48.55400260143029811, 32.63851390996926227 ) ) ;
#20796=CARTESIAN_POINT ( 'NONE',  ( 3.886275563318128068, -50.31076639127566352, 25.69375385968415060 ) ) ;
#20799=ORIENTED_EDGE ( 'NONE', *, *, #7756, .T. ) ;
#20800=CARTESIAN_POINT ( 'NONE',  ( 0.7573849235549120484, -50.15208333428924448, 31.21447844416572792 ) ) ;
#20801=CARTESIAN_POINT ( 'NONE',  ( 5.912663395429907709, -43.55729166714461797, 26.32672608803957459 ) ) ;
#20802=ORIENTED_EDGE ( 'NONE', *, *, #41390, .F. ) ;
#20803=CYLINDRICAL_SURFACE ( 'NONE', #19425, 3.499999999999996003 ) ;
#20808=DIRECTION ( 'NONE',  ( -0.000000000000000000, -1.000000000000000000, -0.000000000000000000 ) ) ;
#20822=CARTESIAN_POINT ( 'NONE',  ( 7.442844854557231216, -42.97906090903023824, 30.75254660746963964 ) ) ;
#20840=EDGE_LOOP ( 'NONE', ( #35639, #13091, #3216, #30510 ) ) ;
#20842=ORIENTED_EDGE ( 'NONE', *, *, #40415, .T. ) ;
#20845=CARTESIAN_POINT ( 'NONE',  ( 7.567941867304904591, -46.09479166714460519, 31.10510344464368870 ) ) ;
#20875=CARTESIAN_POINT ( 'NONE',  ( 5.912663395429907709, -47.96979166714461229, 26.32672608803957459 ) ) ;
#20879=CARTESIAN_POINT ( 'NONE',  ( 2.507384923554909495, -45.41666666666665719, 32.22484141524756751 ) ) ;
#20884=ORIENTED_EDGE ( 'NONE', *, *, #26968, .F. ) ;
#20885=CARTESIAN_POINT ( 'NONE',  ( 7.567941867304902814, -47.68229166714461087, 31.10510344464368870 ) ) ;
#20891=CARTESIAN_POINT ( 'NONE',  ( 6.007384923554907274, -47.16666666666665719, 26.16266358875650866 ) ) ;
#20892=CARTESIAN_POINT ( 'NONE',  ( 2.602106451679909505, -50.80729166714461797, 32.06077891596451224 ) ) ;
#20895=CARTESIAN_POINT ( 'NONE',  ( 1.573496034473122585, -43.13771241576273496, 31.44024898601555051 ) ) ;
#20903=CARTESIAN_POINT ( 'NONE',  ( 7.757384923554904610, -45.90208333428923737, 27.17302655983835180 ) ) ;
#20912=CARTESIAN_POINT ( 'NONE',  ( 7.056215660211524465, -44.99504149609628456, 31.34467003488949999 ) ) ;
#20918=CARTESIAN_POINT ( 'NONE',  ( 2.499829923005070231, -49.60956730763210487, 32.25472987908130307 ) ) ;
#20926=EDGE_CURVE ( 'NONE', #38450, #37054, #20548, .T. ) ;
#20932=CARTESIAN_POINT ( 'NONE',  ( 4.257384923554908163, -43.76562500047794657, 33.01645438728532866 ) ) ;
#20936=CARTESIAN_POINT ( 'NONE',  ( 6.745702299779453348, -44.50793711663224883, 31.67519439456402353 ) ) ;
#20939=CARTESIAN_POINT ( 'NONE',  ( 7.757384923554904610, -44.73895833323773985, 27.17302655983835180 ) ) ;
#20946=CARTESIAN_POINT ( 'NONE',  ( 7.757384923554902834, -42.48541666762258018, 31.21447844416572792 ) ) ;
#20948=ORIENTED_EDGE ( 'NONE', *, *, #13265, .F. ) ;
#20966=CARTESIAN_POINT ( 'NONE',  ( 0.7573849235549120484, -46.45833333333332149, 31.21447844416572792 ) ) ;
#20980=CARTESIAN_POINT ( 'NONE',  ( 4.257384923554908163, -50.76562500047794657, 33.01645438728532866 ) ) ;
#20989=DIRECTION ( 'NONE',  ( -0.8329741740894178736, 0.000000000000000000, 0.5533118698347725406 ) ) ;
#20994=ORIENTED_EDGE ( 'NONE', *, *, #983, .T. ) ;
#21000=CARTESIAN_POINT ( 'NONE',  ( 4.257384923554909051, -49.31875000095590877, 25.15230061767466552 ) ) ;
#21013=AXIS2_PLACEMENT_3D ( 'NONE', #9359, #16382, #16177 ) ;
#21028=CARTESIAN_POINT ( 'NONE',  ( 2.507384923554911715, -49.08333333333332860, 26.16266358875650866 ) ) ;
#21040=ORIENTED_EDGE ( 'NONE', *, *, #37946, .F. ) ;
#21050=CARTESIAN_POINT ( 'NONE',  ( 4.257384923554909051, -45.92812500047794799, 25.37105061671875461 ) ) ;
#21051=CARTESIAN_POINT ( 'NONE',  ( -0.7016216170541935693, 3.250000000000000444, 32.48782483564529855 ) ) ;
#21053=CARTESIAN_POINT ( 'NONE',  ( 6.007384923554907274, -44.66666666666665719, 26.16266358875650866 ) ) ;
#21064=CARTESIAN_POINT ( 'NONE',  ( 2.069836725688824597, -46.12285140054812160, 31.97978806193550838 ) ) ;
#21066=FACE_OUTER_BOUND ( 'NONE', #20, .T. ) ;
#21078=CARTESIAN_POINT ( 'NONE',  ( 0.7573849235549120484, -51.45833333333332149, 31.21447844416572792 ) ) ;
#21081=CARTESIAN_POINT ( 'NONE',  ( 7.567941867304905479, -49.01145833381127659, 27.28240155936039812 ) ) ;
#21084=CARTESIAN_POINT ( 'NONE',  ( 4.257384923554909051, 0.8500000000000035305, 23.69375250200204519 ) ) ;
#21085=CARTESIAN_POINT ( 'NONE',  ( 0.7573849235549129366, -44.99999999999999289, 29.19375250200204164 ) ) ;
#21089=CARTESIAN_POINT ( 'NONE',  ( 0.9413079817532863380, -49.16362983155185873, 30.44622632803701379 ) ) ;
#21091=CARTESIAN_POINT ( 'NONE',  ( 4.257384923554908163, -47.26562500047794657, 33.01645438728532866 ) ) ;
#21092=CARTESIAN_POINT ( 'NONE',  ( 0.9468279798049134000, -48.84479166714461940, 27.28240155936039102 ) ) ;
#21099=CARTESIAN_POINT ( 'NONE',  ( 6.007384923554907274, -46.16666666666666430, 26.16266358875650866 ) ) ;
#21100=CARTESIAN_POINT ( 'NONE',  ( 5.912663395429904156, -48.22395833381128227, 32.06077891596451224 ) ) ;
#21112=CARTESIAN_POINT ( 'NONE',  ( 7.757384923554904610, -48.40208333428923737, 27.17302655983835180 ) ) ;
#21138=CARTESIAN_POINT ( 'NONE',  ( 7.567941867304904591, -43.14062500047794657, 29.19375250200204164 ) ) ;
#21145=CARTESIAN_POINT ( 'NONE',  ( 7.757384923554902834, -45.32229166657106845, 31.21447844416572792 ) ) ;
#21150=CARTESIAN_POINT ( 'NONE',  ( 0.9468279798049125118, -50.80312500047794799, 29.19375250200204164 ) ) ;
#21151=LINE ( 'NONE', #30092, #26555 ) ;
#21161=DIRECTION ( 'NONE',  ( -0.000000000000000000, 1.000000000000000000, -0.000000000000000000 ) ) ;
#21165=CARTESIAN_POINT ( 'NONE',  ( 7.308664971437450752, -51.40384482975849778, 27.41904437436932085 ) ) ;
#21175=CARTESIAN_POINT ( 'NONE',  ( 3.319562750045984334, -49.39732909936924443, 32.69375250200203453 ) ) ;
#21183=CARTESIAN_POINT ( 'NONE',  ( 0.9468279798049124008, -51.84895833381127517, 31.10510344464368515 ) ) ;
#21185=CARTESIAN_POINT ( 'NONE',  ( 5.195207097063831547, -47.64732909936925154, 25.69375250200204164 ) ) ;
#21206=CARTESIAN_POINT ( 'NONE',  ( 6.007384923554904610, -50.02708333428924448, 32.22484141524757462 ) ) ;
#21207=CARTESIAN_POINT ( 'NONE',  ( 2.602106451679912169, -42.97395833381127517, 26.32672608803957459 ) ) ;
#21208=ORIENTED_EDGE ( 'NONE', *, *, #7710, .T. ) ;
#21229=CARTESIAN_POINT ( 'NONE',  ( 7.415972775742373457, -42.90766943771486552, 27.65907125533910005 ) ) ;
#21258=CARTESIAN_POINT ( 'NONE',  ( 4.257384923554908163, -44.17812500047794799, 33.01645438728532866 ) ) ;
#21259=DIRECTION ( 'NONE',  ( 0.000000000000000000, 0.000000000000000000, -1.000000000000000000 ) ) ;
#21260=CARTESIAN_POINT ( 'NONE',  ( 4.257384923554909051, -52.75000000000000000, 25.69375250200204519 ) ) ;
#21287=EDGE_CURVE ( 'NONE', #40959, #13392, #34901, .T. ) ;
#21290=CARTESIAN_POINT ( 'NONE',  ( 0.9468279798049115126, -49.76145833381129080, 31.10510344464368515 ) ) ;
#21291=DIRECTION ( 'NONE',  ( -0.8956692225370904703, 0.000000000000000000, -0.4447208605404110449 ) ) ;
#21295=CARTESIAN_POINT ( 'NONE',  ( 7.757384923554904610, -45.20833333333332149, 27.17302655983835180 ) ) ;
#21297=CARTESIAN_POINT ( 'NONE',  ( 3.993753910296014897, -42.81247602818733355, 25.70228806818058587 ) ) ;
#21300=CARTESIAN_POINT ( 'NONE',  ( 2.602106451679912169, -46.97395833381128227, 26.32672608803957459 ) ) ;
#21301=CARTESIAN_POINT ( 'NONE',  ( 0.9468279798049125118, -48.30312500047795510, 29.19375250200204164 ) ) ;
#21306=CARTESIAN_POINT ( 'NONE',  ( 2.507384923554909495, -45.91666666666666430, 32.22484141524756751 ) ) ;
#21307=CARTESIAN_POINT ( 'NONE',  ( 2.602106451679909505, -48.30729166714461087, 32.06077891596451224 ) ) ;
#21319=ORIENTED_EDGE ( 'NONE', *, *, #40415, .F. ) ;
#21320=CARTESIAN_POINT ( 'NONE',  ( 4.257384923554908163, -47.06875000095590877, 33.23520438632941421 ) ) ;
#21335=DIRECTION ( 'NONE',  ( -0.000000000000000000, -1.000000000000000000, -0.000000000000000000 ) ) ;
#21337=ADVANCED_FACE ( 'NONE', ( #11208 ), #2038, .T. ) ;
#21346=AXIS2_PLACEMENT_3D ( 'NONE', #6279, #12025, #27982 ) ;
#21349=CARTESIAN_POINT ( 'NONE',  ( 7.567941867304904591, -43.59895833381127517, 27.28240155936039812 ) ) ;
#21353=CARTESIAN_POINT ( 'NONE',  ( 7.726933515999540703, -44.42951978164393267, 28.49381454767237543 ) ) ;
#21356=CARTESIAN_POINT ( 'NONE',  ( 0.7573849235549138248, -43.57229166657106845, 27.17302655983835180 ) ) ;
#21360=CARTESIAN_POINT ( 'NONE',  ( 2.771876071094220073, -43.60411812439316748, 32.36300227183464528 ) ) ;
#21362=CARTESIAN_POINT ( 'NONE',  ( 7.567941867304905479, -51.05312500047794799, 29.19375250200204164 ) ) ;
#21382=LINE ( 'NONE', #22015, #11025 ) ;
#21389=ORIENTED_EDGE ( 'NONE', *, *, #22820, .T. ) ;
#21392=CARTESIAN_POINT ( 'NONE',  ( 7.567941867304904591, -51.14062500047794657, 29.19375250200204164 ) ) ;
#21401=EDGE_LOOP ( 'NONE', ( #8018, #22716, #34063, #8324 ) ) ;
#21405=CARTESIAN_POINT ( 'NONE',  ( 6.007384923554904610, -51.36395833323773275, 32.22484141524757462 ) ) ;
#21411=CARTESIAN_POINT ( 'NONE',  ( 6.007384923554904610, -48.52708333428923737, 32.22484141524757462 ) ) ;
#21412=DIRECTION ( 'NONE',  ( 0.000000000000000000, 1.000000000000000000, 0.000000000000000000 ) ) ;
#21413=ORIENTED_EDGE ( 'NONE', *, *, #33813, .F. ) ;
#21414=FACE_OUTER_BOUND ( 'NONE', #36141, .T. ) ;
#21416=CARTESIAN_POINT ( 'NONE',  ( 0.8500072554216021592, -46.71152816945775754, 28.38411078750663563 ) ) ;
#21437=CARTESIAN_POINT ( 'NONE',  ( 7.150037004963030185, -42.99135749276166507, 31.23210907253269042 ) ) ;
#21441=CARTESIAN_POINT ( 'NONE',  ( 2.103547607774241879, -47.62041807668300919, 31.99045429902727022 ) ) ;
#21443=ORIENTED_EDGE ( 'NONE', *, *, #6920, .F. ) ;
#21445=DIRECTION ( 'NONE',  ( -0.000000000000000000, -1.000000000000000000, -0.000000000000000000 ) ) ;
#21448=CARTESIAN_POINT ( 'NONE',  ( 6.782377764758458660, -48.88392221002303017, 26.73472259970680298 ) ) ;
#21462=CARTESIAN_POINT ( 'NONE',  ( 5.912663395429907709, -43.46979166714461940, 26.32672608803957459 ) ) ;
#21464=ORIENTED_EDGE ( 'NONE', *, *, #22454, .F. ) ;
#21493=CARTESIAN_POINT ( 'NONE',  ( 0.9468279798049134000, -44.84479166714461940, 27.28240155936039457 ) ) ;
#21498=CARTESIAN_POINT ( 'NONE',  ( 4.257384923554908163, -44.37499999999999289, 33.23520438632941421 ) ) ;
#21500=CARTESIAN_POINT ( 'NONE',  ( 4.749528318899375989, -49.33045755411509248, 25.72634845830355488 ) ) ;
#21503=CARTESIAN_POINT ( 'NONE',  ( 0.9468279798049124008, -47.84895833381128227, 31.10510344464368515 ) ) ;
#21504=CARTESIAN_POINT ( 'NONE',  ( 2.602106451679911281, -48.38645833381128369, 26.32672608803957459 ) ) ;
#21515=CARTESIAN_POINT ( 'NONE',  ( 7.757384923554905498, -46.24999999999999289, 29.19375250200204164 ) ) ;
#21516=CARTESIAN_POINT ( 'NONE',  ( 4.257384923554908163, -47.76562500047794657, 33.01645438728532866 ) ) ;
#21528=CARTESIAN_POINT ( 'NONE',  ( 0.7573849235549120484, -47.65208333428923737, 31.21447844416572792 ) ) ;
#21550=ORIENTED_EDGE ( 'NONE', *, *, #985, .F. ) ;
#21553=CARTESIAN_POINT ( 'NONE',  ( 5.195207097063836876, -51.14732909936925864, 25.69375250200204519 ) ) ;
#21555=CARTESIAN_POINT ( 'NONE',  ( 6.026141589414074851, -50.52825900653745350, 32.24874485226649767 ) ) ;
#21562=CARTESIAN_POINT ( 'NONE',  ( 7.757384923554905498, -42.78062499990439704, 29.19375250200204164 ) ) ;
#21569=CARTESIAN_POINT ( 'NONE',  ( 0.9468279798049125118, -51.30312500047794799, 29.19375250200204164 ) ) ;
#21599=CARTESIAN_POINT ( 'NONE',  ( 4.257384923554908163, -51.26562500047794657, 33.01645438728532866 ) ) ;
#21611=CARTESIAN_POINT ( 'NONE',  ( 0.7573849235549120484, -51.98895833323772564, 31.21447844416572792 ) ) ;
#21616=CARTESIAN_POINT ( 'NONE',  ( 2.507384923554911715, -46.77708333428923737, 26.16266358875650866 ) ) ;
#21619=ORIENTED_EDGE ( 'NONE', *, *, #23267, .T. ) ;
#21644=CARTESIAN_POINT ( 'NONE',  ( 1.048092603370554654, -48.16146086808551274, 30.59185228920202348 ) ) ;
#21650=CARTESIAN_POINT ( 'NONE',  ( 7.287654462391790489, -48.90293258088438932, 27.39378488270755696 ) ) ;
#21664=CARTESIAN_POINT ( 'NONE',  ( 5.912663395429905044, -44.63645833381128369, 32.06077891596451224 ) ) ;
#21669=CARTESIAN_POINT ( 'NONE',  ( 7.757384923554904610, -44.70833333333332149, 27.17302655983835180 ) ) ;
#21689=FACE_OUTER_BOUND ( 'NONE', #31530, .T. ) ;
#21700=CARTESIAN_POINT ( 'NONE',  ( 0.7573849235549120484, -42.95833333333332149, 31.21447844416572792 ) ) ;
#21706=CARTESIAN_POINT ( 'NONE',  ( 5.912663395429904156, -45.22395833381128227, 32.06077891596451224 ) ) ;
#21708=CARTESIAN_POINT ( 'NONE',  ( 0.9468279798049125118, -44.80312500047794799, 29.19375250200204164 ) ) ;
#21719=CARTESIAN_POINT ( 'NONE',  ( 7.757384923554902834, -45.79166666666666430, 31.21447844416572792 ) ) ;
#21720=CARTESIAN_POINT ( 'NONE',  ( 5.912663395429904156, -47.22395833381128227, 32.06077891596451224 ) ) ;
#21731=CARTESIAN_POINT ( 'NONE',  ( 4.257384923554908163, -46.06875000095590167, 33.23520438632941421 ) ) ;
#21756=CARTESIAN_POINT ( 'NONE',  ( 0.7573849235549138248, -51.04166666666665719, 27.17302655983835180 ) ) ;
#21757=VERTEX_POINT ( 'NONE', #915 ) ;
#21762=CARTESIAN_POINT ( 'NONE',  ( 6.402363158501022333, -50.36881415189684930, 26.39060333789040413 ) ) ;
#21771=CARTESIAN_POINT ( 'NONE',  ( 2.975060292544088991, -42.43615653873800397, 32.45038320576673385 ) ) ;
#21776=CIRCLE ( 'NONE', #1418, 8.161279603635190227 ) ;
#21778=CARTESIAN_POINT ( 'NONE',  ( 0.9468279798049134000, -48.34479166714461940, 27.28240155936039457 ) ) ;
#21791=B_SPLINE_CURVE_WITH_KNOTS ( 'NONE', 3,
 ( #40103, #13953, #10552, #30743, #23957, #33295, #11185, #33935, #1191, #4793, #17772, #7356, #21165, #14373, #3950, #4161, #40320, #16931, #7787, #17566, #766, #23534, #30530, #20329, #13741, #26719, #17144, #24168, #10755 ),
 .UNSPECIFIED., .F., .F.,
 ( 4, 2, 2, 2, 2, 2, 2, 2, 2, 2, 2, 1, 1, 1, 2, 4 ),
 ( 0.03808854773444813463, 0.04126262049067793564, 0.04443669324690773664, 0.04761076600313753765, 0.05078483875936733866, 0.05395891151559713966, 0.05713298427182694761, 0.06030705702805674862, 0.06189409340617164912, 0.06268761159522909243, 0.06308437068975782103, 0.06328275023702217839, 0.06338194001065436400, 0.06343153489747044294, 0.06345633234087849628, 0.06348112978428653574 ),
 .UNSPECIFIED. ) ;
#21814=CARTESIAN_POINT ( 'NONE',  ( 7.567941867304902814, -48.68229166714461087, 31.10510344464368870 ) ) ;
#21821=ORIENTED_EDGE ( 'NONE', *, *, #34208, .F. ) ;
#21825=CARTESIAN_POINT ( 'NONE',  ( 2.507384923554911715, -50.61395833323773985, 26.16266358875650866 ) ) ;
#21831=CARTESIAN_POINT ( 'NONE',  ( 0.7573849235549138248, -46.23541666762256597, 27.17302655983835180 ) ) ;
#21836=CARTESIAN_POINT ( 'NONE',  ( 3.572068845384973379, -46.80250833452109305, 25.75798382792596897 ) ) ;
#21843=ORIENTED_EDGE ( 'NONE', *, *, #40981, .F. ) ;
#21876=VECTOR ( 'NONE', #25225, 1000.000000000000000 ) ;
#21878=CARTESIAN_POINT ( 'NONE',  ( 7.567941867304905479, -44.55312500047794799, 29.19375250200204164 ) ) ;
#21883=ORIENTED_EDGE ( 'NONE', *, *, #25959, .T. ) ;
#21891=PLANE ( 'NONE',  #94 ) ;
#21897=CARTESIAN_POINT ( 'NONE',  ( 6.156270467797392953, -45.52346842833804175, 32.13509314577868281 ) ) ;
#21909=ORIENTED_EDGE ( 'NONE', *, *, #19848, .T. ) ;
#21912=VERTEX_POINT ( 'NONE', #34491 ) ;
#21913=CARTESIAN_POINT ( 'NONE',  ( 2.602106451679909505, -44.30729166714461797, 32.06077891596451224 ) ) ;
#21914=CARTESIAN_POINT ( 'NONE',  ( 7.567941867304905479, -45.51145833381128369, 27.28240155936039457 ) ) ;
#21921=EDGE_CURVE ( 'NONE', #31713, #11420, #5975, .T. ) ;
#21925=CARTESIAN_POINT ( 'NONE',  ( 0.7573849235549138248, -45.04166666666665719, 27.17302655983835180 ) ) ;
#21926=CARTESIAN_POINT ( 'NONE',  ( 5.912663395429904156, -49.22395833381128227, 32.06077891596451224 ) ) ;
#21939=CARTESIAN_POINT ( 'NONE',  ( 6.007384923554904610, -45.52708333428923737, 32.22484141524757462 ) ) ;
#21952=ADVANCED_FACE ( 'NONE', ( #16978 ), #42081, .T. ) ;
#21955=DIRECTION ( 'NONE',  ( -0.3664133999068575620, 0.000000000000000000, 0.9304521590972300027 ) ) ;
#21961=CARTESIAN_POINT ( 'NONE',  ( 0.7573849235549138248, -50.54166666666666430, 27.17302655983835180 ) ) ;
#21964=CARTESIAN_POINT ( 'NONE',  ( 7.757384923554902834, -48.79166666666665719, 31.21447844416572792 ) ) ;
#21967=CYLINDRICAL_SURFACE ( 'NONE', #2028, 3.499999999999996003 ) ;
#21971=CARTESIAN_POINT ( 'NONE',  ( 0.9468279798049143992, -50.93229166714461797, 27.28240155936039812 ) ) ;
#21978=CARTESIAN_POINT ( 'NONE',  ( 3.083927878817848800, -51.09605461309415375, 32.49185118153732077 ) ) ;
#21980=AXIS2_PLACEMENT_3D ( 'NONE', #31611, #2476, #15461 ) ;
#21983=CARTESIAN_POINT ( 'NONE',  ( 0.7573849235549120484, -51.95833333333331439, 31.21447844416572792 ) ) ;
#21989=CARTESIAN_POINT ( 'NONE',  ( 4.257384923554908163, -47.67812500047795510, 33.01645438728532866 ) ) ;
#21993=CARTESIAN_POINT ( 'NONE',  ( 2.507384923554911715, -51.27708333428923737, 26.16266358875650866 ) ) ;
#21999=CARTESIAN_POINT ( 'NONE',  ( 4.257384923554909051, -52.75000000000000000, 29.19375250200204164 ) ) ;
#22009=CARTESIAN_POINT ( 'NONE',  ( 5.195207097063836876, -43.14732909936924443, 25.69375250200204519 ) ) ;
#22015=CARTESIAN_POINT ( 'NONE',  ( -0.7016216170541935693, 7.250000000000000000, 32.48782483564529855 ) ) ;
#22024=CARTESIAN_POINT ( 'NONE',  ( 0.9468279798049132889, -48.39062500047794657, 29.19375250200204164 ) ) ;
#22033=EDGE_LOOP ( 'NONE', ( #20802, #7235, #1936, #18758 ) ) ;
#22036=CARTESIAN_POINT ( 'NONE',  ( 6.007384923554907274, -50.69729166657106845, 26.16266358875650866 ) ) ;
#22040=EDGE_CURVE ( 'NONE', #32848, #26379, #15807, .T. ) ;
#22041=CARTESIAN_POINT ( 'NONE',  ( 7.620821354785999979, -42.46540792933351582, 30.20096157197999531 ) ) ;
#22042=CARTESIAN_POINT ( 'NONE',  ( 4.257384923554909051, -47.31875000095590877, 25.15230061767466552 ) ) ;
#22046=ORIENTED_EDGE ( 'NONE', *, *, #13094, .F. ) ;
#22049=CARTESIAN_POINT ( 'NONE',  ( 3.763199081207714070, -46.58078260122964309, 32.69375242042011109 ) ) ;
#22073=CARTESIAN_POINT ( 'NONE',  ( 4.257384923554909051, -52.75000000000000000, 29.19375250200204164 ) ) ;
#22074=CARTESIAN_POINT ( 'NONE',  ( 3.853488659696043594, -48.07615523671388047, 32.69375262531720949 ) ) ;
#22080=LINE ( 'NONE', #18884, #36270 ) ;
#22086=CARTESIAN_POINT ( 'NONE',  ( 5.913632385058036789, -48.02931069145864029, 32.27730123685776675 ) ) ;
#22091=ORIENTED_EDGE ( 'NONE', *, *, #33181, .T. ) ;
#22095=CARTESIAN_POINT ( 'NONE',  ( 7.567941867304905479, -42.55312500047794799, 29.19375250200204164 ) ) ;
#22096=CARTESIAN_POINT ( 'NONE',  ( 2.975067305262454553, -42.09928137282000904, 32.45038596706375955 ) ) ;
#22120=LINE ( 'NONE', #38705, #10144 ) ;
#22125=CARTESIAN_POINT ( 'NONE',  ( 7.757384923554904610, -42.70833333333332149, 27.17302655983835180 ) ) ;
#22129=AXIS2_PLACEMENT_3D ( 'NONE', #12573, #19572, #25974 ) ;
#22131=CARTESIAN_POINT ( 'NONE',  ( 2.602106451679912169, -44.97395833381127517, 26.32672608803957459 ) ) ;
#22132=CARTESIAN_POINT ( 'NONE',  ( 2.602106451679911281, -43.88645833381129080, 26.32672608803957459 ) ) ;
#22141=CARTESIAN_POINT ( 'NONE',  ( 2.507384923554911715, -50.77708333428923737, 26.16266358875650866 ) ) ;
#22142=CARTESIAN_POINT ( 'NONE',  ( 7.567941867304902814, -45.09895833381128227, 27.28240155936039457 ) ) ;
#22143=ORIENTED_EDGE ( 'NONE', *, *, #13650, .T. ) ;
#22144=CARTESIAN_POINT ( 'NONE',  ( 4.257384923554909051, -42.62499999999998579, 25.69375250200204519 ) ) ;
#22169=CARTESIAN_POINT ( 'NONE',  ( 4.257384923554933032, -44.62499999999999289, 25.69375250200204519 ) ) ;
#22171=ORIENTED_EDGE ( 'NONE', *, *, #40673, .T. ) ;
#22179=CARTESIAN_POINT ( 'NONE',  ( 7.757384923554904610, -50.20833333333332860, 27.17302655983835180 ) ) ;
#22184=CARTESIAN_POINT ( 'NONE',  ( 5.195207097063835988, -51.35267090063072715, 32.69375250200204164 ) ) ;
#22186=CARTESIAN_POINT ( 'NONE',  ( 2.602106451679909505, -51.80729166714461797, 32.06077891596451224 ) ) ;
#22192=CARTESIAN_POINT ( 'NONE',  ( 6.007384923554907274, -43.69729166657106845, 26.16266358875650866 ) ) ;
#22193=CARTESIAN_POINT ( 'NONE',  ( 5.912663395429907709, -52.05729166714461797, 26.32672608803957459 ) ) ;
#22196=CARTESIAN_POINT ( 'NONE',  ( 4.257369266595627977, -50.56937335658698629, 32.69375250193562721 ) ) ;
#22198=CARTESIAN_POINT ( 'NONE',  ( 7.567941867304905479, -49.55312500047794799, 29.19375250200204164 ) ) ;
#22216=CARTESIAN_POINT ( 'NONE',  ( 6.007384923554904610, -46.83333333333332149, 32.22484141524757462 ) ) ;
#22224=CARTESIAN_POINT ( 'NONE',  ( 4.257384923554913492, -49.87499999999998579, 32.69375250200203453 ) ) ;
#22230=CARTESIAN_POINT ( 'NONE',  ( 7.567941867304902814, -47.18229166714461797, 31.10510344464368870 ) ) ;
#22238=VERTEX_POINT ( 'NONE', #4427 ) ;
#22241=CARTESIAN_POINT ( 'NONE',  ( 7.757384923554905498, -52.28062499990439704, 29.19375250200204164 ) ) ;
#22247=ADVANCED_FACE ( 'NONE', ( #27601 ), #11423, .T. ) ;
#22248=CARTESIAN_POINT ( 'NONE',  ( 4.257384923554908163, -45.56875000095590877, 33.23520438632941421 ) ) ;
#22254=CARTESIAN_POINT ( 'NONE',  ( 4.030559182192665624, -46.81336481243554459, 25.70000453595535106 ) ) ;
#22276=CARTESIAN_POINT ( 'NONE',  ( 1.081983712932322872, -48.15953144158772403, 30.66585717381950360 ) ) ;
#22277=EDGE_CURVE ( 'NONE', #6697, #5921, #30368, .T. ) ;
#22280=CARTESIAN_POINT ( 'NONE',  ( 3.689249602914889792, -46.30523570627047292, 25.73827641594606064 ) ) ;
#22282=CARTESIAN_POINT ( 'NONE',  ( 7.567941867304905479, -46.51145833381128369, 27.28240155936039812 ) ) ;
#22285=CARTESIAN_POINT ( 'NONE',  ( 3.319562750045982114, -49.89732909936924443, 32.69375250200203453 ) ) ;
#22290=CARTESIAN_POINT ( 'NONE',  ( 7.407469031562221140, -47.90812882181839427, 27.66823706545921979 ) ) ;
#22305=VERTEX_POINT ( 'NONE', #27396 ) ;
#22313=CARTESIAN_POINT ( 'NONE',  ( 4.257384923554909051, -52.75000000000000000, 29.19375250200204164 ) ) ;
#22320=CARTESIAN_POINT ( 'NONE',  ( 7.430177488131596952, -45.40938595896132313, 27.71609088511753072 ) ) ;
#22330=CARTESIAN_POINT ( 'NONE',  ( 0.7573849235549129366, -42.49999999999998579, 29.19375250200204164 ) ) ;
#22331=ORIENTED_EDGE ( 'NONE', *, *, #38886, .F. ) ;
#22333=ORIENTED_EDGE ( 'NONE', *, *, #36438, .F. ) ;
#22334=CARTESIAN_POINT ( 'NONE',  ( 4.257384923554908163, -44.76562500047793947, 33.01645438728532866 ) ) ;
#22336=CARTESIAN_POINT ( 'NONE',  ( 2.602106451679909505, -45.71979166714461229, 32.06077891596451224 ) ) ;
#22344=CARTESIAN_POINT ( 'NONE',  ( 6.007384923554904610, -51.52708333428923737, 32.22484141524757462 ) ) ;
#22345=CARTESIAN_POINT ( 'NONE',  ( 7.567941867304902814, -44.59895833381127517, 27.28240155936039457 ) ) ;
#22350=CARTESIAN_POINT ( 'NONE',  ( 3.319562750045979005, -51.89732909936925154, 32.69375250200202743 ) ) ;
#22379=CARTESIAN_POINT ( 'NONE',  ( 6.408309811828229563, -47.37045199512397176, 26.39492741656993857 ) ) ;
#22381=CARTESIAN_POINT ( 'NONE',  ( 7.757384923554905498, -49.74999999999998579, 29.19375250200204164 ) ) ;
#22387=CARTESIAN_POINT ( 'NONE',  ( 6.994870607861680689, -43.38967706515961709, 27.01162554253875214 ) ) ;
#22388=CARTESIAN_POINT ( 'NONE',  ( 7.567941867304902814, -51.18229166714461797, 31.10510344464368870 ) ) ;
#22392=CARTESIAN_POINT ( 'NONE',  ( 4.257450628761716871, -44.31875150865747770, 25.69375250261877852 ) ) ;
#22394=ORIENTED_EDGE ( 'NONE', *, *, #12739, .F. ) ;
#22395=CARTESIAN_POINT ( 'NONE',  ( 2.507384923554911715, -49.58333333333332860, 26.16266358875650866 ) ) ;
#22399=CARTESIAN_POINT ( 'NONE',  ( 5.904241062626556236, -46.53119246876942583, 32.29888734342581103 ) ) ;
#22401=CARTESIAN_POINT ( 'NONE',  ( 5.912663395429905044, -49.63645833381128369, 32.06077891596451224 ) ) ;
#22402=CARTESIAN_POINT ( 'NONE',  ( 4.257384923554933032, -46.12499999999999289, 25.69375250200204519 ) ) ;
#22404=CARTESIAN_POINT ( 'NONE',  ( 0.7811708671735319021, -48.68493110547730396, 29.60801628933985796 ) ) ;
#22436=CARTESIAN_POINT ( 'NONE',  ( 0.9468279798049132889, -47.89062500047795368, 29.19375250200204164 ) ) ;
#22441=CARTESIAN_POINT ( 'NONE',  ( 5.912663395429907709, -51.46979166714461940, 26.32672608803957459 ) ) ;
#22447=CARTESIAN_POINT ( 'NONE',  ( 6.007384923554904610, -49.36395833323773275, 32.22484141524757462 ) ) ;
#22454=EDGE_CURVE ( 'NONE', #19510, #18276, #2902, .T. ) ;
#22455=CARTESIAN_POINT ( 'NONE',  ( 7.757384923554902834, -47.48541666762257307, 31.21447844416572792 ) ) ;
#22457=VERTEX_POINT ( 'NONE', #15468 ) ;
#22467=CARTESIAN_POINT ( 'NONE',  ( 4.257384923554907274, -51.87499999999998579, 32.69375250200203453 ) ) ;
#22469=CARTESIAN_POINT ( 'NONE',  ( 0.7573878485754695911, -51.68739197721828305, 29.50209254531660363 ) ) ;
#22474=EDGE_CURVE ( 'NONE', #10651, #34914, #37392, .T. ) ;
#22487=CARTESIAN_POINT ( 'NONE',  ( 0.7623740516855057603, -46.18963251199608067, 29.39096203830372289 ) ) ;
#22488=CARTESIAN_POINT ( 'NONE',  ( 5.912663395429905044, -46.63645833381128369, 32.06077891596451224 ) ) ;
#22490=CARTESIAN_POINT ( 'NONE',  ( 7.757384923554905498, -48.74999999999998579, 29.19375250200204164 ) ) ;
#22497=CARTESIAN_POINT ( 'NONE',  ( 7.141108303417849967, -47.89530833727987158, 27.19567554177005420 ) ) ;
#22506=CARTESIAN_POINT ( 'NONE',  ( 2.964536502290532116, -50.59953207861128277, 32.44622767541088137 ) ) ;
#22509=CARTESIAN_POINT ( 'NONE',  ( 0.7573849235549138248, -42.23541666762257307, 27.17302655983835180 ) ) ;
#22532=CARTESIAN_POINT ( 'NONE',  ( 0.7333764871000142405, -45.69502387869238902, 29.18399187108765958 ) ) ;
#22540=CARTESIAN_POINT ( 'NONE',  ( 1.206062530532070465, -42.65384670844836990, 30.96838786158913237 ) ) ;
#22543=ORIENTED_EDGE ( 'NONE', *, *, #18856, .F. ) ;
#22544=CARTESIAN_POINT ( 'NONE',  ( 2.602106451679909505, -42.30729166714461087, 32.06077891596451224 ) ) ;
#22545=CARTESIAN_POINT ( 'NONE',  ( 0.9468279798049117346, -44.26145833381128369, 31.10510344464368515 ) ) ;
#22555=CARTESIAN_POINT ( 'NONE',  ( 7.567941867304904591, -45.64062500047794657, 29.19375250200204164 ) ) ;
#22591=CARTESIAN_POINT ( 'NONE',  ( 5.912663395429905044, -51.13645833381127659, 32.06077891596451224 ) ) ;
#22595=CARTESIAN_POINT ( 'NONE',  ( 0.7573849235549129366, -50.49999999999998579, 29.19375250200204164 ) ) ;
#22600=CARTESIAN_POINT ( 'NONE',  ( 6.935531341145688700, -43.38750154232880618, 26.94033822869736383 ) ) ;
#22601=CARTESIAN_POINT ( 'NONE',  ( 4.263161279384791058, -50.31887426667181273, 25.69375248084578800 ) ) ;
#22604=CARTESIAN_POINT ( 'NONE',  ( 2.364947325114048038, -51.11505784934748675, 32.17249133374848924 ) ) ;
#22606=ORIENTED_EDGE ( 'NONE', *, *, #12313, .T. ) ;
#22607=CARTESIAN_POINT ( 'NONE',  ( 4.257384923554908163, -49.37499999999998579, 33.23520438632941421 ) ) ;
#22608=AXIS2_PLACEMENT_3D ( 'NONE', #25310, #15532, #18503 ) ;
#22609=CARTESIAN_POINT ( 'NONE',  ( 7.757384923554902834, -45.29166666666666430, 31.21447844416572792 ) ) ;
#22614=CARTESIAN_POINT ( 'NONE',  ( 3.319562750045990107, -45.89732909936925154, 32.69375250200203453 ) ) ;
#22634=CARTESIAN_POINT ( 'NONE',  ( 0.8005478461356869690, -44.20558378326217053, 28.64446800900155310 ) ) ;
#22646=CIRCLE ( 'NONE', #8973, 2.000000000000001776 ) ;
#22652=CARTESIAN_POINT ( 'NONE',  ( 5.912663395429904156, -46.72395833381128227, 32.06077891596451224 ) ) ;
#22657=CARTESIAN_POINT ( 'NONE',  ( 0.9468279798049134000, -50.34479166714461940, 27.28240155936039102 ) ) ;
#22664=CARTESIAN_POINT ( 'NONE',  ( 7.757384923554904610, -48.23895833323773275, 27.17302655983835180 ) ) ;
#22670=CARTESIAN_POINT ( 'NONE',  ( 0.7573849235549120484, -45.15208333428923737, 31.21447844416572792 ) ) ;
#22684=PLANE ( 'NONE',  #1656 ) ;
#22690=DIRECTION ( 'NONE',  ( 0.000000000000000000, 0.000000000000000000, 1.000000000000000000 ) ) ;
#22696=LINE ( 'NONE', #35674, #34275 ) ;
#22701=DIRECTION ( 'NONE',  ( 0.000000000000000000, 0.000000000000000000, 1.000000000000000000 ) ) ;
#22702=ORIENTED_EDGE ( 'NONE', *, *, #33721, .T. ) ;
#22705=CARTESIAN_POINT ( 'NONE',  ( 2.602106451679909505, -46.21979166714461229, 32.06077891596451224 ) ) ;
#22706=CYLINDRICAL_SURFACE ( 'NONE', #34695, 3.499999999999996003 ) ;
#22716=ORIENTED_EDGE ( 'NONE', *, *, #32098, .T. ) ;
#22721=ORIENTED_EDGE ( 'NONE', *, *, #12587, .T. ) ;
#22723=CARTESIAN_POINT ( 'NONE',  ( 3.715142781114328940, -50.80676820811537908, 25.73341133688291293 ) ) ;
#22750=CARTESIAN_POINT ( 'NONE',  ( 3.319562750045982114, -50.89732909936924443, 32.69375250200203453 ) ) ;
#22760=AXIS2_PLACEMENT_3D ( 'NONE', #20440, #39147, #7466 ) ;
#22762=CARTESIAN_POINT ( 'NONE',  ( 7.567941867304905479, -42.51145833381127659, 27.28240155936039457 ) ) ;
#22769=CARTESIAN_POINT ( 'NONE',  ( 0.9468279798049132889, -45.89062500047794657, 29.19375250200204164 ) ) ;
#22774=FACE_OUTER_BOUND ( 'NONE', #2032, .T. ) ;
#22797=CIRCLE ( 'NONE', #11234, 5.499999999999994671 ) ;
#22802=CARTESIAN_POINT ( 'NONE',  ( 7.567941867304905479, -50.51145833381129080, 27.28240155936039812 ) ) ;
#22803=CARTESIAN_POINT ( 'NONE',  ( 3.925745719294190472, -47.31126343589836836, 25.70887367337366314 ) ) ;
#22805=CARTESIAN_POINT ( 'NONE',  ( 0.7573849235549129366, -45.99999999999999289, 29.19375250200204164 ) ) ;
#22813=CARTESIAN_POINT ( 'NONE',  ( 4.257384923554909051, -48.01562500047794657, 25.37105061671875461 ) ) ;
#22819=CARTESIAN_POINT ( 'NONE',  ( 6.007384923554904610, -49.83333333333332860, 32.22484141524757462 ) ) ;
#22820=EDGE_CURVE ( 'NONE', #27786, #20633, #23732, .T. ) ;
#22822=CARTESIAN_POINT ( 'NONE',  ( 4.257461754300457812, -46.31875183025808695, 25.69375250284532441 ) ) ;
#22828=CARTESIAN_POINT ( 'NONE',  ( 4.257386979189129228, -48.56866505152967761, 32.69375250200084793 ) ) ;
#22844=CARTESIAN_POINT ( 'NONE',  ( 2.732842139880885757, -42.41129863770652264, 32.35500919978411360 ) ) ;
#22846=CARTESIAN_POINT ( 'NONE',  ( 6.007384923554907274, -42.86041666762257307, 26.16266358875650866 ) ) ;
#22855=ORIENTED_EDGE ( 'NONE', *, *, #24668, .T. ) ;
#22859=CARTESIAN_POINT ( 'NONE',  ( 0.9468279798049143992, -44.43229166714461797, 27.28240155936039812 ) ) ;
#22863=CARTESIAN_POINT ( 'NONE',  ( 5.912663395429905044, -51.13645833381127659, 32.06077891596451224 ) ) ;
#22867=ORIENTED_EDGE ( 'NONE', *, *, #33813, .T. ) ;
#22868=SHAPE_DEFINITION_REPRESENTATION ( #27547, #33982 ) ;
#22871=CARTESIAN_POINT ( 'NONE',  ( 7.757384923554902834, -47.82229166657106845, 31.21447844416572792 ) ) ;
#22879=CARTESIAN_POINT ( 'NONE',  ( 2.507384923554909495, -44.61041666762257307, 32.22484141524756751 ) ) ;
#22882=CARTESIAN_POINT ( 'NONE',  ( 2.507384923554911715, -43.08333333333332149, 26.16266358875650866 ) ) ;
#22887=CARTESIAN_POINT ( 'NONE',  ( 4.257384923554909051, -52.75000000000000000, 32.19375250200202743 ) ) ;
#22897=CYLINDRICAL_SURFACE ( 'NONE', #3597, 3.499999999999996003 ) ;
#22912=CARTESIAN_POINT ( 'NONE',  ( 7.662663395429905044, -52.19531250023896973, 29.19375250200204164 ) ) ;
#22916=CARTESIAN_POINT ( 'NONE',  ( 4.257384923554908163, -47.17812500047795510, 33.01645438728532866 ) ) ;
#22917=CARTESIAN_POINT ( 'NONE',  ( 4.038569912741984069, -42.40485061181025372, 32.69375250200203453 ) ) ;
#22922=CARTESIAN_POINT ( 'NONE',  ( 7.716730981793489264, -51.93002277015963841, 28.53818617167758376 ) ) ;
#22925=CARTESIAN_POINT ( 'NONE',  ( 2.975064734268261457, -42.40508397444173738, 32.45039488375558534 ) ) ;
#22927=CARTESIAN_POINT ( 'NONE',  ( 4.257384923554907274, -46.37499999999999289, 32.69375250200203453 ) ) ;
#22933=CARTESIAN_POINT ( 'NONE',  ( 3.181052230905419886, -50.59442759521505906, 32.52464168526255861 ) ) ;
#22967=CARTESIAN_POINT ( 'NONE',  ( 0.9468279798049117346, -42.76145833381128369, 31.10510344464368515 ) ) ;
#22972=CARTESIAN_POINT ( 'NONE',  ( 4.658284337105766504, -46.82822810660776724, 25.70768768217521227 ) ) ;
#23004=CARTESIAN_POINT ( 'NONE',  ( 5.912663395429907709, -50.96979166714461940, 26.32672608803957459 ) ) ;
#23008=CARTESIAN_POINT ( 'NONE',  ( 0.7573849235549129366, -47.99999999999999289, 29.19375250200204164 ) ) ;
#23013=CARTESIAN_POINT ( 'NONE',  ( 4.257384951507396487, -49.81875000160972178, 25.69375250200204519 ) ) ;
#23015=CARTESIAN_POINT ( 'NONE',  ( 4.262153375005306444, -43.31885319070804030, 25.69375243662408437 ) ) ;
#23016=CARTESIAN_POINT ( 'NONE',  ( 0.9468279798049124008, -50.34895833381128227, 31.10510344464368515 ) ) ;
#23022=CARTESIAN_POINT ( 'NONE',  ( 2.507384923554911715, -50.08333333333332860, 26.16266358875650866 ) ) ;
#23025=CARTESIAN_POINT ( 'NONE',  ( 7.761257069329811742, -46.45657936012712241, 29.68743104824112677 ) ) ;
#23027=CARTESIAN_POINT ( 'NONE',  ( 0.7573849235549138248, -46.04166666666666430, 27.17302655983835180 ) ) ;
#23029=CARTESIAN_POINT ( 'NONE',  ( 2.069850073676410496, -48.62285096376518823, 31.97979772785634367 ) ) ;
#23032=CARTESIAN_POINT ( 'NONE',  ( 0.7573849235549120484, -48.65208333428924448, 31.21447844416572792 ) ) ;
#23034=( BOUNDED_CURVE ( )  B_SPLINE_CURVE ( 2, ( #5116, #40223, #11908, #15114, #27867, #21078, #30861, #5535, #11094 ),
 .UNSPECIFIED., .F., .F. ) 
 B_SPLINE_CURVE_WITH_KNOTS ( ( 3, 2, 2, 2, 3 ),
 ( 0.06250000000000000000, 0.06666666666666666574, 0.07499999999999999722, 0.08333333333333332871, 0.08749999999999999445 ),
 .UNSPECIFIED. ) 
 CURVE ( )  GEOMETRIC_REPRESENTATION_ITEM ( )  RATIONAL_B_SPLINE_CURVE ( ( 0.9330127018922194093, 0.9330127018922194093, 1.000000000000000000, 0.8660254037844387076, 1.000000000000000000, 0.8660254037844387076, 1.000000000000000000, 0.9330127018922194093, 0.9330127018922194093 ) ) 
 REPRESENTATION_ITEM ( '' )  );
#23048=CARTESIAN_POINT ( 'NONE',  ( 4.257384923554907274, -46.87499999999997868, 32.69375250200203453 ) ) ;
#23050=CARTESIAN_POINT ( 'NONE',  ( 4.257384923554908163, -42.56875000095590877, 33.23520438632941421 ) ) ;
#23063=CARTESIAN_POINT ( 'NONE',  ( 4.257384923554909051, -46.51562500047795368, 25.37105061671875461 ) ) ;
#23067=CARTESIAN_POINT ( 'NONE',  ( 0.9468279798049117346, -50.76145833381127659, 31.10510344464368515 ) ) ;
#23074=CARTESIAN_POINT ( 'NONE',  ( 7.757384923554905498, -47.28062499990440415, 29.19375250200204164 ) ) ;
#23079=VECTOR ( 'NONE', #10620, 1000.000000000000000 ) ;
#23081=CARTESIAN_POINT ( 'NONE',  ( 7.757384923554905498, -43.94375000095590877, 29.19375250200204164 ) ) ;
#23082=CARTESIAN_POINT ( 'NONE',  ( 7.757384923554904610, -44.40208333428923737, 27.17302655983835180 ) ) ;
#23084=EDGE_LOOP ( 'NONE', ( #10022, #5970, #8110, #381 ) ) ;
#23092=DIRECTION ( 'NONE',  ( -0.000000000000000000, -1.000000000000000000, -0.000000000000000000 ) ) ;
#23109=DIRECTION ( 'NONE',  ( -0.000000000000000000, -1.000000000000000000, -0.000000000000000000 ) ) ;
#23120=CARTESIAN_POINT ( 'NONE',  ( 4.257384923554909051, -52.01562500047794657, 25.37105061671875461 ) ) ;
#23122=LINE ( 'NONE', #7177, #33270 ) ;
#23129=CARTESIAN_POINT ( 'NONE',  ( 4.707822264375590926, -48.32862403533003715, 25.69375251710364338 ) ) ;
#23137=CARTESIAN_POINT ( 'NONE',  ( 2.928276342377338803, -50.60039756292551516, 32.43162537804890633 ) ) ;
#23138=CARTESIAN_POINT ( 'NONE',  ( 0.7573849235549129366, -51.19375000095590167, 29.19375250200204164 ) ) ;
#23144=CARTESIAN_POINT ( 'NONE',  ( 4.257384923554909051, -52.75000000000000000, 25.69375250200204519 ) ) ;
#23163=CARTESIAN_POINT ( 'NONE',  ( 6.007384923554907274, -47.16666666666665719, 26.16266358875650866 ) ) ;
#23178=CARTESIAN_POINT ( 'NONE',  ( 3.044481415175603889, -42.20865620537255580, 32.27411812269912161 ) ) ;
#23184=CARTESIAN_POINT ( 'NONE',  ( 2.602106451679909505, -49.71979166714461940, 32.06077891596451224 ) ) ;
#23207=CARTESIAN_POINT ( 'NONE',  ( 0.7573849235549138248, -47.54166666666666430, 27.17302655983835180 ) ) ;
#23213=CARTESIAN_POINT ( 'NONE',  ( 7.567941867304904591, -50.59479166714461940, 31.10510344464368870 ) ) ;
#23217=CARTESIAN_POINT ( 'NONE',  ( 0.7573849235549129366, -46.99999999999999289, 29.19375250200204164 ) ) ;
#23224=CARTESIAN_POINT ( 'NONE',  ( 2.602106451679912169, -50.47395833381128227, 26.32672608803957459 ) ) ;
#23231=CARTESIAN_POINT ( 'NONE',  ( 6.007384923554904610, -50.33333333333332860, 32.22484141524757462 ) ) ;
#23232=CARTESIAN_POINT ( 'NONE',  ( 7.567941867304902814, -51.09895833381127517, 27.28240155936039457 ) ) ;
#23235=CARTESIAN_POINT ( 'NONE',  ( 2.394195599962267273, -43.27583420276952353, 26.19676773333621966 ) ) ;
#23236=CARTESIAN_POINT ( 'NONE',  ( 4.257384923554931255, -45.87499999999999289, 32.69375250200203453 ) ) ;
#23244=CARTESIAN_POINT ( 'NONE',  ( 0.7573849235549138248, -50.23541666762257307, 27.17302655983835180 ) ) ;
#23246=EDGE_CURVE ( 'NONE', #631, #37688, #41991, .T. ) ;
#23258=CARTESIAN_POINT ( 'NONE',  ( 4.240755248502659391, -44.81837509681764686, 25.69378953085992734 ) ) ;
#23267=EDGE_CURVE ( 'NONE', #27947, #31713, #15839, .T. ) ;
#23274=CARTESIAN_POINT ( 'NONE',  ( 5.912663395429907709, -46.05729166714461797, 26.32672608803957459 ) ) ;
#23280=CARTESIAN_POINT ( 'NONE',  ( 7.567941867304905479, -47.51145833381127659, 27.28240155936039457 ) ) ;
#23287=CARTESIAN_POINT ( 'NONE',  ( 4.257384923554908163, -49.40562499990439704, 33.23520438632941421 ) ) ;
#23294=CARTESIAN_POINT ( 'NONE',  ( 4.257384923554909051, -43.31875000095590877, 25.15230061767466552 ) ) ;
#23296=CARTESIAN_POINT ( 'NONE',  ( 2.507384923554911715, -44.27708333428923737, 26.16266358875650866 ) ) ;
#23304=FACE_OUTER_BOUND ( 'NONE', #12580, .T. ) ;
#23306=EDGE_CURVE ( 'NONE', #36237, #35115, #190, .T. ) ;
#23318=UNCERTAINTY_MEASURE_WITH_UNIT (LENGTH_MEASURE( 1.000000000000000082E-05 ), #8968, 'distance_accuracy_value', 'NONE');
#23339=CARTESIAN_POINT ( 'NONE',  ( 0.9468279798049134000, -42.84479166714461940, 27.28240155936039457 ) ) ;
#23348=CARTESIAN_POINT ( 'NONE',  ( 0.7582832065333493521, -42.40498225309123370, 29.47211600025429590 ) ) ;
#23349=EDGE_LOOP ( 'NONE', ( #30616, #39288, #16215, #1791 ) ) ;
#23354=FACE_OUTER_BOUND ( 'NONE', #17658, .T. ) ;
#23358=CARTESIAN_POINT ( 'NONE',  ( 1.279376412211809866, -50.73804284335264470, 27.34751721469076813 ) ) ;
#23359=CARTESIAN_POINT ( 'NONE',  ( 7.757384923554904610, -51.90208333428923737, 27.17302655983835180 ) ) ;
#23363=CARTESIAN_POINT ( 'NONE',  ( 2.507384923554911715, -52.08333333333332149, 26.16266358875650866 ) ) ;
#23374=FACE_OUTER_BOUND ( 'NONE', #30402, .T. ) ;
#23376=CARTESIAN_POINT ( 'NONE',  ( 4.257384923554909051, -52.75000000000000000, 32.69375250200203453 ) ) ;
#23386=CARTESIAN_POINT ( 'NONE',  ( 7.344996782761040066, -42.40485064068575838, 27.54531907653889888 ) ) ;
#23401=CARTESIAN_POINT ( 'NONE',  ( 7.567941867304902814, -42.59479166714461940, 31.10510344464368870 ) ) ;
#23408=CARTESIAN_POINT ( 'NONE',  ( 7.567941867304905479, -46.01145833381127659, 27.28240155936039812 ) ) ;
#23412=CARTESIAN_POINT ( 'NONE',  ( 6.522805344330993016, -46.01169808710153575, 31.89944360682705948 ) ) ;
#23439=CARTESIAN_POINT ( 'NONE',  ( 0.9468279798049115126, -50.26145833381128369, 31.10510344464368515 ) ) ;
#23443=CARTESIAN_POINT ( 'NONE',  ( 2.507384923554911715, -46.58333333333332149, 26.16266358875650866 ) ) ;
#23446=CARTESIAN_POINT ( 'NONE',  ( 7.051836829314712674, -49.49436610938622039, 31.35014469247091640 ) ) ;
#23452=CARTESIAN_POINT ( 'NONE',  ( 5.912663395429907709, -50.05729166714461087, 26.32672608803957459 ) ) ;
#23458=CARTESIAN_POINT ( 'NONE',  ( 7.757384923554905498, -48.74999999999998579, 29.19375250200204164 ) ) ;
#23459=CARTESIAN_POINT ( 'NONE',  ( 7.567941867304902814, -50.09895833381128227, 27.28240155936039457 ) ) ;
#23463=CARTESIAN_POINT ( 'NONE',  ( 0.7573849235549129366, -43.49999999999999289, 29.19375250200204164 ) ) ;
#23470=CARTESIAN_POINT ( 'NONE',  ( 0.7573849235549129366, -49.19375000095590167, 29.19375250200204164 ) ) ;
#23473=VECTOR ( 'NONE', #12800, 1000.000000000000000 ) ;
#23484=CARTESIAN_POINT ( 'NONE',  ( 4.257364759755165373, -44.56955858896998279, 32.69375250189113302 ) ) ;
#23498=CARTESIAN_POINT ( 'NONE',  ( 7.567941867304904591, -45.09895833381128227, 27.28240155936039812 ) ) ;
#23502=EDGE_CURVE ( 'NONE', #219, #21912, #12187, .T. ) ;
#23503=CARTESIAN_POINT ( 'NONE',  ( 0.9468279798049125118, -47.30312500047795510, 29.19375250200204164 ) ) ;
#23510=CARTESIAN_POINT ( 'NONE',  ( 7.757384923554902834, -46.32229166657106845, 31.21447844416572792 ) ) ;
#23513=ORIENTED_EDGE ( 'NONE', *, *, #24296, .F. ) ;
#23516=CARTESIAN_POINT ( 'NONE',  ( 0.7573849235549120484, -44.15208333428923737, 31.21447844416572792 ) ) ;
#23523=FACE_BOUND ( 'NONE', #1586, .T. ) ;
#23534=CARTESIAN_POINT ( 'NONE',  ( 4.446093417420686755, -51.32324111008330902, 25.69864320412302305 ) ) ;
#23547=CARTESIAN_POINT ( 'NONE',  ( 7.335449024299413701, -50.90428575981029269, 27.52242324618551095 ) ) ;
#23556=CARTESIAN_POINT ( 'NONE',  ( 4.257384923554909051, -43.92812500047795510, 25.37105061671875461 ) ) ;
#23567=CARTESIAN_POINT ( 'NONE',  ( 6.152639712747969725, -48.52215057898816042, 32.17047939175514415 ) ) ;
#23572=CARTESIAN_POINT ( 'NONE',  ( 0.8223372283228340685, -44.20836431298379665, 28.52241553216335390 ) ) ;
#23578=CARTESIAN_POINT ( 'NONE',  ( 0.7573849235549120484, -42.45833333333332860, 31.21447844416572792 ) ) ;
#23579=ORIENTED_EDGE ( 'NONE', *, *, #8672, .F. ) ;
#23581=CARTESIAN_POINT ( 'NONE',  ( 4.257384923554907274, -51.87499999999998579, 32.69375250200203453 ) ) ;
#23606=CARTESIAN_POINT ( 'NONE',  ( 6.408298810389828404, -50.01457787082797068, 31.99258616430892488 ) ) ;
#23617=CARTESIAN_POINT ( 'NONE',  ( 0.9468279798049134000, -43.34479166714461940, 27.28240155936039102 ) ) ;
#23622=CARTESIAN_POINT ( 'NONE',  ( 5.912663395429905044, -46.63645833381128369, 32.06077891596451224 ) ) ;
#23626=CARTESIAN_POINT ( 'NONE',  ( 3.319562750045992328, -47.10267090063072004, 25.69375250200203453 ) ) ;
#23652=CARTESIAN_POINT ( 'NONE',  ( 5.195207097063836876, -44.14732909936924443, 25.69375250200204519 ) ) ;
#23656=CARTESIAN_POINT ( 'NONE',  ( 4.257384923554909051, -47.42812500047794799, 25.37105061671875461 ) ) ;
#23661=CARTESIAN_POINT ( 'NONE',  ( 6.007384923554904610, -46.83333333333332149, 32.22484141524757462 ) ) ;
#23667=CARTESIAN_POINT ( 'NONE',  ( 2.602106451679909505, -50.30729166714461087, 32.06077891596451224 ) ) ;
#23673=CARTESIAN_POINT ( 'NONE',  ( 0.7573849235549129366, -47.49999999999999289, 29.19375250200204164 ) ) ;
#23674=CARTESIAN_POINT ( 'NONE',  ( 5.912663395429904156, -49.72395833381128227, 32.06077891596451224 ) ) ;
#23677=CARTESIAN_POINT ( 'NONE',  ( 1.210729646013019467, -43.15252005745412589, 30.92316582435874395 ) ) ;
#23684=CARTESIAN_POINT ( 'NONE',  ( 0.7573849235549120484, -49.65208333428923737, 31.21447844416572792 ) ) ;
#23697=CARTESIAN_POINT ( 'NONE',  ( 0.9927756815795603096, -44.66403625184968007, 30.52993340218751328 ) ) ;
#23698=CARTESIAN_POINT ( 'NONE',  ( 7.757384923554902834, -42.48541666762258018, 31.21447844416572792 ) ) ;
#23710=CARTESIAN_POINT ( 'NONE',  ( 0.9468279798049132889, -46.39062500047794657, 29.19375250200204164 ) ) ;
#23719=CARTESIAN_POINT ( 'NONE',  ( 0.7573849235549138248, -45.07229166657106845, 27.17302655983835180 ) ) ;
#23721=ORIENTED_EDGE ( 'NONE', *, *, #3250, .T. ) ;
#23726=CARTESIAN_POINT ( 'NONE',  ( 7.757384923554905498, -42.94375000095590167, 29.19375250200204164 ) ) ;
#23732=LINE ( 'NONE', #4577, #39336 ) ;
#23741=CARTESIAN_POINT ( 'NONE',  ( 6.007384923554907274, -48.16666666666665719, 26.16266358875650866 ) ) ;
#23751=FACE_OUTER_BOUND ( 'NONE', #38252, .T. ) ;
#23761=CARTESIAN_POINT ( 'NONE',  ( 0.9468279798049125118, -43.30312500047794799, 29.19375250200204164 ) ) ;
#23768=CARTESIAN_POINT ( 'NONE',  ( 6.105366254384113844, -47.86179344348839493, 26.18249806516812939 ) ) ;
#23770=CARTESIAN_POINT ( 'NONE',  ( 1.435889866288661665, -42.40496264135119020, 27.10347114741821883 ) ) ;
#23771=ORIENTED_EDGE ( 'NONE', *, *, #19953, .T. ) ;
#23773=ORIENTED_EDGE ( 'NONE', *, *, #27234, .T. ) ;
#23776=CARTESIAN_POINT ( 'NONE',  ( 0.7624856087582783104, -50.18750275011162643, 29.51951775954584889 ) ) ;
#23780=CARTESIAN_POINT ( 'NONE',  ( 7.757384923554904610, -50.20833333333332860, 27.17302655983835180 ) ) ;
#23782=CARTESIAN_POINT ( 'NONE',  ( 0.7573849235549120484, -48.15208333428924448, 31.21447844416572792 ) ) ;
#23784=CARTESIAN_POINT ( 'NONE',  ( 2.602106451679912169, -42.47395833381127517, 26.32672608803957459 ) ) ;
#23798=CARTESIAN_POINT ( 'NONE',  ( 2.507384923554911715, -44.08333333333332149, 26.16266358875650866 ) ) ;
#23805=CARTESIAN_POINT ( 'NONE',  ( 5.051387889499492800, -42.83724721580873052, 25.77596420562224466 ) ) ;
#23810=CARTESIAN_POINT ( 'NONE',  ( 1.455411836537591874, -47.64140197283645506, 31.34072780320230933 ) ) ;
#23828=EDGE_CURVE ( 'NONE', #27947, #40028, #35319, .T. ) ;
#23836=CARTESIAN_POINT ( 'NONE',  ( 7.567941867304904591, -45.09479166714461940, 31.10510344464368870 ) ) ;
#23842=EDGE_LOOP ( 'NONE', ( #4605, #2099, #31847, #38098 ) ) ;
#23844=ORIENTED_EDGE ( 'NONE', *, *, #5633, .T. ) ;
#23848=B_SPLINE_CURVE_WITH_KNOTS ( 'NONE', 3,
 ( #2354, #25327, #34888, #9151, #5755, #41066, #37871, #18732, #21297, #18519, #28294, #34266, #25117, #35733, #39325, #25747, #32117, #38503, #39122, #28921, #3197, #32532, #2982, #22540, #38713, #13393, #6595, #13184, #10001 ),
 .UNSPECIFIED., .F., .F.,
 ( 4, 2, 1, 1, 1, 1, 1, 2, 2, 2, 2, 2, 2, 2, 2, 2, 4 ),
 ( 0.9268204210416536304, 0.9268328197228067333, 0.9268452184039597253, 0.9268700157662659311, 0.9269196104908782319, 0.9270187999401028334, 0.9272171788385519253, 0.9276139366354503313, 0.9284074522292469211, 0.9299944834168402119, 0.9331685457920267934, 0.9363426081672133749, 0.9395166705424000675, 0.9426907329175866490, 0.9458647952927732305, 0.9490388576679598120, 0.9522129200431463936 ),
 .UNSPECIFIED. ) ;
#23870=CARTESIAN_POINT ( 'NONE',  ( 7.567941867304904591, -48.09479166714461229, 31.10510344464368870 ) ) ;
#23874=CARTESIAN_POINT ( 'NONE',  ( 0.7573849235549120484, -43.45833333333332149, 31.21447844416572792 ) ) ;
#23878=ORIENTED_EDGE ( 'NONE', *, *, #41299, .F. ) ;
#23879=CARTESIAN_POINT ( 'NONE',  ( 5.912663395429904156, -45.72395833381128227, 32.06077891596451224 ) ) ;
#23884=ADVANCED_FACE ( 'NONE', ( #12713 ), #38654, .T. ) ;
#23887=CARTESIAN_POINT ( 'NONE',  ( 7.757384923554904610, -47.20833333333332860, 27.17302655983835180 ) ) ;
#23888=CARTESIAN_POINT ( 'NONE',  ( 4.257384923554909051, -51.51562500047794657, 25.37105061671875106 ) ) ;
#23889=B_SPLINE_CURVE_WITH_KNOTS ( 'NONE', 3,
 ( #24285, #1527, #20463, #30241, #33853, #4714, #33655, #14295, #40445, #897, #37257, #8112, #21089, #677, #36411, #17059, #30026, #13867, #26847, #24704 ),
 .UNSPECIFIED., .F., .F.,
 ( 4, 2, 2, 2, 2, 2, 2, 2, 2, 4 ),
 ( 0.2666204305212847570, 0.2700049220607576017, 0.2733894136002304465, 0.2767739051397032912, 0.2801583966791761360, 0.2835428882186489807, 0.2869273797581218255, 0.2903118712975946702, 0.2920041170673311481, 0.2936963628370675705 ),
 .UNSPECIFIED. ) ;
#23899=CARTESIAN_POINT ( 'NONE',  ( 0.7573849235549120484, -50.15208333428924448, 31.21447844416572792 ) ) ;
#23907=CARTESIAN_POINT ( 'NONE',  ( 4.257393643264853367, -45.06839824424229590, 32.69375250198117300 ) ) ;
#23910=CARTESIAN_POINT ( 'NONE',  ( 4.249084771485784451, -44.81856288079163875, 25.69375986587636973 ) ) ;
#23924=CARTESIAN_POINT ( 'NONE',  ( 7.567941867304904591, -42.64062500047794657, 29.19375250200204164 ) ) ;
#23929=( BOUNDED_CURVE ( )  B_SPLINE_CURVE ( 2, ( #8696, #27236, #8490, #40198, #37428, #21669, #21053, #11269, #17863 ),
 .UNSPECIFIED., .F., .F. ) 
 B_SPLINE_CURVE_WITH_KNOTS ( ( 3, 2, 2, 2, 3 ),
 ( 0.7375000000000000444, 0.7416666666666666963, 0.7500000000000000000, 0.7583333333333333037, 0.7624999999999999556 ),
 .UNSPECIFIED. ) 
 CURVE ( )  GEOMETRIC_REPRESENTATION_ITEM ( )  RATIONAL_B_SPLINE_CURVE ( ( 0.9330127018922194093, 0.9330127018922202975, 1.000000000000000000, 0.8660254037844387076, 1.000000000000000000, 0.8660254037844387076, 1.000000000000000000, 0.9330127018922202975, 0.9330127018922194093 ) ) 
 REPRESENTATION_ITEM ( '' )  );
#23930=EDGE_LOOP ( 'NONE', ( #31910, #6563, #36471 ) ) ;
#23933=CARTESIAN_POINT ( 'NONE',  ( 2.507384923554911715, -46.11395833323773275, 26.16266358875650866 ) ) ;
#23942=CARTESIAN_POINT ( 'NONE',  ( 0.7573849235549120484, -44.65208333428923737, 31.21447844416572792 ) ) ;
#23957=CARTESIAN_POINT ( 'NONE',  ( 6.749094258712378114, -51.50448782472152942, 31.69401048956089184 ) ) ;
#23980=CARTESIAN_POINT ( 'NONE',  ( 5.912663395429907709, -43.96979166714461940, 26.32672608803957459 ) ) ;
#23988=CARTESIAN_POINT ( 'NONE',  ( 5.327914056370817164, -48.54315607333396088, 32.53361639126823235 ) ) ;
#23993=LINE ( 'NONE', #1432, #9693 ) ;
#23997=CARTESIAN_POINT ( 'NONE',  ( 5.195207097063835988, -50.35267090063074136, 32.69375250200204164 ) ) ;
#23999=CARTESIAN_POINT ( 'NONE',  ( 0.7573849235549129366, -48.19375000095590877, 29.19375250200204164 ) ) ;
#24006=DIRECTION ( 'NONE',  ( 0.000000000000000000, 0.000000000000000000, -1.000000000000000000 ) ) ;
#24008=CARTESIAN_POINT ( 'NONE',  ( 3.319562750045980337, -45.10267090063072715, 25.69375250200204519 ) ) ;
#24039=DIRECTION ( 'NONE',  ( -0.000000000000000000, -1.000000000000000000, -0.000000000000000000 ) ) ;
#24048=CARTESIAN_POINT ( 'NONE',  ( 5.912663395429907709, -46.46979166714461229, 26.32672608803957459 ) ) ;
#24081=CARTESIAN_POINT ( 'NONE',  ( 0.9468279798049125118, -49.80312500047794799, 29.19375250200204164 ) ) ;
#24085=CARTESIAN_POINT ( 'NONE',  ( 2.507384923554909495, -43.91666666666665719, 32.22484141524756751 ) ) ;
#24087=CARTESIAN_POINT ( 'NONE',  ( 6.404222161650433343, -49.51496166531647702, 31.99555167500608377 ) ) ;
#24091=VERTEX_POINT ( 'NONE', #27058 ) ;
#24092=CARTESIAN_POINT ( 'NONE',  ( 4.257384923554909051, -46.01562500047794657, 25.37105061671875461 ) ) ;
#24095=DIRECTION ( 'NONE',  ( 0.8956692225370903593, 0.000000000000000000, 0.4447208605404113779 ) ) ;
#24099=CARTESIAN_POINT ( 'NONE',  ( 7.757384923554905498, -46.74999999999999289, 29.19375250200204164 ) ) ;
#24100=CARTESIAN_POINT ( 'NONE',  ( 2.602106451679909505, -50.30729166714461087, 32.06077891596451224 ) ) ;
#24109=CARTESIAN_POINT ( 'NONE',  ( 0.7573849235549138248, -47.73541666762256597, 27.17302655983835180 ) ) ;
#24112=DIRECTION ( 'NONE',  ( 0.000000000000000000, 0.000000000000000000, 1.000000000000000000 ) ) ;
#24120=CARTESIAN_POINT ( 'NONE',  ( 4.257384923554909051, 5.249999999999997335, 29.19375250200204164 ) ) ;
#24123=CARTESIAN_POINT ( 'NONE',  ( 2.357287238234218041, -44.61542465251431366, 32.16301803315884200 ) ) ;
#24125=VECTOR ( 'NONE', #12434, 1000.000000000000000 ) ;
#24127=CARTESIAN_POINT ( 'NONE',  ( 1.201898370969856966, -49.65240414396737378, 30.96129920447186379 ) ) ;
#24139=CARTESIAN_POINT ( 'NONE',  ( 5.912663395429907709, -43.55729166714461797, 26.32672608803957459 ) ) ;
#24145=EDGE_CURVE ( 'NONE', #3413, #32591, #23889, .T. ) ;
#24146=VECTOR ( 'NONE', #29312, 1000.000000000000000 ) ;
#24149=CARTESIAN_POINT ( 'NONE',  ( 2.507384923554909495, -44.94729166657106845, 32.22484141524756751 ) ) ;
#24152=ORIENTED_EDGE ( 'NONE', *, *, #29294, .F. ) ;
#24155=CARTESIAN_POINT ( 'NONE',  ( 4.257384923554908163, -50.17812500047794799, 33.01645438728532866 ) ) ;
#24168=CARTESIAN_POINT ( 'NONE',  ( 4.260921609194730841, -51.31883420771185200, 25.69375246800021273 ) ) ;
#24170=CARTESIAN_POINT ( 'NONE',  ( 7.757384923554902834, -48.29166666666665009, 31.21447844416572792 ) ) ;
#24179=CARTESIAN_POINT ( 'NONE',  ( 4.257384923554909051, -42.40485061181025372, 34.19375250200204164 ) ) ;
#24189=CARTESIAN_POINT ( 'NONE',  ( 2.602106451679909505, -49.30729166714461087, 32.06077891596451224 ) ) ;
#24193=DIRECTION ( 'NONE',  ( 0.000000000000000000, 0.000000000000000000, -1.000000000000000000 ) ) ;
#24203=B_SPLINE_CURVE_WITH_KNOTS ( 'NONE', 1,
 ( #32135, #32545 ),
 .UNSPECIFIED., .F., .F.,
 ( 2, 2 ),
 ( 0.000000000000000000, 1.000000000000000000 ),
 .UNSPECIFIED. ) ;
#24207=CARTESIAN_POINT ( 'NONE',  ( 0.7573849235549120484, -50.65208333428923737, 31.21447844416572792 ) ) ;
#24208=CARTESIAN_POINT ( 'NONE',  ( 0.9468279798049132889, -43.89062500047794657, 29.19375250200204164 ) ) ;
#24230=CARTESIAN_POINT ( 'NONE',  ( 0.7573849235549120484, -48.95833333333333570, 31.21447844416572792 ) ) ;
#24249=CARTESIAN_POINT ( 'NONE',  ( 0.9468279798049115126, -45.26145833381127659, 31.10510344464368515 ) ) ;
#24255=VERTEX_POINT ( 'NONE', #38082 ) ;
#24278=CARTESIAN_POINT ( 'NONE',  ( 4.257384923554909051, -49.42812500047794799, 25.37105061671875461 ) ) ;
#24282=CARTESIAN_POINT ( 'NONE',  ( 7.757384923554902834, -44.29166666666665719, 31.21447844416572792 ) ) ;
#24283=ORIENTED_EDGE ( 'NONE', *, *, #33735, .T. ) ;
#24285=CARTESIAN_POINT ( 'NONE',  ( 4.257284565358973261, -49.31874761147663833, 25.69375250344087291 ) ) ;
#24288=CARTESIAN_POINT ( 'NONE',  ( 5.912663395429907709, -46.55729166714461087, 26.32672608803957459 ) ) ;
#24289=CARTESIAN_POINT ( 'NONE',  ( 4.257384923554908163, -48.17812500047794799, 33.01645438728532866 ) ) ;
#24294=CYLINDRICAL_SURFACE ( 'NONE', #33362, 3.499999999999996003 ) ;
#24295=DIRECTION ( 'NONE',  ( -0.000000000000000000, -1.000000000000000000, -0.000000000000000000 ) ) ;
#24296=EDGE_CURVE ( 'NONE', #29198, #16800, #15546, .T. ) ;
#24299=CARTESIAN_POINT ( 'NONE',  ( 6.007384923554907274, -47.66666666666665719, 26.16266358875650866 ) ) ;
#24300=CARTESIAN_POINT ( 'NONE',  ( 2.602106451679912169, -47.47395833381128227, 26.32672608803957459 ) ) ;
#24311=CARTESIAN_POINT ( 'NONE',  ( 0.7573849235549129366, -48.19375000095590877, 29.19375250200204164 ) ) ;
#24313=( NAMED_UNIT ( * ) SI_UNIT ( $, .STERADIAN. ) SOLID_ANGLE_UNIT ( ) );
#24321=CARTESIAN_POINT ( 'NONE',  ( 6.408309945129365026, -44.87045204157330858, 26.39492752045774537 ) ) ;
#24327=CARTESIAN_POINT ( 'NONE',  ( 3.340572058277928136, -49.79840967281799635, 25.78498827011404515 ) ) ;
#24336=CARTESIAN_POINT ( 'NONE',  ( 4.466478085302152401, -43.82372839456512992, 25.69375745011282319 ) ) ;
#24348=CARTESIAN_POINT ( 'NONE',  ( 6.007384923554904610, -46.36395833323773275, 32.22484141524757462 ) ) ;
#24350=VERTEX_POINT ( 'NONE', #12554 ) ;
#24353=CARTESIAN_POINT ( 'NONE',  ( 2.602106451679911281, -51.38645833381127659, 26.32672608803957459 ) ) ;
#24354=LINE ( 'NONE', #36691, #40122 ) ;
#24379=CARTESIAN_POINT ( 'NONE',  ( 0.7573849235549120484, -49.45833333333333570, 31.21447844416572792 ) ) ;
#24386=CARTESIAN_POINT ( 'NONE',  ( 4.257384923554909051, -51.51562500047793947, 25.37105061671875461 ) ) ;
#24388=CARTESIAN_POINT ( 'NONE',  ( 5.195207097063835988, -47.85267090063072715, 32.69375250200204164 ) ) ;
#24406=CARTESIAN_POINT ( 'NONE',  ( 7.757384923554904610, -49.90208333428923737, 27.17302655983835180 ) ) ;
#24408=CARTESIAN_POINT ( 'NONE',  ( 2.602106451679909505, -42.30729166714461087, 32.06077891596451224 ) ) ;
#24424=DIRECTION ( 'NONE',  ( 0.000000000000000000, 0.000000000000000000, -1.000000000000000000 ) ) ;
#24434=CARTESIAN_POINT ( 'NONE',  ( 3.798521328130547214, -47.57850925890978999, 32.69375254844991474 ) ) ;
#24455=CARTESIAN_POINT ( 'NONE',  ( 4.257384923554909051, -42.92812500047794799, 25.37105061671875461 ) ) ;
#24459=LINE ( 'NONE', #21260, #34303 ) ;
#24463=ORIENTED_EDGE ( 'NONE', *, *, #9575, .F. ) ;
#24471=CARTESIAN_POINT ( 'NONE',  ( 4.257384923554909051, -45.62499999999999289, 25.69375250200204519 ) ) ;
#24486=CARTESIAN_POINT ( 'NONE',  ( 7.567941867304905479, -49.51145833381128369, 27.28240155936039812 ) ) ;
#24491=CARTESIAN_POINT ( 'NONE',  ( 0.7573849235549138248, -45.54166666666666430, 27.17302655983835180 ) ) ;
#24493=CARTESIAN_POINT ( 'NONE',  ( 4.474090282365028592, -49.32390421275025005, 25.69950969705324439 ) ) ;
#24497=CARTESIAN_POINT ( 'NONE',  ( 2.602106451679909505, -47.80729166714461087, 32.06077891596451224 ) ) ;
#24498=CARTESIAN_POINT ( 'NONE',  ( 4.257384923554909051, -48.92812500047794799, 25.37105061671875106 ) ) ;
#24502=FACE_OUTER_BOUND ( 'NONE', #22033, .T. ) ;
#24505=CARTESIAN_POINT ( 'NONE',  ( 4.630631976088899648, 3.250000000000000444, 35.13541431052434660 ) ) ;
#24506=CARTESIAN_POINT ( 'NONE',  ( 0.7573849235549120484, -45.45833333333332149, 31.21447844416572792 ) ) ;
#24507=CARTESIAN_POINT ( 'NONE',  ( 5.912663395429904156, -48.72395833381128227, 32.06077891596451224 ) ) ;
#24517=CARTESIAN_POINT ( 'NONE',  ( 0.7573849235549138248, -47.23541666762257307, 27.17302655983835180 ) ) ;
#24545=CARTESIAN_POINT ( 'NONE',  ( 0.9468279798049124008, -43.34895833381126806, 31.10510344464368515 ) ) ;
#24554=CARTESIAN_POINT ( 'NONE',  ( 6.007384923554907274, -43.19729166657106845, 26.16266358875650866 ) ) ;
#24559=CARTESIAN_POINT ( 'NONE',  ( 2.327074468158384590, -43.61500650186889771, 32.12301660902779332 ) ) ;
#24562=CARTESIAN_POINT ( 'NONE',  ( 4.257384923554909051, -51.92812500047794799, 25.37105061671875461 ) ) ;
#24564=ORIENTED_EDGE ( 'NONE', *, *, #983, .F. ) ;
#24579=ADVANCED_FACE ( 'NONE', ( #11055 ), #33811, .T. ) ;
#24596=CARTESIAN_POINT ( 'NONE',  ( 7.567941867304904591, -50.59895833381128227, 27.28240155936039812 ) ) ;
#24606=ORIENTED_EDGE ( 'NONE', *, *, #35649, .T. ) ;
#24607=CARTESIAN_POINT ( 'NONE',  ( 7.757384923554902834, -51.32229166657106845, 31.21447844416572792 ) ) ;
#24613=CARTESIAN_POINT ( 'NONE',  ( 6.007384923554904610, -50.33333333333332860, 32.22484141524757462 ) ) ;
#24615=FACE_OUTER_BOUND ( 'NONE', #5650, .T. ) ;
#24617=CARTESIAN_POINT ( 'NONE',  ( 7.757384923554902834, -48.98541666762257307, 31.21447844416572792 ) ) ;
#24622=CARTESIAN_POINT ( 'NONE',  ( 4.257384923554909051, -52.75000000000000000, 32.69375250200203453 ) ) ;
#24625=( GEOMETRIC_REPRESENTATION_CONTEXT ( 3 ) GLOBAL_UNCERTAINTY_ASSIGNED_CONTEXT ( ( #39052 ) ) GLOBAL_UNIT_ASSIGNED_CONTEXT ( ( #26884, #36662, #24745 ) ) REPRESENTATION_CONTEXT ( 'NONE', 'WORKASPACE' ) );
#24645=CARTESIAN_POINT ( 'NONE',  ( 4.257384923554919709, -48.87499999999998579, 32.69375250200203453 ) ) ;
#24649=CYLINDRICAL_SURFACE ( 'NONE', #28699, 3.499999999999996003 ) ;
#24658=CIRCLE ( 'NONE', #35512, 10.16127960363519200 ) ;
#24668=EDGE_CURVE ( 'NONE', #16800, #22457, #35940, .T. ) ;
#24669=CARTESIAN_POINT ( 'NONE',  ( 5.912663395429905044, -43.13645833381128369, 32.06077891596451224 ) ) ;
#24676=ORIENTED_EDGE ( 'NONE', *, *, #26428, .T. ) ;
#24697=CARTESIAN_POINT ( 'NONE',  ( 2.602106451679911281, -46.38645833381128369, 26.32672608803957459 ) ) ;
#24701=FACE_OUTER_BOUND ( 'NONE', #23930, .T. ) ;
#24702=CARTESIAN_POINT ( 'NONE',  ( 6.007384923554904610, -44.33333333333332149, 32.22484141524757462 ) ) ;
#24704=CARTESIAN_POINT ( 'NONE',  ( 4.257388422463325384, -49.06861128833901375, 32.69375250199872340 ) ) ;
#24706=CARTESIAN_POINT ( 'NONE',  ( 7.567941867304904591, -46.59895833381128227, 27.28240155936039812 ) ) ;
#24709=CARTESIAN_POINT ( 'NONE',  ( 7.567941867304905479, -48.01145833381128369, 27.28240155936039457 ) ) ;
#24718=CARTESIAN_POINT ( 'NONE',  ( 6.007384923554907274, -44.66666666666665719, 26.16266358875650866 ) ) ;
#24719=CARTESIAN_POINT ( 'NONE',  ( 7.567941867304904591, -47.64062500047794657, 29.19375250200204164 ) ) ;
#24726=DIRECTION ( 'NONE',  ( -0.000000000000000000, -1.000000000000000000, -0.000000000000000000 ) ) ;
#24730=CARTESIAN_POINT ( 'NONE',  ( 4.257384923554908163, -48.06875000095591588, 33.23520438632941421 ) ) ;
#24745=( NAMED_UNIT ( * ) SI_UNIT ( $, .STERADIAN. ) SOLID_ANGLE_UNIT ( ) );
#24746=CARTESIAN_POINT ( 'NONE',  ( 4.257384923554909051, -52.75000000000000000, 25.69375250200204519 ) ) ;
#24761=CARTESIAN_POINT ( 'NONE',  ( 4.257369266595627977, -50.56937335658698629, 32.69375250193562721 ) ) ;
#24765=CARTESIAN_POINT ( 'NONE',  ( 5.956679180686003328, -44.53036646474713223, 32.27154590803652923 ) ) ;
#24769=CARTESIAN_POINT ( 'NONE',  ( 7.757384923554902834, -43.32229166657107555, 31.21447844416572792 ) ) ;
#24773=CARTESIAN_POINT ( 'NONE',  ( 1.758707139541242581, -43.63051132904563190, 31.69042147953313915 ) ) ;
#24775=CARTESIAN_POINT ( 'NONE',  ( 7.757384923554904610, -42.40208333428923737, 27.17302655983835180 ) ) ;
#24777=CARTESIAN_POINT ( 'NONE',  ( 6.007384923554907274, -51.66666666666665719, 26.16266358875650866 ) ) ;
#24802=CARTESIAN_POINT ( 'NONE',  ( 7.757384923554905498, -49.74999999999998579, 29.19375250200204164 ) ) ;
#24807=ORIENTED_EDGE ( 'NONE', *, *, #6920, .T. ) ;
#24810=CARTESIAN_POINT ( 'NONE',  ( 5.912663395429904156, -49.72395833381128227, 32.06077891596451224 ) ) ;
#24823=CARTESIAN_POINT ( 'NONE',  ( 0.7573849235549129366, -51.53062499990439704, 29.19375250200204164 ) ) ;
#24831=CARTESIAN_POINT ( 'NONE',  ( 6.007384923554904610, -47.52708333428923737, 32.22484141524757462 ) ) ;
#24836=CARTESIAN_POINT ( 'NONE',  ( 3.928057110000706675, -46.81093971469515935, 25.70857008654676790 ) ) ;
#24846=CARTESIAN_POINT ( 'NONE',  ( 4.257384923554909051, -52.12499999999999289, 25.69375250200204519 ) ) ;
#24875=CARTESIAN_POINT ( 'NONE',  ( 4.257384923554908163, -43.17812500047794799, 33.01645438728532866 ) ) ;
#24890=DIRECTION ( 'NONE',  ( -0.000000000000000000, -1.000000000000000000, -0.000000000000000000 ) ) ;
#24898=CARTESIAN_POINT ( 'NONE',  ( 4.257406269681411004, -45.56789735307413736, 32.69375250187820825 ) ) ;
#24910=CARTESIAN_POINT ( 'NONE',  ( 7.344996782761040066, -42.40485064068575838, 27.54531907653889888 ) ) ;
#24915=CARTESIAN_POINT ( 'NONE',  ( 4.257384923554908163, -42.76562500047794657, 33.01645438728532866 ) ) ;
#24917=CARTESIAN_POINT ( 'NONE',  ( 5.912663395429905044, -44.13645833381129080, 32.06077891596451224 ) ) ;
#24926=CARTESIAN_POINT ( 'NONE',  ( 6.007384923554904610, -45.83333333333332149, 32.22484141524757462 ) ) ;
#24927=CARTESIAN_POINT ( 'NONE',  ( 2.602106451679909505, -47.30729166714461087, 32.06077891596451224 ) ) ;
#24929=CYLINDRICAL_SURFACE ( 'NONE', #28046, 10.16127960363519200 ) ;
#24931=EDGE_CURVE ( 'NONE', #16017, #26970, #13210, .T. ) ;
#24934=EDGE_CURVE ( 'NONE', #29243, #40134, #9139, .T. ) ;
#24940=CARTESIAN_POINT ( 'NONE',  ( 7.757384923554904610, -46.40208333428924448, 27.17302655983835180 ) ) ;
#24946=EDGE_CURVE ( 'NONE', #8437, #19510, #6966, .T. ) ;
#24955=PLANE ( 'NONE',  #851 ) ;
#24965=CARTESIAN_POINT ( 'NONE',  ( 6.007384923554904610, -48.83333333333332860, 32.22484141524757462 ) ) ;
#24970=CARTESIAN_POINT ( 'NONE',  ( 7.567941867304904591, -50.64062500047794657, 29.19375250200204164 ) ) ;
#24976=ADVANCED_FACE ( 'NONE', ( #17595 ), #11213, .T. ) ;
#24977=CARTESIAN_POINT ( 'NONE',  ( 4.257384923554908163, -43.40562499990440415, 33.23520438632941421 ) ) ;
#24982=CARTESIAN_POINT ( 'NONE',  ( 4.257384923554907274, -43.87499999999999289, 32.69375250200203453 ) ) ;
#24983=CARTESIAN_POINT ( 'NONE',  ( 2.975074317980819671, -42.09928120585051659, 32.45038872836079236 ) ) ;
#25002=CARTESIAN_POINT ( 'NONE',  ( 3.319562750045980337, -46.60267090063073425, 25.69375250200204519 ) ) ;
#25013=VECTOR ( 'NONE', #21335, 1000.000000000000000 ) ;
#25016=CARTESIAN_POINT ( 'NONE',  ( 0.9468279798049124008, -51.34895833381127517, 31.10510344464368515 ) ) ;
#25023=EDGE_LOOP ( 'NONE', ( #1829, #19113, #26999, #7397 ) ) ;
#25027=CARTESIAN_POINT ( 'NONE',  ( 4.257384923554908163, -51.40562499990439704, 33.23520438632941421 ) ) ;
#25033=CARTESIAN_POINT ( 'NONE',  ( 7.758818148817964833, -42.44274674358672428, 29.14466722536933929 ) ) ;
#25034=CARTESIAN_POINT ( 'NONE',  ( 7.757384923554904610, -47.40208333428923737, 27.17302655983835180 ) ) ;
#25037=CYLINDRICAL_SURFACE ( 'NONE', #1789, 3.499999999999996003 ) ;
#25046=( BOUNDED_CURVE ( )  B_SPLINE_CURVE ( 1, ( #31629, #5690 ),
 .UNSPECIFIED., .F., .T. ) 
 B_SPLINE_CURVE_WITH_KNOTS ( ( 2, 2 ),
 ( 0.000000000000000000, 1.000000000000000000 ),
 .UNSPECIFIED. ) 
 CURVE ( )  GEOMETRIC_REPRESENTATION_ITEM ( )  RATIONAL_B_SPLINE_CURVE ( ( 0.9666183089693827224, 0.9666183089693827224 ) ) 
 REPRESENTATION_ITEM ( '' )  );
#25061=CARTESIAN_POINT ( 'NONE',  ( 3.708850978226579720, -48.30635022852703031, 25.73525105580526429 ) ) ;
#25063=EDGE_CURVE ( 'NONE', #24091, #8437, #22120, .T. ) ;
#25072=DIRECTION ( 'NONE',  ( -0.000000000000000000, -1.000000000000000000, -0.000000000000000000 ) ) ;
#25080=CARTESIAN_POINT ( 'NONE',  ( 2.602106451679911281, -42.88645833381128369, 26.32672608803957459 ) ) ;
#25097=ADVANCED_FACE ( 'NONE', ( #35092 ), #25951, .F. ) ;
#25114=CARTESIAN_POINT ( 'NONE',  ( 4.257384923554909051, -42.62499999999998579, 25.15230061767466552 ) ) ;
#25117=CARTESIAN_POINT ( 'NONE',  ( 3.106756894555131154, -42.79106943002106078, 25.87600656864968940 ) ) ;
#25120=CARTESIAN_POINT ( 'NONE',  ( 0.9468279798049132889, -44.89062500047794657, 29.19375250200204164 ) ) ;
#25121=CARTESIAN_POINT ( 'NONE',  ( 0.9468279798049125118, -46.30312500047794799, 29.19375250200204164 ) ) ;
#25128=AXIS2_PLACEMENT_3D ( 'NONE', #22073, #35044, #18879 ) ;
#25131=CARTESIAN_POINT ( 'NONE',  ( 0.7573849235549120484, -43.95833333333332149, 31.21447844416572792 ) ) ;
#25132=CARTESIAN_POINT ( 'NONE',  ( 5.912663395429907709, -47.05729166714461087, 26.32672608803957459 ) ) ;
#25144=CARTESIAN_POINT ( 'NONE',  ( 2.507384923554911715, -45.77708333428923737, 26.16266358875650866 ) ) ;
#25146=VECTOR ( 'NONE', #30754, 1000.000000000000114 ) ;
#25168=CARTESIAN_POINT ( 'NONE',  ( 4.257384923554909051, -52.75000000000000000, 29.19375250200204164 ) ) ;
#25169=CARTESIAN_POINT ( 'NONE',  ( 6.007384923554904610, -49.33333333333332860, 32.22484141524757462 ) ) ;
#25174=DIRECTION ( 'NONE',  ( -0.000000000000000000, -1.000000000000000000, -0.000000000000000000 ) ) ;
#25178=CARTESIAN_POINT ( 'NONE',  ( 4.257384923554908163, -51.76562500047794657, 33.01645438728532866 ) ) ;
#25186=CARTESIAN_POINT ( 'NONE',  ( 6.007384923554907274, -52.16666666666665719, 26.16266358875650866 ) ) ;
#25190=ORIENTED_EDGE ( 'NONE', *, *, #22454, .T. ) ;
#25191=CARTESIAN_POINT ( 'NONE',  ( 4.042262034348572897, -43.81363054781109412, 25.69942139003217463 ) ) ;
#25193=CARTESIAN_POINT ( 'NONE',  ( 2.602106451679909505, -47.71979166714461229, 32.06077891596451224 ) ) ;
#25198=CARTESIAN_POINT ( 'NONE',  ( 4.257384923554931255, -44.87499999999998579, 32.69375250200203453 ) ) ;
#25221=CARTESIAN_POINT ( 'NONE',  ( 7.567941867304902814, -47.68229166714461087, 31.10510344464368870 ) ) ;
#25225=DIRECTION ( 'NONE',  ( -0.000000000000000000, -1.000000000000000000, -0.000000000000000000 ) ) ;
#25231=CARTESIAN_POINT ( 'NONE',  ( 7.757384923554905498, -51.28062499990439704, 29.19375250200204164 ) ) ;
#25237=CARTESIAN_POINT ( 'NONE',  ( 5.083244801588882922, -42.54911808638452442, 32.61679797821260962 ) ) ;
#25238=CARTESIAN_POINT ( 'NONE',  ( 7.757384923554902834, -46.98541666762256597, 31.21447844416572792 ) ) ;
#25241=B_SPLINE_CURVE_WITH_KNOTS ( 'NONE', 3,
 ( #15903, #9298, #29473, #16727, #38640, #6724, #35664, #29689, #9508, #22469, #553, #25471, #35451, #32261, #42054, #3128, #16118, #25886 ),
 .UNSPECIFIED., .F., .F.,
 ( 4, 2, 2, 2, 2, 2, 2, 2, 4 ),
 ( 0.01269626617145068817, 0.01587030136682536854, 0.01904433656220004892, 0.02221837175757473276, 0.02539240695294941313, 0.02856644214832409351, 0.03174047734369877388, 0.03491451253907345426, 0.03808854773444813463 ),
 .UNSPECIFIED. ) ;
#25244=CARTESIAN_POINT ( 'NONE',  ( 0.8100546162232599157, -46.70685583473532887, 28.58854779002507840 ) ) ;
#25245=VECTOR ( 'NONE', #32981, 1000.000000000000000 ) ;
#25266=CARTESIAN_POINT ( 'NONE',  ( 4.257384923554909051, -52.24999999999999289, 29.19375250200204164 ) ) ;
#25267=CARTESIAN_POINT ( 'NONE',  ( 1.318558130418294505, -48.14744179591594531, 31.11822535290284719 ) ) ;
#25289=ADVANCED_FACE ( 'NONE', ( #7224 ), #26796, .T. ) ;
#25290=CARTESIAN_POINT ( 'NONE',  ( 2.602106451679909505, -42.71979166714461940, 32.06077891596451224 ) ) ;
#25291=CARTESIAN_POINT ( 'NONE',  ( 0.7573849235549120484, -42.15208333428924448, 31.21447844416572792 ) ) ;
#25310=CARTESIAN_POINT ( 'NONE',  ( 4.257384923554909051, -52.75000000000000000, 29.19375250200204164 ) ) ;
#25315=CARTESIAN_POINT ( 'NONE',  ( 1.107246976453030607, -45.65813249023252496, 30.71920075532867500 ) ) ;
#25325=CARTESIAN_POINT ( 'NONE',  ( 6.007384923554907274, -43.16666666666665719, 26.16266358875650866 ) ) ;
#25326=VERTEX_POINT ( 'NONE', #7004 ) ;
#25327=CARTESIAN_POINT ( 'NONE',  ( 4.256924955887364526, -42.81873904943027043, 25.69375249716527421 ) ) ;
#25330=CARTESIAN_POINT ( 'NONE',  ( 0.9468279798049143992, -43.93229166714461087, 27.28240155936039812 ) ) ;
#25331=CARTESIAN_POINT ( 'NONE',  ( 2.602106451679909505, -45.21979166714461940, 32.06077891596451224 ) ) ;
#25340=CARTESIAN_POINT ( 'NONE',  ( 7.757384923554902834, -51.48541666762258018, 31.21447844416572792 ) ) ;
#25341=CARTESIAN_POINT ( 'NONE',  ( 5.912663395429904156, -45.22395833381128227, 32.06077891596451224 ) ) ;
#25363=EDGE_CURVE ( 'NONE', #39859, #30827, #38068, .T. ) ;
#25380=CYLINDRICAL_SURFACE ( 'NONE', #40311, 3.499999999999996003 ) ;
#25381=CARTESIAN_POINT ( 'NONE',  ( 4.257384923554909051, -50.62499999999999289, 25.15230061767466552 ) ) ;
#25382=EDGE_LOOP ( 'NONE', ( #20157, #35107, #16394, #21619, #31602, #13600 ) ) ;
#25389=CARTESIAN_POINT ( 'NONE',  ( 4.307319872299898655, -50.31982466645489893, 25.69405780657330496 ) ) ;
#25392=CARTESIAN_POINT ( 'NONE',  ( 4.440365562216346262, -44.32310655671223998, 25.69375593653602863 ) ) ;
#25394=ORIENTED_EDGE ( 'NONE', *, *, #16569, .F. ) ;
#25395=CARTESIAN_POINT ( 'NONE',  ( 7.757384923554902834, -43.82229166657106134, 31.21447844416572792 ) ) ;
#25400=CARTESIAN_POINT ( 'NONE',  ( 0.9468279798049134000, -49.34479166714461940, 27.28240155936039457 ) ) ;
#25418=CARTESIAN_POINT ( 'NONE',  ( 2.507384923554911715, -42.58333333333332149, 26.16266358875650866 ) ) ;
#25436=CARTESIAN_POINT ( 'NONE',  ( 0.9468279798049124008, -47.34895833381128227, 31.10510344464368515 ) ) ;
#25437=FACE_BOUND ( 'NONE', #5777, .T. ) ;
#25441=CARTESIAN_POINT ( 'NONE',  ( 5.912663395429907709, -51.96979166714461940, 26.32672608803957459 ) ) ;
#25449=CARTESIAN_POINT ( 'NONE',  ( 4.257384923554909051, -51.15562499990439704, 25.15230061767466552 ) ) ;
#25451=ORIENTED_EDGE ( 'NONE', *, *, #28802, .F. ) ;
#25455=CARTESIAN_POINT ( 'NONE',  ( 0.7573849235549120484, -47.65208333428923737, 31.21447844416572792 ) ) ;
#25471=CARTESIAN_POINT ( 'NONE',  ( 1.021891431808815254, -51.66324700204889098, 30.58243428464492553 ) ) ;
#25485=CARTESIAN_POINT ( 'NONE',  ( 0.9528645021558187489, -48.16750466167951572, 30.35412302403416973 ) ) ;
#25489=CARTESIAN_POINT ( 'NONE',  ( 7.757384923554904610, -49.20833333333334281, 27.17302655983835180 ) ) ;
#25490=CARTESIAN_POINT ( 'NONE',  ( 7.567941867304904591, -46.59479166714461229, 31.10510344464368870 ) ) ;
#25493=CARTESIAN_POINT ( 'NONE',  ( 2.507384923554911715, -50.08333333333332860, 26.16266358875650866 ) ) ;
#25497=CARTESIAN_POINT ( 'NONE',  ( 4.704968455724195309, -48.05695080473028469, 32.69375236534889240 ) ) ;
#25544=CARTESIAN_POINT ( 'NONE',  ( 7.567941867304904591, -43.14062500047794657, 29.19375250200204164 ) ) ;
#25545=CARTESIAN_POINT ( 'NONE',  ( 0.9468279798049134000, -43.84479166714461940, 27.28240155936039102 ) ) ;
#25552=APPLICATION_CONTEXT ( 'automotive_design' ) ;
#25554=CARTESIAN_POINT ( 'NONE',  ( 4.965282557631612192, -42.35814529442676246, 33.23404929009055309 ) ) ;
#25555=CARTESIAN_POINT ( 'NONE',  ( 7.567941867304904591, -44.64062500047794657, 29.19375250200204164 ) ) ;
#25578=CARTESIAN_POINT ( 'NONE',  ( 4.257384923554907274, -44.37499999999999289, 32.69375250200203453 ) ) ;
#25590=CARTESIAN_POINT ( 'NONE',  ( 4.257384923554908163, -48.87499999999999289, 33.23520438632941421 ) ) ;
#25591=EDGE_LOOP ( 'NONE', ( #22331, #22702, #35842, #21443 ) ) ;
#25596=CARTESIAN_POINT ( 'NONE',  ( 5.912663395429904156, -51.22395833381127517, 32.06077891596451224 ) ) ;
#25602=CARTESIAN_POINT ( 'NONE',  ( 4.257384923554908163, -50.37499999999998579, 33.23520438632941421 ) ) ;
#25607=CARTESIAN_POINT ( 'NONE',  ( 7.567941867304904591, -48.59479166714461940, 31.10510344464368870 ) ) ;
#25610=CARTESIAN_POINT ( 'NONE',  ( 4.257443491160582738, -48.81875139542229647, 25.69375250249206744 ) ) ;
#25615=DIRECTION ( 'NONE',  ( 0.000000000000000000, 1.000000000000000000, 0.000000000000000000 ) ) ;
#25624=CARTESIAN_POINT ( 'NONE',  ( 4.257384923414707423, -42.56875000095865147, 32.69375250200203453 ) ) ;
#25645=CARTESIAN_POINT ( 'NONE',  ( 7.567941867304904591, -47.59895833381127517, 27.28240155936039812 ) ) ;
#25647=CARTESIAN_POINT ( 'NONE',  ( -1.074868669588189274, 3.250000000000000444, 26.54616302712299358 ) ) ;
#25650=CARTESIAN_POINT ( 'NONE',  ( 7.567941867304902814, -49.09479166714461940, 31.10510344464368870 ) ) ;
#25656=CARTESIAN_POINT ( 'NONE',  ( 7.757384923554904610, -47.73895833323772564, 27.17302655983835180 ) ) ;
#25662=CARTESIAN_POINT ( 'NONE',  ( 6.007384923554904610, -46.02708333428923737, 32.22484141524757462 ) ) ;
#25668=CARTESIAN_POINT ( 'NONE',  ( 4.249621227796039236, -46.81856517011009799, 25.69375887927994384 ) ) ;
#25689=CARTESIAN_POINT ( 'NONE',  ( 4.257373627235431890, -46.56920070325035255, 32.69375250196738847 ) ) ;
#25692=CARTESIAN_POINT ( 'NONE',  ( 2.565369802365478513, -48.27717615699516074, 26.09936479663073428 ) ) ;
#25695=CARTESIAN_POINT ( 'NONE',  ( 0.7703089471767631258, -46.18739773062322485, 29.49436004105545095 ) ) ;
#25696=CARTESIAN_POINT ( 'NONE',  ( 4.257384923554908163, -46.17812500047794799, 33.01645438728532866 ) ) ;
#25698=CYLINDRICAL_SURFACE ( 'NONE', #29183, 3.499999999999996003 ) ;
#25699=CARTESIAN_POINT ( 'NONE',  ( 4.257384923554909051, -52.75000000000000000, 25.69375250200204519 ) ) ;
#25705=EDGE_CURVE ( 'NONE', #22238, #6186, #20152, .T. ) ;
#25713=CARTESIAN_POINT ( 'NONE',  ( 4.027086321176827965, -50.57517120998122806, 32.69375244722802165 ) ) ;
#25747=CARTESIAN_POINT ( 'NONE',  ( 1.765745432160127359, -42.75449012074169985, 26.69342302482501950 ) ) ;
#25750=CARTESIAN_POINT ( 'NONE',  ( 5.912663395429907709, -43.05729166714461797, 26.32672608803957459 ) ) ;
#25751=CARTESIAN_POINT ( 'NONE',  ( 4.257384923554908163, -46.17812500047794799, 33.01645438728532866 ) ) ;
#25759=CARTESIAN_POINT ( 'NONE',  ( 0.9468279798049143992, -46.43229166714461087, 27.28240155936039457 ) ) ;
#25769=ORIENTED_EDGE ( 'NONE', *, *, #25363, .T. ) ;
#25779=AXIS2_PLACEMENT_3D ( 'NONE', #617, #26366, #17438 ) ;
#25792=CARTESIAN_POINT ( 'NONE',  ( 3.319562750045983890, -50.60267090063073425, 25.69375250200204519 ) ) ;
#25793=CARTESIAN_POINT ( 'NONE',  ( 6.020064490496515042, -47.36010138981654194, 26.13550782929713634 ) ) ;
#25796=CARTESIAN_POINT ( 'NONE',  ( 0.7573849235549138248, -49.54166666666665719, 27.17302655983835180 ) ) ;
#25799=VECTOR ( 'NONE', #33025, 1000.000000000000000 ) ;
#25802=CARTESIAN_POINT ( 'NONE',  ( 7.075611749087492797, -43.49718370044060123, 31.32356712241794838 ) ) ;
#25810=CARTESIAN_POINT ( 'NONE',  ( 2.507384923554909495, -49.91666666666665719, 32.22484141524756751 ) ) ;
#25814=CARTESIAN_POINT ( 'NONE',  ( 2.820144263893410663, -43.60297437004412302, 32.38510178048757382 ) ) ;
#25816=CARTESIAN_POINT ( 'NONE',  ( 5.912663395429907709, -49.46979166714461940, 26.32672608803957459 ) ) ;
#25824=VECTOR ( 'NONE', #28306, 1000.000000000000114 ) ;
#25836=CARTESIAN_POINT ( 'NONE',  ( 0.7573849235549129366, -42.49999999999998579, 29.19375250200204164 ) ) ;
#25849=ORIENTED_EDGE ( 'NONE', *, *, #5200, .F. ) ;
#25851=CARTESIAN_POINT ( 'NONE',  ( 2.602106451679912169, -47.47395833381128227, 26.32672608803957459 ) ) ;
#25857=CARTESIAN_POINT ( 'NONE',  ( 2.602106451679911281, -50.88645833381127659, 26.32672608803957459 ) ) ;
#25862=CARTESIAN_POINT ( 'NONE',  ( 0.7573849235549120484, -49.48895833323773985, 31.21447844416572792 ) ) ;
#25869=CARTESIAN_POINT ( 'NONE',  ( 2.507384923554911715, -44.77708333428923737, 26.16266358875650866 ) ) ;
#25871=ORIENTED_EDGE ( 'NONE', *, *, #27250, .T. ) ;
#25874=ADVANCED_FACE ( 'NONE', ( #6119 ), #25698, .T. ) ;
#25886=CARTESIAN_POINT ( 'NONE',  ( 4.257384918501243121, -51.56875000107599760, 32.69375250200203453 ) ) ;
#25902=CARTESIAN_POINT ( 'NONE',  ( 0.9468279798049134000, -45.34479166714461940, 27.28240155936039457 ) ) ;
#25905=DIRECTION ( 'NONE',  ( 0.000000000000000000, 0.000000000000000000, -1.000000000000000000 ) ) ;
#25909=EDGE_CURVE ( 'NONE', #14935, #9899, #9747, .T. ) ;
#25913=CIRCLE ( 'NONE', #5516, 8.161279603635190227 ) ;
#25914=CARTESIAN_POINT ( 'NONE',  ( 6.009358330555831351, -48.02703704610012636, 32.22391843402733258 ) ) ;
#25923=( BOUNDED_CURVE ( )  B_SPLINE_CURVE ( 2, ( #29541, #17001, #13173, #16585, #9990, #13382, #406, #26362, #7000 ),
 .UNSPECIFIED., .F., .T. ) 
 B_SPLINE_CURVE_WITH_KNOTS ( ( 3, 2, 2, 2, 3 ),
 ( 0.4125000000000000333, 0.4166666666666666852, 0.4249999999999999889, 0.4333333333333333481, 0.4375000000000000000 ),
 .UNSPECIFIED. ) 
 CURVE ( )  GEOMETRIC_REPRESENTATION_ITEM ( )  RATIONAL_B_SPLINE_CURVE ( ( 0.9330127018922194093, 0.9330127018922198534, 1.000000000000000000, 0.8660254037844387076, 1.000000000000000000, 0.8660254037844387076, 1.000000000000000000, 0.9330127018922194093, 0.9330127018922194093 ) ) 
 REPRESENTATION_ITEM ( '' )  );
#25927=CARTESIAN_POINT ( 'NONE',  ( 2.975064734268261457, -42.40508397444173738, 32.45039488375558534 ) ) ;
#25931=EDGE_CURVE ( 'NONE', #32848, #40028, #39708, .T. ) ;
#25947=CARTESIAN_POINT ( 'NONE',  ( 4.257385003886612118, -45.31875000283309163, 25.69375250200204874 ) ) ;
#25950=CARTESIAN_POINT ( 'NONE',  ( 0.8068914002680659392, -45.70862948725645936, 28.57224053245856865 ) ) ;
#25951=PLANE ( 'NONE',  #21013 ) ;
#25959=EDGE_CURVE ( 'NONE', #37054, #28413, #39567, .T. ) ;
#25962=CARTESIAN_POINT ( 'NONE',  ( 4.257384923554909051, -42.51562500047793947, 25.37105061671875461 ) ) ;
#25964=CARTESIAN_POINT ( 'NONE',  ( 0.9468279798049117346, -42.26145833381127659, 31.10510344464368515 ) ) ;
#25972=CARTESIAN_POINT ( 'NONE',  ( 7.567941867304904591, -46.14062500047794657, 29.19375250200204164 ) ) ;
#25974=DIRECTION ( 'NONE',  ( 0.000000000000000000, 0.000000000000000000, -1.000000000000000000 ) ) ;
#25987=CARTESIAN_POINT ( 'NONE',  ( 4.257284565358973261, -49.31874761147663833, 25.69375250344087291 ) ) ;
#26003=CARTESIAN_POINT ( 'NONE',  ( 5.173518667958606265, -47.33941487687306449, 25.78485257736267755 ) ) ;
#26006=CARTESIAN_POINT ( 'NONE',  ( 7.757384923554905498, -46.74999999999999289, 29.19375250200204164 ) ) ;
#26012=CARTESIAN_POINT ( 'NONE',  ( 5.912663395429904156, -50.22395833381128227, 32.06077891596451224 ) ) ;
#26017=CARTESIAN_POINT ( 'NONE',  ( 4.257384923554909051, -51.12499999999998579, 25.15230061767466552 ) ) ;
#26021=ORIENTED_EDGE ( 'NONE', *, *, #9288, .F. ) ;
#26022=CARTESIAN_POINT ( 'NONE',  ( 6.431250365814399572, -46.37294634308543806, 26.42228680478639191 ) ) ;
#26026=CARTESIAN_POINT ( 'NONE',  ( 4.157799930344774353, -48.81638049171181137, 25.69496657512030779 ) ) ;
#26029=CARTESIAN_POINT ( 'NONE',  ( 2.507384923554911715, -51.77708333428923737, 26.16266358875650866 ) ) ;
#26030=EDGE_CURVE ( 'NONE', #5047, #8688, #23122, .T. ) ;
#26061=CARTESIAN_POINT ( 'NONE',  ( 0.9468279798049143992, -47.93229166714461797, 27.28240155936039812 ) ) ;
#26065=CARTESIAN_POINT ( 'NONE',  ( 0.9468279798049125118, -51.30312500047794799, 29.19375250200204164 ) ) ;
#26072=CARTESIAN_POINT ( 'NONE',  ( 0.7573849235549120484, -47.98895833323773275, 31.21447844416572792 ) ) ;
#26078=CARTESIAN_POINT ( 'NONE',  ( 0.7573849235549129366, -45.19375000095590877, 29.19375250200204164 ) ) ;
#26082=CARTESIAN_POINT ( 'NONE',  ( 4.257384923554907274, -42.87499999999998579, 32.69375250200203453 ) ) ;
#26105=DIRECTION ( 'NONE',  ( -0.000000000000000000, -1.000000000000000000, -0.000000000000000000 ) ) ;
#26115=CARTESIAN_POINT ( 'NONE',  ( 7.567941867304905479, -45.51145833381128369, 27.28240155936039812 ) ) ;
#26116=CARTESIAN_POINT ( 'NONE',  ( 2.975064734268261457, -42.40508397444173738, 32.45039488375558534 ) ) ;
#26122=CARTESIAN_POINT ( 'NONE',  ( 6.749184859680589454, -51.88301522436444202, 26.69358580375569190 ) ) ;
#26125=CARTESIAN_POINT ( 'NONE',  ( 7.430171961869254105, -47.90938564858907256, 27.71607901816532404 ) ) ;
#26136=CARTESIAN_POINT ( 'NONE',  ( 0.7500724074134144104, -50.68373782334830224, 29.61001911352128957 ) ) ;
#26138=CYLINDRICAL_SURFACE ( 'NONE', #15862, 5.499999999999994671 ) ;
#26159=CARTESIAN_POINT ( 'NONE',  ( 5.195207097063835988, -47.35267090063072715, 32.69375250200204164 ) ) ;
#26181=CARTESIAN_POINT ( 'NONE',  ( 5.430226715076759803, -46.84665669354581752, 25.88056892681358789 ) ) ;
#26183=CARTESIAN_POINT ( 'NONE',  ( 2.602106451679912169, -46.47395833381128227, 26.32672608803957459 ) ) ;
#26213=CARTESIAN_POINT ( 'NONE',  ( 7.567941867304905479, -51.51145833381127659, 27.28240155936039812 ) ) ;
#26217=CARTESIAN_POINT ( 'NONE',  ( 0.7573849235549120484, -46.95833333333332860, 31.21447844416572792 ) ) ;
#26223=CARTESIAN_POINT ( 'NONE',  ( 0.9468279798049143992, -50.43229166714461087, 27.28240155936039812 ) ) ;
#26228=ADVANCED_FACE ( 'NONE', ( #41333 ), #21967, .T. ) ;
#26230=EDGE_CURVE ( 'NONE', #27947, #32848, #26355, .T. ) ;
#26231=CARTESIAN_POINT ( 'NONE',  ( 4.257384923554909051, -50.12499999999999289, 25.15230061767466552 ) ) ;
#26240=CARTESIAN_POINT ( 'NONE',  ( 3.048173750227104239, -48.59728132053212590, 32.49173506186149041 ) ) ;
#26243=CARTESIAN_POINT ( 'NONE',  ( 4.257384923554909051, -48.81875000095590167, 25.15230061767466552 ) ) ;
#26245=CARTESIAN_POINT ( 'NONE',  ( 7.757384923554902834, -51.29166666666666430, 31.21447844416572792 ) ) ;
#26253=CARTESIAN_POINT ( 'NONE',  ( 3.763192054706554934, -44.08078250628619088, 32.69375242044492325 ) ) ;
#26258=CARTESIAN_POINT ( 'NONE',  ( 0.7573849235549138248, -42.23541666762257307, 27.17302655983835180 ) ) ;
#26270=CARTESIAN_POINT ( 'NONE',  ( 0.9468279798049124008, -46.34895833381128227, 31.10510344464368515 ) ) ;
#26275=CARTESIAN_POINT ( 'NONE',  ( 0.9468279798049117346, -50.26145833381128369, 31.10510344464368515 ) ) ;
#26279=ORIENTED_EDGE ( 'NONE', *, *, #9560, .F. ) ;
#26280=CARTESIAN_POINT ( 'NONE',  ( 0.7573849235549129366, -48.53062499990439704, 29.19375250200204164 ) ) ;
#26287=CARTESIAN_POINT ( 'NONE',  ( 7.757384923554904610, -44.40208333428923737, 27.17302655983835180 ) ) ;
#26289=CARTESIAN_POINT ( 'NONE',  ( 7.757384923554902834, -43.48541666762257307, 31.21447844416572792 ) ) ;
#26290=FACE_OUTER_BOUND ( 'NONE', #3366, .T. ) ;
#26304=CARTESIAN_POINT ( 'NONE',  ( 6.007384923554907274, -51.66666666666665719, 26.16266358875650866 ) ) ;
#26314=CARTESIAN_POINT ( 'NONE',  ( 4.257384923554909051, -52.75000000000000000, 25.69375250200204519 ) ) ;
#26316=CARTESIAN_POINT ( 'NONE',  ( 4.257384923554907274, -46.87499999999997868, 32.69375250200203453 ) ) ;
#26324=CARTESIAN_POINT ( 'NONE',  ( 3.044482980331683741, -42.20865616597446746, 32.27411873898371653 ) ) ;
#26333=CARTESIAN_POINT ( 'NONE',  ( 7.307774966076294731, -42.40391780584809567, 27.47736923338838011 ) ) ;
#26339=ORIENTED_EDGE ( 'NONE', *, *, #18040, .T. ) ;
#26341=CARTESIAN_POINT ( 'NONE',  ( 2.343930994826709746, -50.61444787527633338, 32.18460225104747963 ) ) ;
#26342=CARTESIAN_POINT ( 'NONE',  ( 2.975060292544088991, -42.40553153883359272, 32.45038320576673385 ) ) ;
#26355=( BOUNDED_CURVE ( )  B_SPLINE_CURVE ( 2, ( #5811, #31743, #1982, #31957, #2827 ),
 .UNSPECIFIED., .F., .T. ) 
 B_SPLINE_CURVE_WITH_KNOTS ( ( 3, 2, 3 ),
 ( 0.000000000000000000, 0.008333333333333333218, 0.01250000000000000243 ),
 .UNSPECIFIED. ) 
 CURVE ( )  GEOMETRIC_REPRESENTATION_ITEM ( )  RATIONAL_B_SPLINE_CURVE ( ( 1.000000000000000000, 0.8660254037844387076, 1.000000000000000000, 0.9330127018922192983, 0.9330127018922194093 ) ) 
 REPRESENTATION_ITEM ( '' )  );
#26362=CARTESIAN_POINT ( 'NONE',  ( 3.319562750045979005, -47.89732909936925154, 32.69375250200202743 ) ) ;
#26366=DIRECTION ( 'NONE',  ( -0.000000000000000000, -1.000000000000000000, -0.000000000000000000 ) ) ;
#26379=VERTEX_POINT ( 'NONE', #13029 ) ;
#26380=ORIENTED_EDGE ( 'NONE', *, *, #25705, .T. ) ;
#26385=FACE_OUTER_BOUND ( 'NONE', #14056, .T. ) ;
#26388=CARTESIAN_POINT ( 'NONE',  ( 2.507384923554911715, -47.08333333333332149, 26.16266358875650866 ) ) ;
#26413=CARTESIAN_POINT ( 'NONE',  ( 2.602106451679909505, -50.71979166714461940, 32.06077891596451224 ) ) ;
#26414=CARTESIAN_POINT ( 'NONE',  ( 7.056215699020109255, -47.49504139826993310, 31.34466998627043921 ) ) ;
#26417=CARTESIAN_POINT ( 'NONE',  ( 6.007384923554907274, -47.16666666666665719, 26.16266358875650866 ) ) ;
#26421=LINE ( 'NONE', #29384, #29775 ) ;
#26424=CARTESIAN_POINT ( 'NONE',  ( 7.567941867304904591, -48.14062500047794657, 29.19375250200204164 ) ) ;
#26428=EDGE_CURVE ( 'NONE', #29198, #3504, #4737, .T. ) ;
#26433=CARTESIAN_POINT ( 'NONE',  ( 0.7573849235549138248, -50.54166666666665009, 27.17302655983835180 ) ) ;
#26434=CARTESIAN_POINT ( 'NONE',  ( 7.567941867304902814, -49.59895833381128227, 27.28240155936039457 ) ) ;
#26435=ORIENTED_EDGE ( 'NONE', *, *, #34915, .T. ) ;
#26437=CARTESIAN_POINT ( 'NONE',  ( 3.334650224474709379, -43.08834127834490602, 32.59525975058342340 ) ) ;
#26442=CARTESIAN_POINT ( 'NONE',  ( 6.007384923554904610, -48.52708333428923737, 32.22484141524757462 ) ) ;
#26471=CARTESIAN_POINT ( 'NONE',  ( 2.602106451679909505, -44.80729166714461797, 32.06077891596451224 ) ) ;
#26476=CARTESIAN_POINT ( 'NONE',  ( 7.567941867304902814, -50.09479166714461940, 31.10510344464368870 ) ) ;
#26485=CARTESIAN_POINT ( 'NONE',  ( 2.507384923554909495, -48.94729166657106845, 32.22484141524756751 ) ) ;
#26492=CARTESIAN_POINT ( 'NONE',  ( 2.507384923554909495, -44.11041666762257307, 32.22484141524756751 ) ) ;
#26493=CARTESIAN_POINT ( 'NONE',  ( 6.007384923554907274, -43.36041666762257307, 26.16266358875650866 ) ) ;
#26495=ORIENTED_EDGE ( 'NONE', *, *, #15701, .T. ) ;
#26520=CYLINDRICAL_SURFACE ( 'NONE', #28165, 3.499999999999996003 ) ;
#26531=CARTESIAN_POINT ( 'NONE',  ( 7.567941867304905479, -44.51145833381129080, 27.28240155936039812 ) ) ;
#26534=CARTESIAN_POINT ( 'NONE',  ( 5.603141568192350874, -44.03864290532750658, 32.44232603011292326 ) ) ;
#26535=EDGE_CURVE ( 'NONE', #5487, #15360, #16662, .T. ) ;
#26541=CARTESIAN_POINT ( 'NONE',  ( 6.393954179667081128, -42.40356835356715948, 26.40841452900434660 ) ) ;
#26547=ORIENTED_EDGE ( 'NONE', *, *, #28101, .F. ) ;
#26550=CARTESIAN_POINT ( 'NONE',  ( 4.239997387274279106, -50.81836832095942924, 25.69378492736172603 ) ) ;
#26551=CARTESIAN_POINT ( 'NONE',  ( 7.757384923554904610, -42.70833333333332149, 27.17302655983835180 ) ) ;
#26552=ORIENTED_EDGE ( 'NONE', *, *, #9235, .T. ) ;
#26555=VECTOR ( 'NONE', #30515, 1000.000000000000000 ) ;
#26569=AXIS2_PLACEMENT_3D ( 'NONE', #8326, #24295, #37266 ) ;
#26573=CARTESIAN_POINT ( 'NONE',  ( 7.295377909465710076, -45.40241934028199466, 27.45471989673159285 ) ) ;
#26594=CARTESIAN_POINT ( 'NONE',  ( 7.567941867304905479, -48.55312500047794799, 29.19375250200204164 ) ) ;
#26598=CARTESIAN_POINT ( 'NONE',  ( 4.876771394649241032, -46.05400271020102565, 32.63851473213794918 ) ) ;
#26625=CARTESIAN_POINT ( 'NONE',  ( 0.9468279798049115126, -50.76145833381128369, 31.10510344464368515 ) ) ;
#26628=CARTESIAN_POINT ( 'NONE',  ( 0.7573849235549138248, -46.54166666666665009, 27.17302655983835180 ) ) ;
#26635=CARTESIAN_POINT ( 'NONE',  ( 7.567941867304902814, -49.18229166714461087, 31.10510344464368870 ) ) ;
#26644=CARTESIAN_POINT ( 'NONE',  ( 0.7573849235549120484, -48.45833333333332860, 31.21447844416572792 ) ) ;
#26645=CARTESIAN_POINT ( 'NONE',  ( 7.567941867304902814, -51.18229166714461797, 31.10510344464368870 ) ) ;
#26648=CARTESIAN_POINT ( 'NONE',  ( 4.257384923554933032, -43.62499999999999289, 25.69375250200204519 ) ) ;
#26655=CARTESIAN_POINT ( 'NONE',  ( 0.7573849235549129366, -50.19375000095590167, 29.19375250200204164 ) ) ;
#26668=CARTESIAN_POINT ( 'NONE',  ( 4.199126769893688049, -44.81743657241514001, 25.69416810585581246 ) ) ;
#26670=CARTESIAN_POINT ( 'NONE',  ( 0.7573849235549120484, -42.15208333428924448, 31.21447844416572792 ) ) ;
#26683=CARTESIAN_POINT ( 'NONE',  ( 7.567941867304902814, -44.18229166714461797, 31.10510344464368870 ) ) ;
#26689=CARTESIAN_POINT ( 'NONE',  ( 4.257384923554909051, -46.42812500047795510, 25.37105061671875106 ) ) ;
#26691=ORIENTED_EDGE ( 'NONE', *, *, #25063, .T. ) ;
#26693=ORIENTED_EDGE ( 'NONE', *, *, #35302, .F. ) ;
#26694=CARTESIAN_POINT ( 'NONE',  ( 4.257384923554909051, -46.65562499990440415, 25.15230061767466552 ) ) ;
#26700=CARTESIAN_POINT ( 'NONE',  ( 2.507384923554911715, -45.27708333428923737, 26.16266358875650866 ) ) ;
#26719=CARTESIAN_POINT ( 'NONE',  ( 4.276329171579276611, -51.31920101901584275, 25.69380055443256694 ) ) ;
#26734=FACE_OUTER_BOUND ( 'NONE', #38627, .T. ) ;
#26744=CARTESIAN_POINT ( 'NONE',  ( 7.567941867304904591, -52.09895833381127517, 27.28240155936039812 ) ) ;
#26752=CARTESIAN_POINT ( 'NONE',  ( 2.352663490024888837, -42.40491282218779645, 26.25426194342115949 ) ) ;
#26763=CARTESIAN_POINT ( 'NONE',  ( 7.757384923554905498, -51.44375000095590877, 29.19375250200204164 ) ) ;
#26796=CYLINDRICAL_SURFACE ( 'NONE', #25779, 3.499999999999996003 ) ;
#26802=ORIENTED_EDGE ( 'NONE', *, *, #23502, .F. ) ;
#26806=CARTESIAN_POINT ( 'NONE',  ( 7.567941867304902814, -43.59479166714461940, 31.10510344464368870 ) ) ;
#26811=CARTESIAN_POINT ( 'NONE',  ( 7.567941867304905479, -47.01145833381128369, 27.28240155936039812 ) ) ;
#26818=ORIENTED_EDGE ( 'NONE', *, *, #5555, .T. ) ;
#26839=CARTESIAN_POINT ( 'NONE',  ( 7.567941867304905479, -47.55312500047795510, 29.19375250200204164 ) ) ;
#26843=CARTESIAN_POINT ( 'NONE',  ( 7.757384923554904610, -46.20833333333332860, 27.17302655983835180 ) ) ;
#26844=EDGE_LOOP ( 'NONE', ( #727, #35212, #38195, #11922 ) ) ;
#26845=CIRCLE ( 'NONE', #8486, 5.499999999999994671 ) ;
#26847=CARTESIAN_POINT ( 'NONE',  ( 3.925158143724454707, -49.07590282302166429, 32.69375252099408158 ) ) ;
#26851=CARTESIAN_POINT ( 'NONE',  ( 2.602106451679909505, -48.80729166714461087, 32.06077891596451224 ) ) ;
#26857=CARTESIAN_POINT ( 'NONE',  ( 0.7573849235549138248, -47.04166666666665719, 27.17302655983835180 ) ) ;
#26858=CARTESIAN_POINT ( 'NONE',  ( 5.912663395429904156, -50.72395833381128227, 32.06077891596451224 ) ) ;
#26861=CARTESIAN_POINT ( 'NONE',  ( 1.421267855278717018, -43.14349537615628094, 31.24617366225838921 ) ) ;
#26867=CARTESIAN_POINT ( 'NONE',  ( 4.257384923554908163, -50.06875000095590877, 33.23520438632941421 ) ) ;
#26884=( LENGTH_UNIT ( ) NAMED_UNIT ( * ) SI_UNIT ( .MILLI., .METRE. ) );
#26895=CARTESIAN_POINT ( 'NONE',  ( 0.9468279798049143992, -44.93229166714461797, 27.28240155936039812 ) ) ;
#26899=CARTESIAN_POINT ( 'NONE',  ( 2.602106451679909505, -48.21979166714461229, 32.06077891596451224 ) ) ;
#26907=CARTESIAN_POINT ( 'NONE',  ( 2.507384923554911715, -45.61395833323773275, 26.16266358875650866 ) ) ;
#26915=CARTESIAN_POINT ( 'NONE',  ( 4.257384923554909051, -44.81875000095590877, 25.15230061767466552 ) ) ;
#26944=CARTESIAN_POINT ( 'NONE',  ( 7.073436380858386663, -50.89265132922104584, 27.10231022074763985 ) ) ;
#26954=CARTESIAN_POINT ( 'NONE',  ( 0.9468279798049134000, -44.34479166714461940, 27.28240155936039457 ) ) ;
#26961=CARTESIAN_POINT ( 'NONE',  ( 2.701825989912535420, -42.40378162294259567, 26.05556204608703297 ) ) ;
#26965=CARTESIAN_POINT ( 'NONE',  ( 0.8135968151556176586, -44.20730582845119017, 28.56879549243070215 ) ) ;
#26966=CARTESIAN_POINT ( 'NONE',  ( 0.9693024015420681483, -50.16649487625740989, 30.39321862621029879 ) ) ;
#26968=EDGE_CURVE ( 'NONE', #10374, #8545, #14597, .T. ) ;
#26970=VERTEX_POINT ( 'NONE', #17783 ) ;
#26974=CARTESIAN_POINT ( 'NONE',  ( 0.7573849235549129366, -50.69375000095590167, 29.19375250200204164 ) ) ;
#26975=CARTESIAN_POINT ( 'NONE',  ( 2.602106451679909505, -42.80729166714461797, 32.06077891596451224 ) ) ;
#26998=EDGE_CURVE ( 'NONE', #36911, #34930, #36506, .T. ) ;
#26999=ORIENTED_EDGE ( 'NONE', *, *, #15701, .F. ) ;
#27002=ADVANCED_FACE ( 'NONE', ( #17156 ), #1409, .T. ) ;
#27005=CARTESIAN_POINT ( 'NONE',  ( 7.056218770635680926, -49.89014762800230329, 27.04283885558784206 ) ) ;
#27012=LINE ( 'NONE', #20626, #17964 ) ;
#27021=CARTESIAN_POINT ( 'NONE',  ( 2.602106451679911281, -47.38645833381128369, 26.32672608803957459 ) ) ;
#27025=CARTESIAN_POINT ( 'NONE',  ( 2.507384923554909495, -46.91666666666665719, 32.22484141524756751 ) ) ;
#27052=CARTESIAN_POINT ( 'NONE',  ( 0.9468279798049125118, -48.80312500047794799, 29.19375250200204164 ) ) ;
#27055=CARTESIAN_POINT ( 'NONE',  ( 0.7573849235549138248, -43.54166666666665719, 27.17302655983835180 ) ) ;
#27058=CARTESIAN_POINT ( 'NONE',  ( 9.216391464164017222, 7.250000000000000000, 25.89968016835878828 ) ) ;
#27061=CARTESIAN_POINT ( 'NONE',  ( 2.602106451679909505, -45.80729166714461797, 32.06077891596451224 ) ) ;
#27068=CARTESIAN_POINT ( 'NONE',  ( 4.257384923554909051, -47.62499999999999289, 25.15230061767466552 ) ) ;
#27069=CARTESIAN_POINT ( 'NONE',  ( 0.9468279798049124008, -50.34895833381128227, 31.10510344464368515 ) ) ;
#27072=CARTESIAN_POINT ( 'NONE',  ( 4.257337177015303453, -43.31874891592651977, 25.69375250232772245 ) ) ;
#27078=CARTESIAN_POINT ( 'NONE',  ( 7.757384923554904610, -49.90208333428923737, 27.17302655983835180 ) ) ;
#27087=AXIS2_PLACEMENT_3D ( 'NONE', #28616, #41604, #10309 ) ;
#27088=CARTESIAN_POINT ( 'NONE',  ( 5.173501304529385614, -45.04716196579540366, 32.60265709178494120 ) ) ;
#27091=CARTESIAN_POINT ( 'NONE',  ( 3.216122365118785797, -44.79496908644021147, 25.84198015498908418 ) ) ;
#27092=CARTESIAN_POINT ( 'NONE',  ( 4.965282557631612192, -42.05189529538266413, 33.23404929009055309 ) ) ;
#27103=CARTESIAN_POINT ( 'NONE',  ( 4.257384923554909051, -52.75000000000000000, 29.19375250200204164 ) ) ;
#27105=CARTESIAN_POINT ( 'NONE',  ( 7.567941867304904591, -44.59895833381127517, 27.28240155936039812 ) ) ;
#27113=CARTESIAN_POINT ( 'NONE',  ( 0.7573849235549120484, -45.98895833323773275, 31.21447844416572792 ) ) ;
#27120=CARTESIAN_POINT ( 'NONE',  ( 0.7573849235549129366, -42.69375000095590167, 29.19375250200204164 ) ) ;
#27146=DIRECTION ( 'NONE',  ( 0.000000000000000000, 0.000000000000000000, -1.000000000000000000 ) ) ;
#27147=CARTESIAN_POINT ( 'NONE',  ( 4.257387527570275054, -50.81875003717480155, 25.69375250200301508 ) ) ;
#27159=CARTESIAN_POINT ( 'NONE',  ( 0.9468279798049125118, -42.80312500047794799, 29.19375250200204164 ) ) ;
#27161=CARTESIAN_POINT ( 'NONE',  ( 4.257384923554907274, -47.87499999999998579, 32.69375250200203453 ) ) ;
#27168=CARTESIAN_POINT ( 'NONE',  ( 7.374927007105729793, -48.48051793228978568, 30.84718077364634325 ) ) ;
#27172=CARTESIAN_POINT ( 'NONE',  ( 1.845800272608178805, -44.25774875339960346, 26.62124224106074522 ) ) ;
#27173=CARTESIAN_POINT ( 'NONE',  ( 0.9792418605697054135, -50.16582323308576008, 30.42012263915129466 ) ) ;
#27180=CARTESIAN_POINT ( 'NONE',  ( 2.507384923554911715, -48.27708333428923737, 26.16266358875650866 ) ) ;
#27181=CARTESIAN_POINT ( 'NONE',  ( 4.257384923554908163, -42.76562500047794657, 33.01645438728532866 ) ) ;
#27200=EDGE_CURVE ( 'NONE', #37126, #8428, #14187, .T. ) ;
#27213=CARTESIAN_POINT ( 'NONE',  ( 7.568192971388668866, -42.40485061181026083, 30.47826289542339850 ) ) ;
#27216=CARTESIAN_POINT ( 'NONE',  ( 7.757384886080981090, -49.93134098896545936, 28.73560331212381413 ) ) ;
#27232=CARTESIAN_POINT ( 'NONE',  ( 5.912663395429907709, -46.96979166714461229, 26.32672608803957459 ) ) ;
#27234=EDGE_CURVE ( 'NONE', #2420, #37126, #12561, .T. ) ;
#27236=CARTESIAN_POINT ( 'NONE',  ( 5.195207097063846646, -44.85267090063072004, 32.69375250200202743 ) ) ;
#27250=EDGE_CURVE ( 'NONE', #5445, #3413, #37764, .T. ) ;
#27265=CARTESIAN_POINT ( 'NONE',  ( 0.9468279798049125118, -49.30312500047794799, 29.19375250200204164 ) ) ;
#27269=CARTESIAN_POINT ( 'NONE',  ( 4.257384923554908163, -44.87499999999998579, 33.23520438632941421 ) ) ;
#27275=CARTESIAN_POINT ( 'NONE',  ( 7.567941867304904591, -47.14062500047794657, 29.19375250200204164 ) ) ;
#27281=CARTESIAN_POINT ( 'NONE',  ( 0.7573849235549120484, -46.45833333333332149, 31.21447844416572792 ) ) ;
#27282=CARTESIAN_POINT ( 'NONE',  ( 4.257384923554909051, -50.51562500047794657, 25.37105061671875106 ) ) ;
#27294=CARTESIAN_POINT ( 'NONE',  ( 7.757384923554902834, -45.98541666762256597, 31.21447844416572792 ) ) ;
#27322=CARTESIAN_POINT ( 'NONE',  ( 4.257384923554909051, -43.51562500047794657, 25.37105061671875461 ) ) ;
#27328=CARTESIAN_POINT ( 'NONE',  ( 0.7573849235549120484, -45.48895833323772564, 31.21447844416572792 ) ) ;
#27334=CARTESIAN_POINT ( 'NONE',  ( 5.912663395429907709, -50.46979166714461940, 26.32672608803957459 ) ) ;
#27349=CARTESIAN_POINT ( 'NONE',  ( 4.257384923554896616, -48.12499999999998579, 25.69375250200204519 ) ) ;
#27359=CARTESIAN_POINT ( 'NONE',  ( 4.257384923554909051, -49.62499999999998579, 25.69375250200204519 ) ) ;
#27360=CARTESIAN_POINT ( 'NONE',  ( 7.785153877754746432, -50.94001279456478670, 28.97065275420805719 ) ) ;
#27369=CARTESIAN_POINT ( 'NONE',  ( 5.912663395429907709, -51.05729166714461797, 26.32672608803957459 ) ) ;
#27372=CARTESIAN_POINT ( 'NONE',  ( 0.7585221375395087007, -45.20447198729367955, 28.72629514470142098 ) ) ;
#27384=VERTEX_POINT ( 'NONE', #89 ) ;
#27386=CARTESIAN_POINT ( 'NONE',  ( 4.257384923414707423, -42.56875000095865147, 32.69375250200203453 ) ) ;
#27387=B_SPLINE_CURVE_WITH_KNOTS ( 'NONE', 3,
 ( #10465, #10891, #1113, #11103, #24087, #23446, #7701, #37056, #7913, #1526, #14504, #37256, #27475, #40443, #11301, #8111, #7277, #33211, #31485, #2562, #18106, #8729, #18305, #38079, #15545, #41278, #21500, #31902, #24493, #35099, #5544, #31277, #8317, #18934, #31076, #5961 ),
 .UNSPECIFIED., .F., .F.,
 ( 4, 2, 2, 2, 2, 2, 2, 2, 2, 2, 2, 2, 2, 2, 1, 1, 1, 1, 2, 4 ),
 ( 0.2412155680408511749, 0.2443911758509053067, 0.2475667836609594663, 0.2507423914710135704, 0.2539179992810677300, 0.2555058031860947820, 0.2562997051386083358, 0.2566966561148650849, 0.2568951316029934873, 0.2570936070911218341, 0.2602692149011761602, 0.2634448227112304308, 0.2650326266162575939, 0.2658265285687712032, 0.2662234795450279523, 0.2664219550331563546, 0.2665211927772205835, 0.2665708116492526703, 0.2665956210852686858, 0.2666204305212847570 ),
 .UNSPECIFIED. ) ;
#27388=CARTESIAN_POINT ( 'NONE',  ( 7.757384923554902834, -49.98541666762256597, 31.21447844416572792 ) ) ;
#27389=CARTESIAN_POINT ( 'NONE',  ( 5.912663395429904156, -42.72395833381127517, 32.06077891596451224 ) ) ;
#27394=AXIS2_PLACEMENT_3D ( 'NONE', #1894, #8283, #21259 ) ;
#27396=CARTESIAN_POINT ( 'NONE',  ( 4.257403086791381241, -47.31875042192206848, 25.69375250204917194 ) ) ;
#27398=CARTESIAN_POINT ( 'NONE',  ( 2.507384923554911715, -45.08333333333332149, 26.16266358875650866 ) ) ;
#27404=CARTESIAN_POINT ( 'NONE',  ( 3.319562750045979005, -43.89732909936924443, 32.69375250200202743 ) ) ;
#27418=CARTESIAN_POINT ( 'NONE',  ( 3.319562750045980337, -49.10267090063073425, 25.69375250200204519 ) ) ;
#27430=VERTEX_POINT ( 'NONE', #41805 ) ;
#27438=CARTESIAN_POINT ( 'NONE',  ( 5.912663395429907709, -45.96979166714461229, 26.32672608803957459 ) ) ;
#27469=CARTESIAN_POINT ( 'NONE',  ( 5.912663395429905044, -48.63645833381128369, 32.06077891596451224 ) ) ;
#27473=CARTESIAN_POINT ( 'NONE',  ( 6.007384923554904610, -43.33333333333332149, 32.22484141524757462 ) ) ;
#27474=ORIENTED_EDGE ( 'NONE', *, *, #2190, .F. ) ;
#27475=CARTESIAN_POINT ( 'NONE',  ( 7.643501020819684300, -49.42355217493608421, 28.30084737174210119 ) ) ;
#27481=CARTESIAN_POINT ( 'NONE',  ( 0.9468279798049132889, -45.39062500047794657, 29.19375250200204164 ) ) ;
#27489=CARTESIAN_POINT ( 'NONE',  ( 7.757384923554902834, -48.79166666666665719, 31.21447844416572792 ) ) ;
#27490=CARTESIAN_POINT ( 'NONE',  ( 0.9468279798049124008, -46.84895833381128227, 31.10510344464368515 ) ) ;
#27501=ORIENTED_EDGE ( 'NONE', *, *, #35809, .F. ) ;
#27502=CARTESIAN_POINT ( 'NONE',  ( 4.257384923554909051, -45.81875000095590877, 25.15230061767466552 ) ) ;
#27511=AXIS2_PLACEMENT_3D ( 'NONE', #31714, #18959, #6405 ) ;
#27528=CARTESIAN_POINT ( 'NONE',  ( 6.443981235129863983, -44.01662816252333243, 31.94562492207214532 ) ) ;
#27536=CARTESIAN_POINT ( 'NONE',  ( 5.153009714167651190, -44.34000239886071171, 25.80093352943575624 ) ) ;
#27540=VERTEX_POINT ( 'NONE', #29214 ) ;
#27541=CARTESIAN_POINT ( 'NONE',  ( 2.507384923554909495, -45.44729166657106845, 32.22484141524756751 ) ) ;
#27542=ADVANCED_FACE ( 'NONE', ( #20081 ), #33296, .T. ) ;
#27547=PRODUCT_DEFINITION_SHAPE ( 'NONE', 'NONE',  #35872 ) ;
#27571=CARTESIAN_POINT ( 'NONE',  ( 4.257384923554909051, -52.75000000000000000, 25.69375250200204519 ) ) ;
#27578=CARTESIAN_POINT ( 'NONE',  ( 2.602106451679912169, -50.97395833381128227, 26.32672608803957459 ) ) ;
#27581=CARTESIAN_POINT ( 'NONE',  ( 3.801776162730060804, -45.30874399747600023, 25.71606408062995186 ) ) ;
#27583=CARTESIAN_POINT ( 'NONE',  ( 7.757384923554902834, -46.29166666666666430, 31.21447844416572792 ) ) ;
#27596=CARTESIAN_POINT ( 'NONE',  ( 2.507384923554911715, -48.77708333428924448, 26.16266358875650866 ) ) ;
#27597=CARTESIAN_POINT ( 'NONE',  ( 7.567941867304902814, -43.59895833381127517, 27.28240155936039457 ) ) ;
#27601=FACE_OUTER_BOUND ( 'NONE', #1071, .T. ) ;
#27622=CARTESIAN_POINT ( 'NONE',  ( 6.949807758536119096, -42.40485061181024662, 31.50941140565776521 ) ) ;
#27632=EDGE_LOOP ( 'NONE', ( #36679, #27785 ) ) ;
#27635=B_SPLINE_CURVE_WITH_KNOTS ( 'NONE', 3,
 ( #33998, #4852, #14224, #7852, #30804, #21437, #20822, #4227, #1869, #11438, #4649, #14437, #1664, #40381, #39955, #11242, #30172, #34200, #21229, #14849, #20606, #33585, #14651, #30384, #23805, #17628, #11644, #37603 ),
 .UNSPECIFIED., .F., .F.,
 ( 4, 2, 2, 2, 1, 1, 2, 2, 2, 2, 2, 2, 2, 2, 4 ),
 ( 0.9030297558812198089, 0.9060035890262738700, 0.9089774221713278202, 0.9119512553163818813, 0.9123229844595136528, 0.9125088490310795386, 0.9126017813168624260, 0.9126947136026454244, 0.9134381718889089674, 0.9149250884614361645, 0.9164120050339633616, 0.9178989216064905587, 0.9208727547515448419, 0.9238465878965992362, 0.9268204210416536304 ),
 .UNSPECIFIED. ) ;
#27636=CARTESIAN_POINT ( 'NONE',  ( 0.9468279798049134000, -46.34479166714461229, 27.28240155936039457 ) ) ;
#27651=CARTESIAN_POINT ( 'NONE',  ( 4.257384923554909051, -52.75000000000000000, 29.19375250200204164 ) ) ;
#27665=CARTESIAN_POINT ( 'NONE',  ( 5.912663395429905044, -49.13645833381128369, 32.06077891596451224 ) ) ;
#27666=CARTESIAN_POINT ( 'NONE',  ( 9.216391464164017222, 3.250000000000000444, 25.89968016835878828 ) ) ;
#27671=CARTESIAN_POINT ( 'NONE',  ( 7.757384923554905498, -45.74999999999999289, 29.19375250200204164 ) ) ;
#27673=DIRECTION ( 'NONE',  ( 0.000000000000000000, 1.000000000000000000, 0.000000000000000000 ) ) ;
#27677=CARTESIAN_POINT ( 'NONE',  ( 4.257384923554909051, -47.51562500047794657, 25.37105061671875461 ) ) ;
#27678=CARTESIAN_POINT ( 'NONE',  ( 5.912663395429907709, -47.96979166714461229, 26.32672608803957459 ) ) ;
#27684=CARTESIAN_POINT ( 'NONE',  ( 6.007384923554907274, -43.66666666666665719, 26.16266358875650866 ) ) ;
#27685=CARTESIAN_POINT ( 'NONE',  ( 2.602106451679912169, -48.97395833381128227, 26.32672608803957459 ) ) ;
#27686=VERTEX_POINT ( 'NONE', #34102 ) ;
#27689=DIRECTION ( 'NONE',  ( -0.8329741740894178736, 0.000000000000000000, 0.5533118698347725406 ) ) ;
#27693=CARTESIAN_POINT ( 'NONE',  ( 4.257384923554909051, 0.8500000000000035305, 29.19375250200204164 ) ) ;
#27697=CARTESIAN_POINT ( 'NONE',  ( 6.007384923554904610, -47.52708333428923737, 32.22484141524757462 ) ) ;
#27711=CARTESIAN_POINT ( 'NONE',  ( 3.800677651558625580, -49.57769189237037466, 32.69375258067127277 ) ) ;
#27728=CARTESIAN_POINT ( 'NONE',  ( 0.9468279798049132889, -43.89062500047794657, 29.19375250200204164 ) ) ;
#27735=CARTESIAN_POINT ( 'NONE',  ( 7.757384923554905498, -43.78062499990439704, 29.19375250200204164 ) ) ;
#27739=CARTESIAN_POINT ( 'NONE',  ( 0.8223141326495693182, -43.67278512565541604, 30.01974839623697733 ) ) ;
#27741=CARTESIAN_POINT ( 'NONE',  ( 0.7573849235549129366, -42.19375000095590167, 29.19375250200204164 ) ) ;
#27768=DIRECTION ( 'NONE',  ( -0.000000000000000000, -1.000000000000000000, -0.000000000000000000 ) ) ;
#27777=CARTESIAN_POINT ( 'NONE',  ( 7.567941867304904591, -50.09895833381128227, 27.28240155936039812 ) ) ;
#27779=CARTESIAN_POINT ( 'NONE',  ( 4.257384923554896616, -47.62499999999999289, 25.69375250200204519 ) ) ;
#27782=CARTESIAN_POINT ( 'NONE',  ( 0.9468279798049117346, -51.76145833381128369, 31.10510344464368515 ) ) ;
#27785=ORIENTED_EDGE ( 'NONE', *, *, #40918, .F. ) ;
#27786=VERTEX_POINT ( 'NONE', #17104 ) ;
#27792=ORIENTED_EDGE ( 'NONE', *, *, #23306, .T. ) ;
#27796=CARTESIAN_POINT ( 'NONE',  ( 7.757384923554905498, -49.94375000095590167, 29.19375250200204164 ) ) ;
#27797=CARTESIAN_POINT ( 'NONE',  ( 0.9468279798049143992, -42.43229166714461087, 27.28240155936039457 ) ) ;
#27809=VECTOR ( 'NONE', #20989, 999.9999999999998863 ) ;
#27814=CARTESIAN_POINT ( 'NONE',  ( 4.257384923554909051, -52.75000000000000000, 32.69375250200203453 ) ) ;
#27830=CARTESIAN_POINT ( 'NONE',  ( 6.498972721485651860, -49.01416129530534960, 31.88203314327804705 ) ) ;
#27843=CARTESIAN_POINT ( 'NONE',  ( 2.815359705850238203, -42.21442365662066010, 32.18390073966531162 ) ) ;
#27867=CARTESIAN_POINT ( 'NONE',  ( 0.7573849235549129366, -51.49999999999999289, 29.19375250200204164 ) ) ;
#27870=CARTESIAN_POINT ( 'NONE',  ( 7.567941867304904591, -45.09479166714461940, 31.10510344464368870 ) ) ;
#27875=CARTESIAN_POINT ( 'NONE',  ( 2.507384923554911715, -45.58333333333332149, 26.16266358875650866 ) ) ;
#27877=DIRECTION ( 'NONE',  ( 0.000000000000000000, 0.000000000000000000, 1.000000000000000000 ) ) ;
#27880=CARTESIAN_POINT ( 'NONE',  ( 4.257384923554909051, -45.51562500047795368, 25.37105061671875461 ) ) ;
#27882=CARTESIAN_POINT ( 'NONE',  ( 2.602106451679911281, -47.38645833381128369, 26.32672608803957459 ) ) ;
#27891=CARTESIAN_POINT ( 'NONE',  ( 7.757384923554904610, -46.20833333333332860, 27.17302655983835180 ) ) ;
#27892=CARTESIAN_POINT ( 'NONE',  ( 5.912663395429904156, -47.72395833381128227, 32.06077891596451224 ) ) ;
#27905=CARTESIAN_POINT ( 'NONE',  ( 7.757384923554905498, -47.94375000095590877, 29.19375250200204164 ) ) ;
#27943=CARTESIAN_POINT ( 'NONE',  ( 2.507384923554911715, -44.11395833323773275, 26.16266358875650866 ) ) ;
#27947=VERTEX_POINT ( 'NONE', #34726 ) ;
#27949=CARTESIAN_POINT ( 'NONE',  ( 7.567941867304904591, -50.59479166714461940, 31.10510344464368870 ) ) ;
#27973=CARTESIAN_POINT ( 'NONE',  ( 4.257384923554909051, -49.62499999999998579, 25.69375250200204519 ) ) ;
#27980=CARTESIAN_POINT ( 'NONE',  ( 2.602106451679909505, -50.30729166714461087, 32.06077891596451224 ) ) ;
#27982=DIRECTION ( 'NONE',  ( 0.000000000000000000, 0.000000000000000000, -1.000000000000000000 ) ) ;
#27994=CARTESIAN_POINT ( 'NONE',  ( 7.757384923554905498, -49.78062499990439704, 29.19375250200204164 ) ) ;
#27998=DIRECTION ( 'NONE',  ( 0.000000000000000000, 0.000000000000000000, -1.000000000000000000 ) ) ;
#28000=CARTESIAN_POINT ( 'NONE',  ( 7.757384923554904610, -47.90208333428924448, 27.17302655983835180 ) ) ;
#28006=CARTESIAN_POINT ( 'NONE',  ( 2.301935840106695608, -46.61584905371291399, 32.14356851289637262 ) ) ;
#28011=STYLED_ITEM('',(#42159),#9789);
#28025=CARTESIAN_POINT ( 'NONE',  ( 7.757384923554902834, -42.79166666666665719, 31.21447844416572792 ) ) ;
#28030=CARTESIAN_POINT ( 'NONE',  ( 0.9558879971306745160, -48.22066990446241874, 28.02850401729872587 ) ) ;
#28033=CARTESIAN_POINT ( 'NONE',  ( 2.102736010332902250, -46.26514746516544818, 26.39680565092787745 ) ) ;
#28035=CARTESIAN_POINT ( 'NONE',  ( 4.555202053852652533, -48.82584087666496231, 25.69375748506524459 ) ) ;
#28046=AXIS2_PLACEMENT_3D ( 'NONE', #11516, #15561, #28519 ) ;
#28050=CARTESIAN_POINT ( 'NONE',  ( 7.567941867304905479, -43.51145833381128369, 27.28240155936039812 ) ) ;
#28063=VECTOR ( 'NONE', #38498, 1000.000000000000114 ) ;
#28074=EDGE_CURVE ( 'NONE', #21912, #22305, #29662, .T. ) ;
#28083=CARTESIAN_POINT ( 'NONE',  ( 4.257384923554909051, -52.75000000000000000, 29.19375250200204164 ) ) ;
#28085=CARTESIAN_POINT ( 'NONE',  ( 7.307774966076294731, -42.40391780584809567, 27.47736923338838011 ) ) ;
#28086=ORIENTED_EDGE ( 'NONE', *, *, #9235, .F. ) ;
#28090=CARTESIAN_POINT ( 'NONE',  ( 0.9468279798049124008, -42.84895833381128227, 31.10510344464368515 ) ) ;
#28091=CARTESIAN_POINT ( 'NONE',  ( 0.9468279798049117346, -48.76145833381128369, 31.10510344464368515 ) ) ;
#28099=CARTESIAN_POINT ( 'NONE',  ( 7.757384923554902834, -45.29166666666666430, 31.21447844416572792 ) ) ;
#28100=CARTESIAN_POINT ( 'NONE',  ( 2.602106451679909505, -48.80729166714461087, 32.06077891596451224 ) ) ;
#28101=EDGE_CURVE ( 'NONE', #30878, #10651, #10042, .T. ) ;
#28112=CARTESIAN_POINT ( 'NONE',  ( 0.7573849235549120484, -46.15208333428923737, 31.21447844416572792 ) ) ;
#28136=CARTESIAN_POINT ( 'NONE',  ( 6.007384923554907274, -51.16666666666665719, 26.16266358875650866 ) ) ;
#28143=CARTESIAN_POINT ( 'NONE',  ( 7.662294699331928527, -50.42087562615415663, 28.26360934989538976 ) ) ;
#28149=CARTESIAN_POINT ( 'NONE',  ( 0.7573849235549120484, -42.48895833323773985, 31.21447844416572792 ) ) ;
#28152=VERTEX_POINT ( 'NONE', #43 ) ;
#28153=CARTESIAN_POINT ( 'NONE',  ( 4.249906065732344196, -43.81857193763509173, 25.69375837711970689 ) ) ;
#28155=CARTESIAN_POINT ( 'NONE',  ( 0.9468279798049125118, -51.80312500047794799, 29.19375250200204164 ) ) ;
#28165=AXIS2_PLACEMENT_3D ( 'NONE', #19708, #16127, #32886 ) ;
#28166=CARTESIAN_POINT ( 'NONE',  ( 0.7573849235549138248, -45.04166666666665719, 27.17302655983835180 ) ) ;
#28169=CARTESIAN_POINT ( 'NONE',  ( 4.257384923554909051, -52.75000000000000000, 32.19375250200202743 ) ) ;
#28183=DIRECTION ( 'NONE',  ( -0.000000000000000000, -1.000000000000000000, -0.000000000000000000 ) ) ;
#28188=ORIENTED_EDGE ( 'NONE', *, *, #41840, .F. ) ;
#28190=CARTESIAN_POINT ( 'NONE',  ( 0.9468279798049132889, -50.89062500047794657, 29.19375250200204164 ) ) ;
#28192=CARTESIAN_POINT ( 'NONE',  ( 3.135676423308826344, -45.29353611237173283, 25.87055131345620396 ) ) ;
#28194=EDGE_CURVE ( 'NONE', #22305, #10524, #41890, .T. ) ;
#28204=CARTESIAN_POINT ( 'NONE',  ( 4.257384923554908163, -51.90562499990439704, 33.23520438632941421 ) ) ;
#28206=ORIENTED_EDGE ( 'NONE', *, *, #37475, .F. ) ;
#28209=FACE_OUTER_BOUND ( 'NONE', #11823, .T. ) ;
#28210=CARTESIAN_POINT ( 'NONE',  ( 0.7573849235549138248, -46.73541666762257307, 27.17302655983835180 ) ) ;
#28244=CARTESIAN_POINT ( 'NONE',  ( 6.249441703847010032, -49.02120636121514252, 32.07587203229304862 ) ) ;
#28261=CARTESIAN_POINT ( 'NONE',  ( 7.567941867304905479, -43.01145833381129080, 27.28240155936039812 ) ) ;
#28285=CARTESIAN_POINT ( 'NONE',  ( 2.507384923554911715, -51.08333333333332860, 26.16266358875650866 ) ) ;
#28294=CARTESIAN_POINT ( 'NONE',  ( 3.663683714554331949, -42.80459458338349776, 25.74132980801078219 ) ) ;
#28296=ORIENTED_EDGE ( 'NONE', *, *, #39924, .T. ) ;
#28297=CARTESIAN_POINT ( 'NONE',  ( 0.9468279798049132889, -43.39062500047794657, 29.19375250200204164 ) ) ;
#28299=CARTESIAN_POINT ( 'NONE',  ( 0.9468279798049117346, -46.26145833381128369, 31.10510344464368515 ) ) ;
#28306=DIRECTION ( 'NONE',  ( 6.826639262027968510E-05, -0.9999999973084910954, 2.688340370303683700E-05 ) ) ;
#28307=CARTESIAN_POINT ( 'NONE',  ( 7.757384923554902834, -44.29166666666665719, 31.21447844416572792 ) ) ;
#28308=CARTESIAN_POINT ( 'NONE',  ( 7.567941867304904591, -47.14062500047794657, 29.19375250200204164 ) ) ;
#28319=CARTESIAN_POINT ( 'NONE',  ( 7.757384923554905498, -45.44375000095590877, 29.19375250200204164 ) ) ;
#28345=CARTESIAN_POINT ( 'NONE',  ( 4.257384923554908163, -50.87499999999999289, 33.23520438632941421 ) ) ;
#28351=CARTESIAN_POINT ( 'NONE',  ( 4.826061406679848176, -50.33108957957715290, 25.73837363542503454 ) ) ;
#28355=CARTESIAN_POINT ( 'NONE',  ( 1.233183934848494090, -51.23543006082289963, 27.37530175405039756 ) ) ;
#28358=CARTESIAN_POINT ( 'NONE',  ( 2.507384923554909495, -51.91666666666665719, 32.22484141524756751 ) ) ;
#28363=CARTESIAN_POINT ( 'NONE',  ( 4.149881526161019352, -43.81619127845937811, 25.69516697897984869 ) ) ;
#28365=CARTESIAN_POINT ( 'NONE',  ( 4.257384923554909051, -47.92812500047795510, 25.37105061671875461 ) ) ;
#28369=ORIENTED_EDGE ( 'NONE', *, *, #6490, .T. ) ;
#28385=B_SPLINE_CURVE_WITH_KNOTS ( 'NONE', 3,
 ( #35091, #18925, #15964, #41270, #41691, #9574, #2345, #15536, #38495, #9358, #5748, #6164, #19141, #18725, #9143, #32109, #12114, #31684, #25950, #22532, #12970, #38914, #2974, #28913, #41910, #9792, #35725, #25315, #2552, #28490, #41483, #18508, #12331, #15332, #10413, #9993, #29966 ),
 .UNSPECIFIED., .F., .F.,
 ( 4, 2, 2, 2, 2, 2, 2, 2, 2, 2, 2, 2, 2, 2, 1, 2, 2, 2, 4 ),
 ( 0.6221130816552334908, 0.6228658801651089094, 0.6236186786749843280, 0.6251242756947351653, 0.6281354697342367288, 0.6311466637737384033, 0.6315230630286761127, 0.6318994622836138220, 0.6326522607934892406, 0.6341578578132399668, 0.6371690518527414193, 0.6379218503626168379, 0.6382982496175545473, 0.6383923494312889746, 0.6384864492450234019, 0.6386746488724922566, 0.6401802458922432049, 0.6431914399317451014, 0.6462026339712469980 ),
 .UNSPECIFIED. ) ;
#28398=CARTESIAN_POINT ( 'NONE',  ( 4.257384923554908163, -47.26562500047794657, 33.01645438728532866 ) ) ;
#28410=CARTESIAN_POINT ( 'NONE',  ( 2.507384923554911715, -50.11395833323773275, 26.16266358875650866 ) ) ;
#28413=VERTEX_POINT ( 'NONE', #17892 ) ;
#28417=CARTESIAN_POINT ( 'NONE',  ( 0.7573849235549129366, -47.19375000095590877, 29.19375250200204164 ) ) ;
#28445=CARTESIAN_POINT ( 'NONE',  ( 0.7333762779117662944, -48.19502308338536523, 29.18402562998522498 ) ) ;
#28448=CARTESIAN_POINT ( 'NONE',  ( 4.243342579807457327, -46.31841569698277539, 25.69377886201739258 ) ) ;
#28456=CARTESIAN_POINT ( 'NONE',  ( 5.101246524473073585, -48.04811261334901928, 32.60856362856925017 ) ) ;
#28457=CARTESIAN_POINT ( 'NONE',  ( 2.846747488547164195, -42.40474187973472198, 32.39985900329909896 ) ) ;
#28466=CARTESIAN_POINT ( 'NONE',  ( 0.9468279798049125118, -43.30312500047794799, 29.19375250200204164 ) ) ;
#28486=CARTESIAN_POINT ( 'NONE',  ( 7.598592992106777189, -45.47255777792018705, 30.36078635111350721 ) ) ;
#28490=CARTESIAN_POINT ( 'NONE',  ( 1.158228355687792366, -45.65544408568549528, 30.82060206115991718 ) ) ;
#28496=CARTESIAN_POINT ( 'NONE',  ( 0.7573849235549129366, -42.99999999999999289, 29.19375250200204164 ) ) ;
#28498=ORIENTED_EDGE ( 'NONE', *, *, #2276, .T. ) ;
#28503=CARTESIAN_POINT ( 'NONE',  ( 4.257384923554908163, -45.26562500047794657, 33.01645438728532866 ) ) ;
#28504=CARTESIAN_POINT ( 'NONE',  ( 4.257384923554909051, -45.42812500047794799, 25.37105061671875106 ) ) ;
#28514=CARTESIAN_POINT ( 'NONE',  ( 6.505480384804974037, -47.01528671727714936, 31.89680220675908373 ) ) ;
#28516=CARTESIAN_POINT ( 'NONE',  ( 0.7573849235549138248, -46.04166666666666430, 27.17302655983835180 ) ) ;
#28517=CARTESIAN_POINT ( 'NONE',  ( 0.9468279798049124008, -45.34895833381127517, 31.10510344464368515 ) ) ;
#28519=DIRECTION ( 'NONE',  ( 0.000000000000000000, 0.000000000000000000, -1.000000000000000000 ) ) ;
#28522=CARTESIAN_POINT ( 'NONE',  ( 4.257384923554909051, -52.12499999999999289, 25.69375250200204519 ) ) ;
#28545=FACE_OUTER_BOUND ( 'NONE', #39039, .T. ) ;
#28554=CARTESIAN_POINT ( 'NONE',  ( 7.757384923554902834, -49.79166666666666430, 31.21447844416572792 ) ) ;
#28560=CARTESIAN_POINT ( 'NONE',  ( 0.9468279798049124008, -50.84895833381128938, 31.10510344464368515 ) ) ;
#28567=EDGE_CURVE ( 'NONE', #25326, #6171, #14708, .T. ) ;
#28568=CARTESIAN_POINT ( 'NONE',  ( 7.757384923554904610, -51.70833333333332149, 27.17302655983835180 ) ) ;
#28569=CARTESIAN_POINT ( 'NONE',  ( 6.007384923554907274, -45.16666666666665719, 26.16266358875650866 ) ) ;
#28571=ORIENTED_EDGE ( 'NONE', *, *, #27200, .F. ) ;
#28572=CARTESIAN_POINT ( 'NONE',  ( 4.256002020745222936, -43.81871707480075173, 25.69375246828927217 ) ) ;
#28573=VECTOR ( 'NONE', #3733, 1000.000000000000114 ) ;
#28574=CARTESIAN_POINT ( 'NONE',  ( 6.007384923554907274, -43.66666666666665719, 26.16266358875650866 ) ) ;
#28575=CARTESIAN_POINT ( 'NONE',  ( 4.257384923554909051, -48.42812500047795510, 25.37105061671875461 ) ) ;
#28578=CARTESIAN_POINT ( 'NONE',  ( 0.7675964355322045796, -48.68811677174470987, 29.46109505110420557 ) ) ;
#28602=CARTESIAN_POINT ( 'NONE',  ( 6.007384923554904610, -49.83333333333332860, 32.22484141524757462 ) ) ;
#28609=CARTESIAN_POINT ( 'NONE',  ( 7.567941867304904591, -48.59895833381128227, 27.28240155936039812 ) ) ;
#28616=CARTESIAN_POINT ( 'NONE',  ( 4.257384923554909051, 5.249999999999997335, 37.35503210563722831 ) ) ;
#28621=CARTESIAN_POINT ( 'NONE',  ( 7.757384923554902834, -49.82229166657106845, 31.21447844416572792 ) ) ;
#28626=CARTESIAN_POINT ( 'NONE',  ( 6.133664661390401562, -42.52236636718797058, 32.16901770770208202 ) ) ;
#28627=CARTESIAN_POINT ( 'NONE',  ( 2.507384923554911715, -45.77708333428923737, 26.16266358875650866 ) ) ;
#28628=FACE_OUTER_BOUND ( 'NONE', #26844, .T. ) ;
#28629=ADVANCED_FACE ( 'NONE', ( #29921 ), #22706, .T. ) ;
#28631=CARTESIAN_POINT ( 'NONE',  ( 4.257384923554933032, -47.12499999999998579, 25.69375250200204519 ) ) ;
#28633=CARTESIAN_POINT ( 'NONE',  ( 3.718296712020623840, -46.80597361220125663, 25.73265484211133725 ) ) ;
#28653=DIRECTION ( 'NONE',  ( 0.000000000000000000, 0.000000000000000000, -1.000000000000000000 ) ) ;
#28654=CARTESIAN_POINT ( 'NONE',  ( 0.7573849235549120484, -45.45833333333330728, 31.21447844416572792 ) ) ;
#28657=CARTESIAN_POINT ( 'NONE',  ( 0.9468279798049115126, -45.26145833381127659, 31.10510344464368515 ) ) ;
#28658=DIRECTION ( 'NONE',  ( -0.000000000000000000, -1.000000000000000000, -0.000000000000000000 ) ) ;
#28695=CARTESIAN_POINT ( 'NONE',  ( 4.257364757503538932, -47.06955867894671286, 32.69375250189110460 ) ) ;
#28698=CARTESIAN_POINT ( 'NONE',  ( 0.7573849235549138248, -51.04166666666665719, 27.17302655983835180 ) ) ;
#28699=AXIS2_PLACEMENT_3D ( 'NONE', #8467, #21445, #15069 ) ;
#28701=LINE ( 'NONE', #35519, #28063 ) ;
#28709=CARTESIAN_POINT ( 'NONE',  ( 5.912663395429907709, -44.05729166714461797, 26.32672608803957459 ) ) ;
#28710=CARTESIAN_POINT ( 'NONE',  ( 4.257384923554908163, -44.17812500047794799, 33.01645438728532866 ) ) ;
#28720=CARTESIAN_POINT ( 'NONE',  ( 6.007384923554907274, -50.86041666762257307, 26.16266358875650866 ) ) ;
#28721=CARTESIAN_POINT ( 'NONE',  ( 4.257384923554908163, -46.26562500047795368, 33.01645438728532866 ) ) ;
#28745=CARTESIAN_POINT ( 'NONE',  ( 4.257384923554909051, -52.75000000000000000, 32.69375250200203453 ) ) ;
#28748=EDGE_LOOP ( 'NONE', ( #12803, #22333, #9045, #5398 ) ) ;
#28754=CARTESIAN_POINT ( 'NONE',  ( 4.228262433353894956, -47.31809345233035913, 25.69385632612526393 ) ) ;
#28755=CARTESIAN_POINT ( 'NONE',  ( 4.257384923554909051, -52.75000000000000000, 29.19375250200204164 ) ) ;
#28756=CARTESIAN_POINT ( 'NONE',  ( 6.007384923554907274, -49.16666666666665719, 26.16266358875650866 ) ) ;
#28762=CARTESIAN_POINT ( 'NONE',  ( 4.257384923554909051, -51.51562500047793947, 25.37105061671875461 ) ) ;
#28766=CARTESIAN_POINT ( 'NONE',  ( 4.257384923554909051, -52.75000000000000000, 32.69375250200203453 ) ) ;
#28771=CARTESIAN_POINT ( 'NONE',  ( 7.757384923554905498, -50.24999999999998579, 29.19375250200204164 ) ) ;
#28774=CARTESIAN_POINT ( 'NONE',  ( 6.995351021890339638, -46.39111613183766991, 26.97784304621217899 ) ) ;
#28776=CARTESIAN_POINT ( 'NONE',  ( 7.567941867304905479, -50.05312500047794799, 29.19375250200204164 ) ) ;
#28777=CARTESIAN_POINT ( 'NONE',  ( 4.257384918501243121, -51.56875000107599760, 32.69375250200203453 ) ) ;
#28781=CARTESIAN_POINT ( 'NONE',  ( 7.757384923554905498, -51.94375000095590877, 29.19375250200204164 ) ) ;
#28794=CARTESIAN_POINT ( 'NONE',  ( 4.257384923554909051, -49.12499999999998579, 25.69375250200204519 ) ) ;
#28800=VECTOR ( 'NONE', #28658, 1000.000000000000000 ) ;
#28802=EDGE_CURVE ( 'NONE', #4835, #16017, #3306, .T. ) ;
#28814=CARTESIAN_POINT ( 'NONE',  ( 4.257384923554909051, -48.01562500047794657, 25.37105061671875461 ) ) ;
#28819=CARTESIAN_POINT ( 'NONE',  ( 4.257384923554909051, -49.92812500047794799, 25.37105061671875106 ) ) ;
#28826=CARTESIAN_POINT ( 'NONE',  ( 0.7573849235549138248, -50.07229166657107555, 27.17302655983835180 ) ) ;
#28832=CARTESIAN_POINT ( 'NONE',  ( 2.507384923554911715, -46.27708333428923737, 26.16266358875650866 ) ) ;
#28838=CARTESIAN_POINT ( 'NONE',  ( 4.257440696971988459, -46.81875132889357616, 25.69375250244642572 ) ) ;
#28846=CARTESIAN_POINT ( 'NONE',  ( 6.007384923554904610, -51.83333333333332149, 32.22484141524757462 ) ) ;
#28863=CARTESIAN_POINT ( 'NONE',  ( 1.107247685034800089, -48.15813245032141054, 30.71920221828264275 ) ) ;
#28869=CARTESIAN_POINT ( 'NONE',  ( 0.9468279798049125118, -46.80312500047795510, 29.19375250200204164 ) ) ;
#28871=CARTESIAN_POINT ( 'NONE',  ( 5.195207097063836876, -48.64732909936924443, 25.69375250200204519 ) ) ;
#28873=CARTESIAN_POINT ( 'NONE',  ( 3.319562750045983890, -50.10267090063073425, 25.69375250200204519 ) ) ;
#28882=CARTESIAN_POINT ( 'NONE',  ( -1.074868669588189274, 3.250000000000000444, 26.54616302712299358 ) ) ;
#28887=CARTESIAN_POINT ( 'NONE',  ( 3.346259073890879954, -50.59059138846220094, 32.57504056305004525 ) ) ;
#28913=CARTESIAN_POINT ( 'NONE',  ( 1.022889827332605250, -45.66298599198375285, 30.53245352100160659 ) ) ;
#28919=CARTESIAN_POINT ( 'NONE',  ( 0.7573849235549138248, -43.04166666666666430, 27.17302655983835180 ) ) ;
#28921=CARTESIAN_POINT ( 'NONE',  ( 0.7573832686564593297, -42.70010706788384880, 28.88545897044883048 ) ) ;
#28924=CARTESIAN_POINT ( 'NONE',  ( 7.567941867304904591, -43.09895833381128227, 27.28240155936039812 ) ) ;
#28925=CARTESIAN_POINT ( 'NONE',  ( 2.602106451679911281, -45.88645833381128369, 26.32672608803957459 ) ) ;
#28928=LINE ( 'NONE', #38720, #37265 ) ;
#28931=CARTESIAN_POINT ( 'NONE',  ( 7.311909869858278732, -46.98665802880962161, 30.92828675216940937 ) ) ;
#28932=CARTESIAN_POINT ( 'NONE',  ( 4.257384923554908163, -44.76562500047795368, 33.01645438728532866 ) ) ;
#28935=CARTESIAN_POINT ( 'NONE',  ( 4.257384923554909051, -52.75000000000000000, 29.19375250200204164 ) ) ;
#28956=CARTESIAN_POINT ( 'NONE',  ( 3.319562750045979005, -44.39732909936925154, 32.69375250200202743 ) ) ;
#28965=CARTESIAN_POINT ( 'NONE',  ( 4.257364757503538932, -47.06955867894671286, 32.69375250189110460 ) ) ;
#28968=CARTESIAN_POINT ( 'NONE',  ( 7.757384923554902834, -50.79166666666665719, 31.21447844416572792 ) ) ;
#28973=CARTESIAN_POINT ( 'NONE',  ( 4.542534705770139070, -50.32490493678626109, 25.70492051762469288 ) ) ;
#28977=CARTESIAN_POINT ( 'NONE',  ( 0.7462550633098445907, -51.18586255738846802, 29.54662903476010882 ) ) ;
#28981=CARTESIAN_POINT ( 'NONE',  ( 7.757384923554905498, -50.74999999999999289, 29.19375250200204164 ) ) ;
#28986=CARTESIAN_POINT ( 'NONE',  ( 7.567941867304905479, -50.01145833381128369, 27.28240155936039812 ) ) ;
#28987=CARTESIAN_POINT ( 'NONE',  ( 0.7573849235549120484, -45.95833333333332149, 31.21447844416572792 ) ) ;
#28989=CARTESIAN_POINT ( 'NONE',  ( 1.178321774070217209, -48.65447275059298704, 30.91595237883363723 ) ) ;
#28994=( BOUNDED_CURVE ( )  B_SPLINE_CURVE ( 2, ( #23048, #9245, #22216, #6049, #31996, #3280, #2862, #32615, #38801 ),
 .UNSPECIFIED., .F., .F. ) 
 B_SPLINE_CURVE_WITH_KNOTS ( ( 3, 2, 2, 2, 3 ),
 ( 0.5374999999999999778, 0.5416666666666666297, 0.5500000000000000444, 0.5583333333333333481, 0.5625000000000000000 ),
 .UNSPECIFIED. ) 
 CURVE ( )  GEOMETRIC_REPRESENTATION_ITEM ( )  RATIONAL_B_SPLINE_CURVE ( ( 0.9330127018922194093, 0.9330127018922194093, 1.000000000000000000, 0.8660254037844387076, 1.000000000000000000, 0.8660254037844387076, 1.000000000000000000, 0.9330127018922194093, 0.9330127018922194093 ) ) 
 REPRESENTATION_ITEM ( '' )  );
#29003=EDGE_CURVE ( 'NONE', #6186, #15067, #31560, .T. ) ;
#29024=CARTESIAN_POINT ( 'NONE',  ( 4.257384923554909051, -47.51562500047794657, 25.37105061671875461 ) ) ;
#29029=CARTESIAN_POINT ( 'NONE',  ( 7.567941867304905479, -51.55312500047794799, 29.19375250200204164 ) ) ;
#29035=CARTESIAN_POINT ( 'NONE',  ( 2.507384923554909495, -49.44729166657106845, 32.22484141524756751 ) ) ;
#29042=CARTESIAN_POINT ( 'NONE',  ( 6.007384923554907274, -44.36041666762257307, 26.16266358875650866 ) ) ;
#29075=CARTESIAN_POINT ( 'NONE',  ( 0.9468279798049125118, -44.80312500047794799, 29.19375250200204164 ) ) ;
#29081=CARTESIAN_POINT ( 'NONE',  ( 4.257384924376430568, -51.81875000097547002, 25.69375250200204519 ) ) ;
#29126=ADVANCED_FACE ( 'NONE', ( #5437 ), #18833, .F. ) ;
#29127=CARTESIAN_POINT ( 'NONE',  ( 7.567941867304905479, -44.55312500047794799, 29.19375250200204164 ) ) ;
#29135=CARTESIAN_POINT ( 'NONE',  ( 4.257384923554909051, -44.51562500047793947, 25.37105061671875106 ) ) ;
#29141=ADVANCED_FACE ( 'NONE', ( #12667, #25437 ), #41814, .T. ) ;
#29156=CARTESIAN_POINT ( 'NONE',  ( 0.7573849235549138248, -44.54166666666666430, 27.17302655983835180 ) ) ;
#29164=CARTESIAN_POINT ( 'NONE',  ( 5.912663395429905044, -50.63645833381128369, 32.06077891596451224 ) ) ;
#29165=DIRECTION ( 'NONE',  ( -0.000000000000000000, -1.000000000000000000, -0.000000000000000000 ) ) ;
#29168=CARTESIAN_POINT ( 'NONE',  ( 2.507384923554911715, -46.08333333333332149, 26.16266358875650866 ) ) ;
#29173=CARTESIAN_POINT ( 'NONE',  ( 7.543520603492674503, -43.47513858521659813, 30.48983315170279695 ) ) ;
#29174=CARTESIAN_POINT ( 'NONE',  ( 0.9468279798049132889, -48.39062500047794657, 29.19375250200204164 ) ) ;
#29177=CARTESIAN_POINT ( 'NONE',  ( 4.630631976088899648, 3.250000000000000444, 35.13541431052434660 ) ) ;
#29179=CARTESIAN_POINT ( 'NONE',  ( 2.507384923554911715, -51.08333333333332860, 26.16266358875650866 ) ) ;
#29180=CARTESIAN_POINT ( 'NONE',  ( 7.757384923554904610, -45.20833333333333570, 27.17302655983835180 ) ) ;
#29183=AXIS2_PLACEMENT_3D ( 'NONE', #38454, #12929, #25905 ) ;
#29186=CARTESIAN_POINT ( 'NONE',  ( 0.7573849235549129366, -45.99999999999999289, 29.19375250200204164 ) ) ;
#29188=CARTESIAN_POINT ( 'NONE',  ( 3.972765932095535746, -48.81198303460183752, 25.70487737982361409 ) ) ;
#29198=VERTEX_POINT ( 'NONE', #16085 ) ;
#29214=CARTESIAN_POINT ( 'NONE',  ( 4.257386978954926349, -46.06866506076136147, 32.69375250200084793 ) ) ;
#29221=CARTESIAN_POINT ( 'NONE',  ( 0.9468279798049143992, -48.93229166714461087, 27.28240155936039812 ) ) ;
#29225=CARTESIAN_POINT ( 'NONE',  ( 2.602106451679909505, -50.71979166714461940, 32.06077891596451224 ) ) ;
#29232=CARTESIAN_POINT ( 'NONE',  ( 2.507384923554909495, -47.94729166657106845, 32.22484141524756751 ) ) ;
#29235=ORIENTED_EDGE ( 'NONE', *, *, #37475, .T. ) ;
#29240=( BOUNDED_CURVE ( )  B_SPLINE_CURVE ( 2, ( #26648, #33229, #29614, #39608, #23463, #20481, #36427, #4310, #17292 ),
 .UNSPECIFIED., .F., .T. ) 
 B_SPLINE_CURVE_WITH_KNOTS ( ( 3, 2, 2, 2, 3 ),
 ( 0.8624999999999999334, 0.8666666666666666963, 0.8750000000000000000, 0.8833333333333333037, 0.8875000000000000666 ),
 .UNSPECIFIED. ) 
 CURVE ( )  GEOMETRIC_REPRESENTATION_ITEM ( )  RATIONAL_B_SPLINE_CURVE ( ( 0.9330127018922194093, 0.9330127018922185211, 1.000000000000000000, 0.8660254037844387076, 1.000000000000000000, 0.8660254037844387076, 1.000000000000000000, 0.9330127018922185211, 0.9330127018922194093 ) ) 
 REPRESENTATION_ITEM ( '' )  );
#29241=CARTESIAN_POINT ( 'NONE',  ( 6.007384923554904610, -45.02708333428923737, 32.22484141524757462 ) ) ;
#29242=CYLINDRICAL_SURFACE ( 'NONE', #35377, 3.499999999999996003 ) ;
#29243=VERTEX_POINT ( 'NONE', #4446 ) ;
#29278=CARTESIAN_POINT ( 'NONE',  ( 5.912663395429905044, -47.13645833381128369, 32.06077891596451224 ) ) ;
#29294=EDGE_CURVE ( 'NONE', #7185, #34443, #27635, .T. ) ;
#29299=CARTESIAN_POINT ( 'NONE',  ( 1.579978953920546880, -50.75005515726860494, 26.93759995285082454 ) ) ;
#29312=DIRECTION ( 'NONE',  ( -0.000000000000000000, -1.000000000000000000, -0.000000000000000000 ) ) ;
#29344=CARTESIAN_POINT ( 'NONE',  ( 5.912663395429907709, -44.55729166714461797, 26.32672608803957459 ) ) ;
#29376=CARTESIAN_POINT ( 'NONE',  ( 4.257384923554908163, -51.67812500047794799, 33.01645438728532866 ) ) ;
#29380=CARTESIAN_POINT ( 'NONE',  ( 4.257384923554908163, -45.87499999999999289, 33.23520438632941421 ) ) ;
#29382=CARTESIAN_POINT ( 'NONE',  ( 4.257384923554909939, -52.75000000000000000, 25.69375250200204519 ) ) ;
#29384=CARTESIAN_POINT ( 'NONE',  ( 4.257384923554909051, -52.75000000000000000, 25.69375250200204519 ) ) ;
#29387=CARTESIAN_POINT ( 'NONE',  ( 7.567941867304904591, -49.09895833381128227, 27.28240155936039812 ) ) ;
#29394=CARTESIAN_POINT ( 'NONE',  ( 0.7573849235549129366, -50.49999999999998579, 29.19375250200204164 ) ) ;
#29399=CARTESIAN_POINT ( 'NONE',  ( 4.257373627235431890, -46.56920070325035255, 32.69375250196738847 ) ) ;
#29403=CARTESIAN_POINT ( 'NONE',  ( 0.8281876886673197324, -48.67826584204664186, 29.90909137722739075 ) ) ;
#29407=CARTESIAN_POINT ( 'NONE',  ( 0.7573849235549129366, -50.69375000095590167, 29.19375250200204164 ) ) ;
#29422=CARTESIAN_POINT ( 'NONE',  ( 6.007384923554904610, -42.52708333428924448, 32.22484141524757462 ) ) ;
#29436=CARTESIAN_POINT ( 'NONE',  ( 2.602106451679909505, -45.80729166714461797, 32.06077891596451224 ) ) ;
#29440=CARTESIAN_POINT ( 'NONE',  ( 7.567941867304905479, -51.05312500047794799, 29.19375250200204164 ) ) ;
#29447=CARTESIAN_POINT ( 'NONE',  ( 0.7573849235549129366, -47.53062499990440415, 29.19375250200204164 ) ) ;
#29454=CARTESIAN_POINT ( 'NONE',  ( 4.257384923554908163, -45.06875000095590877, 33.23520438632941421 ) ) ;
#29455=CARTESIAN_POINT ( 'NONE',  ( 0.7573849235549120484, -43.65208333428924448, 31.21447844416572792 ) ) ;
#29456=AXIS2_PLACEMENT_3D ( 'NONE', #28083, #40438, #34263 ) ;
#29459=CARTESIAN_POINT ( 'NONE',  ( 3.319562750045980337, -43.10267090063072715, 25.69375250200204519 ) ) ;
#29473=CARTESIAN_POINT ( 'NONE',  ( 3.083781589471024542, -51.79081263043109118, 25.85356938787166570 ) ) ;
#29494=CARTESIAN_POINT ( 'NONE',  ( 0.9468279798049134000, -42.34479166714461940, 27.28240155936039457 ) ) ;
#29504=CARTESIAN_POINT ( 'NONE',  ( 0.9221606767940556670, -42.40512242781733221, 30.29131972140003981 ) ) ;
#29516=CARTESIAN_POINT ( 'NONE',  ( 2.507384923554911715, -51.27708333428923737, 26.16266358875650866 ) ) ;
#29519=CARTESIAN_POINT ( 'NONE',  ( 0.7573849235549120484, -51.95833333333331439, 31.21447844416572792 ) ) ;
#29520=VECTOR ( 'NONE', #9563, 1000.000000000000000 ) ;
#29541=CARTESIAN_POINT ( 'NONE',  ( 4.257384923554896616, -48.12499999999998579, 25.69375250200204519 ) ) ;
#29545=CARTESIAN_POINT ( 'NONE',  ( 5.173502482472142283, -49.83905443926843049, 25.78484812725744035 ) ) ;
#29556=CARTESIAN_POINT ( 'NONE',  ( 5.912663395429907709, -42.96979166714461940, 26.32672608803957459 ) ) ;
#29559=ORIENTED_EDGE ( 'NONE', *, *, #24145, .F. ) ;
#29568=ADVANCED_FACE ( 'NONE', ( #37670 ), #8529, .T. ) ;
#29570=CARTESIAN_POINT ( 'NONE',  ( 7.691984149497818279, -45.95987976028958855, 30.00395136325351331 ) ) ;
#29593=CARTESIAN_POINT ( 'NONE',  ( 4.257384923554909051, -51.92812500047794799, 25.37105061671875461 ) ) ;
#29594=CARTESIAN_POINT ( 'NONE',  ( 0.9927745011854999246, -47.16403644771965986, 30.52993055814623347 ) ) ;
#29597=CARTESIAN_POINT ( 'NONE',  ( 7.757384923554902834, -47.29166666666665719, 31.21447844416572792 ) ) ;
#29603=CARTESIAN_POINT ( 'NONE',  ( 5.920669429198600398, -43.35682288729847045, 26.08430258552080616 ) ) ;
#29604=CARTESIAN_POINT ( 'NONE',  ( 4.257384923554908163, -50.26562500047794657, 33.01645438728532866 ) ) ;
#29610=CARTESIAN_POINT ( 'NONE',  ( 7.757384923554902834, -50.79166666666665719, 31.21447844416572792 ) ) ;
#29611=CARTESIAN_POINT ( 'NONE',  ( 0.9468279798049143992, -49.43229166714461087, 27.28240155936039457 ) ) ;
#29612=ORIENTED_EDGE ( 'NONE', *, *, #14756, .T. ) ;
#29614=CARTESIAN_POINT ( 'NONE',  ( 2.507384923554911715, -43.58333333333332149, 26.16266358875650866 ) ) ;
#29621=CARTESIAN_POINT ( 'NONE',  ( 7.757384923554904610, -50.90208333428924448, 27.17302655983835180 ) ) ;
#29633=CARTESIAN_POINT ( 'NONE',  ( 3.252675342093400257, -44.09224868242262829, 32.58724094250069925 ) ) ;
#29647=ORIENTED_EDGE ( 'NONE', *, *, #33573, .F. ) ;
#29649=CARTESIAN_POINT ( 'NONE',  ( 7.567941867304904591, -46.09895833381127517, 27.28240155936039812 ) ) ;
#29653=CARTESIAN_POINT ( 'NONE',  ( 4.257384923554908163, -50.17812500047794799, 33.01645438728532866 ) ) ;
#29659=CARTESIAN_POINT ( 'NONE',  ( 0.7573849235549138248, -47.07229166657106845, 27.17302655983835180 ) ) ;
#29662=B_SPLINE_CURVE_WITH_KNOTS ( 'NONE', 3,
 ( #4961, #16221, #19195, #13023, #32374, #26414, #35568, #2822, #41961, #9415, #31952, #35147, #9630, #22379, #25793, #26003, #3237, #35774 ),
 .UNSPECIFIED., .F., .F.,
 ( 4, 2, 2, 2, 2, 2, 2, 2, 4 ),
 ( 0.4443862158066621548, 0.4475577649473410080, 0.4507293140880198612, 0.4539008632286987144, 0.4570724123693775676, 0.4602439615100563652, 0.4634155106507352184, 0.4665870597914140716, 0.4697586089320929248 ),
 .UNSPECIFIED. ) ;
#29663=ORIENTED_EDGE ( 'NONE', *, *, #12739, .T. ) ;
#29664=ORIENTED_EDGE ( 'NONE', *, *, #16575, .T. ) ;
#29667=CARTESIAN_POINT ( 'NONE',  ( 7.757384923554904610, -43.90208333428925158, 27.17302655983835180 ) ) ;
#29668=CARTESIAN_POINT ( 'NONE',  ( 7.757384923554904610, -44.90208333428923737, 27.17302655983835180 ) ) ;
#29689=CARTESIAN_POINT ( 'NONE',  ( 0.7980479019723020206, -51.70747884063762001, 28.53812147572290669 ) ) ;
#29705=PLANE ( 'NONE',  #253 ) ;
#29709=CARTESIAN_POINT ( 'NONE',  ( 2.602106451679909505, -43.71979166714461940, 32.06077891596451224 ) ) ;
#29712=CARTESIAN_POINT ( 'NONE',  ( 7.761282395711493365, -43.95657515630785639, 29.68725950006516712 ) ) ;
#29718=CARTESIAN_POINT ( 'NONE',  ( 1.273635590791570849, -42.40443913519641228, 27.34205447556008650 ) ) ;
#29722=CARTESIAN_POINT ( 'NONE',  ( 4.241737398881509691, -44.31837742377857126, 25.69378524721488333 ) ) ;
#29726=ORIENTED_EDGE ( 'NONE', *, *, #1717, .T. ) ;
#29727=CARTESIAN_POINT ( 'NONE',  ( 1.208596878131372732, -50.65097713590605366, 30.99419647321455784 ) ) ;
#29728=CARTESIAN_POINT ( 'NONE',  ( 0.7573849235549138248, -43.04166666666666430, 27.17302655983835180 ) ) ;
#29750=EDGE_CURVE ( 'NONE', #15341, #7238, #25913, .T. ) ;
#29752=DIRECTION ( 'NONE',  ( -0.000000000000000000, 1.000000000000000000, -0.000000000000000000 ) ) ;
#29763=VECTOR ( 'NONE', #6581, 1000.000000000000000 ) ;
#29767=CARTESIAN_POINT ( 'NONE',  ( 0.9468279798049134000, -42.34479166714461940, 27.28240155936039102 ) ) ;
#29773=CARTESIAN_POINT ( 'NONE',  ( 2.602106451679911281, -49.38645833381128369, 26.32672608803957459 ) ) ;
#29775=VECTOR ( 'NONE', #13238, 1000.000000000000000 ) ;
#29790=CARTESIAN_POINT ( 'NONE',  ( 5.195207097063846646, -45.85267090063072715, 32.69375250200202743 ) ) ;
#29804=CARTESIAN_POINT ( 'NONE',  ( 4.257384923554909051, -50.42812500047794799, 25.37105061671875461 ) ) ;
#29808=CARTESIAN_POINT ( 'NONE',  ( 7.757384923554905498, -48.24999999999998579, 29.19375250200204164 ) ) ;
#29811=CARTESIAN_POINT ( 'NONE',  ( 4.257384923554907274, -51.37499999999998579, 32.69375250200203453 ) ) ;
#29812=ADVANCED_FACE ( 'NONE', ( #24502 ), #24294, .T. ) ;
#29818=CARTESIAN_POINT ( 'NONE',  ( 5.912663395429904156, -48.22395833381128227, 32.06077891596451224 ) ) ;
#29824=CARTESIAN_POINT ( 'NONE',  ( 4.257384923554909051, -46.62499999999999289, 25.15230061767466552 ) ) ;
#29825=CARTESIAN_POINT ( 'NONE',  ( 4.257384923554909051, -51.01562500047795368, 25.37105061671875106 ) ) ;
#29835=CARTESIAN_POINT ( 'NONE',  ( 0.7573849235549129366, -49.69375000095590167, 29.19375250200204164 ) ) ;
#29863=ADVANCED_FACE ( 'NONE', ( #8325 ), #30669, .F. ) ;
#29864=CARTESIAN_POINT ( 'NONE',  ( 4.257384923554909051, -45.51562500047795368, 25.37105061671875461 ) ) ;
#29868=CARTESIAN_POINT ( 'NONE',  ( 7.567941867304902814, -46.59479166714461229, 31.10510344464368870 ) ) ;
#29871=( BOUNDED_CURVE ( )  B_SPLINE_CURVE ( 2, ( #27161, #24388, #40127, #10995, #7810, #20786, #37357, #21185, #27779 ),
 .UNSPECIFIED., .F., .T. ) 
 B_SPLINE_CURVE_WITH_KNOTS ( ( 3, 2, 2, 2, 3 ),
 ( 0.4375000000000000000, 0.4416666666666666519, 0.4500000000000000111, 0.4583333333333333148, 0.4625000000000000222 ),
 .UNSPECIFIED. ) 
 CURVE ( )  GEOMETRIC_REPRESENTATION_ITEM ( )  RATIONAL_B_SPLINE_CURVE ( ( 0.9330127018922194093, 0.9330127018922194093, 1.000000000000000000, 0.8660254037844387076, 1.000000000000000000, 0.8660254037844387076, 1.000000000000000000, 0.9330127018922189652, 0.9330127018922194093 ) ) 
 REPRESENTATION_ITEM ( '' )  );
#29875=CARTESIAN_POINT ( 'NONE',  ( 0.7573849235549120484, -48.48895833323773985, 31.21447844416572792 ) ) ;
#29883=CARTESIAN_POINT ( 'NONE',  ( 6.007384923554907274, -44.36041666762257307, 26.16266358875650866 ) ) ;
#29885=ORIENTED_EDGE ( 'NONE', *, *, #40918, .T. ) ;
#29889=DIRECTION ( 'NONE',  ( 0.000000000000000000, 1.000000000000000000, 0.000000000000000000 ) ) ;
#29892=CARTESIAN_POINT ( 'NONE',  ( 4.257384923554909051, -52.75000000000000000, 29.19375250200204164 ) ) ;
#29898=VECTOR ( 'NONE', #14169, 1000.000000000000000 ) ;
#29920=CARTESIAN_POINT ( 'NONE',  ( 0.9468279798049125118, -42.30312500047794799, 29.19375250200204164 ) ) ;
#29921=FACE_OUTER_BOUND ( 'NONE', #6761, .T. ) ;
#29929=CARTESIAN_POINT ( 'NONE',  ( 1.808430394464034086, -42.40553076861114334, 26.67726045672475266 ) ) ;
#29933=CARTESIAN_POINT ( 'NONE',  ( 2.160902675073581136, -44.26684287379865879, 26.36684526822706331 ) ) ;
#29939=CARTESIAN_POINT ( 'NONE',  ( 2.732834802411810315, -42.41129881240816246, 32.35500496349436617 ) ) ;
#29957=CARTESIAN_POINT ( 'NONE',  ( 2.507384923554909495, -44.41666666666665719, 32.22484141524756751 ) ) ;
#29964=CARTESIAN_POINT ( 'NONE',  ( 7.757384923554904610, -47.20833333333332149, 27.17302655983835180 ) ) ;
#29966=CARTESIAN_POINT ( 'NONE',  ( 4.257406269681411004, -45.56789735307413736, 32.69375250187820825 ) ) ;
#29977=VERTEX_POINT ( 'NONE', #8533 ) ;
#29984=CARTESIAN_POINT ( 'NONE',  ( 4.257384923554909051, -45.42812500047795510, 25.37105061671875461 ) ) ;
#29989=CARTESIAN_POINT ( 'NONE',  ( 5.992657237601167530, -45.85846872874419944, 26.12101365305726475 ) ) ;
#30013=CARTESIAN_POINT ( 'NONE',  ( 7.757384923554904610, -44.20833333333332149, 27.17302655983835180 ) ) ;
#30016=CARTESIAN_POINT ( 'NONE',  ( 2.602106451679909505, -50.21979166714461940, 32.06077891596451224 ) ) ;
#30022=CARTESIAN_POINT ( 'NONE',  ( 0.7573849235549129366, -47.49999999999999289, 29.19375250200204164 ) ) ;
#30023=ORIENTED_EDGE ( 'NONE', *, *, #38902, .F. ) ;
#30026=CARTESIAN_POINT ( 'NONE',  ( 2.985734175343026209, -49.09750057137531343, 32.47016482631166667 ) ) ;
#30030=CARTESIAN_POINT ( 'NONE',  ( 7.567941867304904591, -49.64062500047794657, 29.19375250200204164 ) ) ;
#30036=CARTESIAN_POINT ( 'NONE',  ( 4.257384923554909051, -48.62499999999999289, 25.15230061767466552 ) ) ;
#30037=CARTESIAN_POINT ( 'NONE',  ( 0.9468279798049132889, -51.89062500047794657, 29.19375250200204164 ) ) ;
#30040=CARTESIAN_POINT ( 'NONE',  ( 1.573552204378268149, -43.13771038209208797, 31.44031508315671530 ) ) ;
#30048=CARTESIAN_POINT ( 'NONE',  ( 0.7573849235549120484, -50.65208333428923737, 31.21447844416572792 ) ) ;
#30075=CARTESIAN_POINT ( 'NONE',  ( 2.602106451679909505, -45.30729166714461797, 32.06077891596451224 ) ) ;
#30081=CARTESIAN_POINT ( 'NONE',  ( 5.912663395429907709, -48.46979166714461229, 26.32672608803957459 ) ) ;
#30087=CARTESIAN_POINT ( 'NONE',  ( 4.257384923554909051, -45.15562499990439704, 25.15230061767466552 ) ) ;
#30091=CARTESIAN_POINT ( 'NONE',  ( 4.257384923554909051, -44.31875000095590167, 25.15230061767466552 ) ) ;
#30092=CARTESIAN_POINT ( 'NONE',  ( 4.257384923554909939, -52.75000000000000000, 34.69375250200203453 ) ) ;
#30121=CARTESIAN_POINT ( 'NONE',  ( 7.425301425433979752, -50.90910804929642808, 27.70541345816713275 ) ) ;
#30131=CARTESIAN_POINT ( 'NONE',  ( 0.9468279798049115126, -43.76145833381129080, 31.10510344464368515 ) ) ;
#30132=CARTESIAN_POINT ( 'NONE',  ( 0.7573849235549129366, -48.49999999999998579, 29.19375250200204164 ) ) ;
#30139=CARTESIAN_POINT ( 'NONE',  ( 3.208508050662746580, -42.40319028618246477, 25.84327095886215631 ) ) ;
#30143=CARTESIAN_POINT ( 'NONE',  ( 3.572165792437857590, -44.30251055891951495, 25.75796499744019030 ) ) ;
#30144=CARTESIAN_POINT ( 'NONE',  ( 0.7909271606244239194, -50.21140335626795093, 28.48882664525053343 ) ) ;
#30150=CARTESIAN_POINT ( 'NONE',  ( 4.257384923554908163, -51.56875000095590877, 33.23520438632941421 ) ) ;
#30151=CARTESIAN_POINT ( 'NONE',  ( 3.044482980331683741, -42.29615616597446603, 32.27411873898371653 ) ) ;
#30169=EDGE_CURVE ( 'NONE', #321, #40959, #28928, .T. ) ;
#30172=CARTESIAN_POINT ( 'NONE',  ( 7.712613168901164329, -42.92878591757344253, 28.55116430672686789 ) ) ;
#30177=CARTESIAN_POINT ( 'NONE',  ( 3.135666725655635201, -47.79353590434853061, 25.87055444772102675 ) ) ;
#30200=CARTESIAN_POINT ( 'NONE',  ( 2.602106451679911281, -45.38645833381128369, 26.32672608803957459 ) ) ;
#30205=CARTESIAN_POINT ( 'NONE',  ( 5.327903877006456845, -46.04315631083164817, 32.53361966697914909 ) ) ;
#30232=CARTESIAN_POINT ( 'NONE',  ( 4.257384923554909051, -48.92812500047794089, 25.37105061671875461 ) ) ;
#30236=CARTESIAN_POINT ( 'NONE',  ( 0.7573849235549129366, -43.49999999999999289, 29.19375250200204164 ) ) ;
#30239=CARTESIAN_POINT ( 'NONE',  ( 4.257384923554909051, -42.40485061181025372, 29.19375250200204164 ) ) ;
#30241=CARTESIAN_POINT ( 'NONE',  ( 3.137392399014917288, -49.29199330512964394, 25.86393627527463224 ) ) ;
#30245=CARTESIAN_POINT ( 'NONE',  ( 2.602106451679909505, -46.30729166714461797, 32.06077891596451224 ) ) ;
#30248=ORIENTED_EDGE ( 'NONE', *, *, #3311, .T. ) ;
#30251=CARTESIAN_POINT ( 'NONE',  ( 6.007384923554907274, -48.66666666666665719, 26.16266358875650866 ) ) ;
#30252=CARTESIAN_POINT ( 'NONE',  ( 5.912663395429904156, -51.72395833381127517, 32.06077891596451224 ) ) ;
#30263=CARTESIAN_POINT ( 'NONE',  ( 6.007384923554907274, -48.86041666762257307, 26.16266358875650866 ) ) ;
#30276=CARTESIAN_POINT ( 'NONE',  ( 2.507384923554909495, -43.11041666762257307, 32.22484141524756751 ) ) ;
#30290=CARTESIAN_POINT ( 'NONE',  ( 5.912663395429904156, -45.72395833381128227, 32.06077891596451224 ) ) ;
#30298=CARTESIAN_POINT ( 'NONE',  ( 7.757384923554904610, -46.23895833323772564, 27.17302655983835180 ) ) ;
#30304=CARTESIAN_POINT ( 'NONE',  ( 7.757384923554905498, -43.44375000095590167, 29.19375250200204164 ) ) ;
#30310=CYLINDRICAL_SURFACE ( 'NONE', #5110, 3.499999999999996003 ) ;
#30327=DIRECTION ( 'NONE',  ( -0.000000000000000000, -1.000000000000000000, -0.000000000000000000 ) ) ;
#30331=CARTESIAN_POINT ( 'NONE',  ( 5.189085141169427651, -50.83934484251926733, 25.78801598714841958 ) ) ;
#30341=CARTESIAN_POINT ( 'NONE',  ( 7.567941867304905479, -42.55312500047794799, 29.19375250200204164 ) ) ;
#30350=CARTESIAN_POINT ( 'NONE',  ( 4.574053741823596475, -48.56117271074194264, 32.68319764452591869 ) ) ;
#30353=ADVANCED_FACE ( 'NONE', ( #4344 ), #30496, .T. ) ;
#30355=CARTESIAN_POINT ( 'NONE',  ( 4.257450628761716871, -44.31875150865747770, 25.69375250261877852 ) ) ;
#30362=CARTESIAN_POINT ( 'NONE',  ( 2.507384923554909495, -49.61041666762257307, 32.22484141524756751 ) ) ;
#30363=CARTESIAN_POINT ( 'NONE',  ( 7.567941867304902814, -42.59895833381128227, 27.28240155936039457 ) ) ;
#30368=LINE ( 'NONE', #24622, #18277 ) ;
#30375=( BOUNDED_CURVE ( )  B_SPLINE_CURVE ( 2, ( #24982, #18591, #31759, #37943, #8805, #34748, #28574, #11368, #38360 ),
 .UNSPECIFIED., .F., .T. ) 
 B_SPLINE_CURVE_WITH_KNOTS ( ( 3, 2, 2, 2, 3 ),
 ( 0.8375000000000000222, 0.8416666666666666741, 0.8499999999999999778, 0.8583333333333332815, 0.8624999999999999334 ),
 .UNSPECIFIED. ) 
 CURVE ( )  GEOMETRIC_REPRESENTATION_ITEM ( )  RATIONAL_B_SPLINE_CURVE ( ( 0.9330127018922194093, 0.9330127018922194093, 1.000000000000000000, 0.8660254037844387076, 1.000000000000000000, 0.8660254037844387076, 1.000000000000000000, 0.9330127018922202975, 0.9330127018922194093 ) ) 
 REPRESENTATION_ITEM ( '' )  );
#30384=CARTESIAN_POINT ( 'NONE',  ( 5.359079145924995125, -42.84438428034778923, 25.85022418778922670 ) ) ;
#30402=EDGE_LOOP ( 'NONE', ( #20799, #1886, #29612, #30982 ) ) ;
#30405=ORIENTED_EDGE ( 'NONE', *, *, #23828, .F. ) ;
#30413=CARTESIAN_POINT ( 'NONE',  ( 0.9468279798049115126, -46.26145833381128369, 31.10510344464368515 ) ) ;
#30428=CARTESIAN_POINT ( 'NONE',  ( 4.630631976088899648, 3.250000000000000444, 35.13541431052434660 ) ) ;
#30443=CARTESIAN_POINT ( 'NONE',  ( 0.9468279798049134000, -49.34479166714461940, 27.28240155936039457 ) ) ;
#30447=CARTESIAN_POINT ( 'NONE',  ( 6.007384923554907274, -44.66666666666665719, 26.16266358875650866 ) ) ;
#30454=CARTESIAN_POINT ( 'NONE',  ( 0.9468279798049124008, -46.34895833381128227, 31.10510344464368515 ) ) ;
#30458=CARTESIAN_POINT ( 'NONE',  ( 4.257384923554909051, -52.75000000000000000, 29.19375250200204164 ) ) ;
#30460=CARTESIAN_POINT ( 'NONE',  ( 0.7573849235549129366, -46.49999999999999289, 29.19375250200204164 ) ) ;
#30461=CARTESIAN_POINT ( 'NONE',  ( 5.912663395429907709, -51.55729166714461797, 26.32672608803957459 ) ) ;
#30465=CARTESIAN_POINT ( 'NONE',  ( 1.724453646921511707, -43.13231259820148011, 31.61439615956409455 ) ) ;
#30468=DIRECTION ( 'NONE',  ( 0.000000000000000000, 0.000000000000000000, -1.000000000000000000 ) ) ;
#30472=CARTESIAN_POINT ( 'NONE',  ( 6.007384923554904610, -46.02708333428923737, 32.22484141524757462 ) ) ;
#30482=CARTESIAN_POINT ( 'NONE',  ( 7.666291964556426031, -44.92227858612246649, 28.27764524214758879 ) ) ;
#30496=CYLINDRICAL_SURFACE ( 'NONE', #17557, 3.499999999999996003 ) ;
#30498=CARTESIAN_POINT ( 'NONE',  ( 5.912663395429904156, -43.72395833381127517, 32.06077891596451224 ) ) ;
#30503=CARTESIAN_POINT ( 'NONE',  ( 6.895067737584072098, -44.38758398380049641, 26.86046860018497995 ) ) ;
#30506=VERTEX_POINT ( 'NONE', #17325 ) ;
#30507=CARTESIAN_POINT ( 'NONE',  ( 0.7573849235549129366, -45.53062499990440415, 29.19375250200204164 ) ) ;
#30510=ORIENTED_EDGE ( 'NONE', *, *, #19689, .T. ) ;
#30513=CARTESIAN_POINT ( 'NONE',  ( 6.007384923554904610, -50.83333333333332860, 32.22484141524757462 ) ) ;
#30514=CARTESIAN_POINT ( 'NONE',  ( 0.7573849235549138248, -42.23541666762257307, 27.17302655983835180 ) ) ;
#30515=DIRECTION ( 'NONE',  ( -0.000000000000000000, -1.000000000000000000, -0.000000000000000000 ) ) ;
#30519=FACE_OUTER_BOUND ( 'NONE', #5293, .T. ) ;
#30530=CARTESIAN_POINT ( 'NONE',  ( 4.389810430224767579, -51.32190178482158416, 25.69590247710682362 ) ) ;
#30541=CARTESIAN_POINT ( 'NONE',  ( 7.478334101600789374, -50.91215596758620876, 27.82260484730123196 ) ) ;
#30551=CARTESIAN_POINT ( 'NONE',  ( 5.912663395429907709, -49.55729166714461087, 26.32672608803957459 ) ) ;
#30555=CARTESIAN_POINT ( 'NONE',  ( 4.257393643264853367, -45.06839824424229590, 32.69375250198117300 ) ) ;
#30560=EDGE_CURVE ( 'NONE', #1417, #27430, #32674, .T. ) ;
#30561=CARTESIAN_POINT ( 'NONE',  ( 4.257384923554909051, -52.75000000000000000, 29.19375250200204164 ) ) ;
#30572=CARTESIAN_POINT ( 'NONE',  ( 0.7573849235549129366, -50.19375000095590167, 29.19375250200204164 ) ) ;
#30573=CARTESIAN_POINT ( 'NONE',  ( 0.9468279798049132889, -42.89062500047794657, 29.19375250200204164 ) ) ;
#30575=DIRECTION ( 'NONE',  ( -0.000000000000000000, -1.000000000000000000, -0.000000000000000000 ) ) ;
#30596=CARTESIAN_POINT ( 'NONE',  ( 4.257420362424698901, -42.81875084473693249, 25.69375250218146078 ) ) ;
#30606=CARTESIAN_POINT ( 'NONE',  ( 5.853331401024200353, -48.85741974055400050, 26.05617601532485850 ) ) ;
#30616=ORIENTED_EDGE ( 'NONE', *, *, #26428, .F. ) ;
#30620=CARTESIAN_POINT ( 'NONE',  ( 4.257384923554908163, -47.17812500047795510, 33.01645438728532866 ) ) ;
#30623=( BOUNDED_CURVE ( )  B_SPLINE_CURVE ( 2, ( #15001, #37542, #11798, #34766, #18397, #31369, #8396, #22009, #41368 ),
 .UNSPECIFIED., .F., .T. ) 
 B_SPLINE_CURVE_WITH_KNOTS ( ( 3, 2, 2, 2, 3 ),
 ( 0.8875000000000000666, 0.8916666666666667185, 0.9000000000000000222, 0.9083333333333333259, 0.9124999999999999778 ),
 .UNSPECIFIED. ) 
 CURVE ( )  GEOMETRIC_REPRESENTATION_ITEM ( )  RATIONAL_B_SPLINE_CURVE ( ( 0.9330127018922194093, 0.9330127018922202975, 1.000000000000000000, 0.8660254037844387076, 1.000000000000000000, 0.8660254037844387076, 1.000000000000000000, 0.9330127018922194093, 0.9330127018922194093 ) ) 
 REPRESENTATION_ITEM ( '' )  );
#30637=CARTESIAN_POINT ( 'NONE',  ( 1.178306903736272115, -46.15447346524587147, 30.91592691177982033 ) ) ;
#30655=CARTESIAN_POINT ( 'NONE',  ( 7.567941867304904591, -49.09479166714461940, 31.10510344464368870 ) ) ;
#30658=CARTESIAN_POINT ( 'NONE',  ( 2.507384923554909495, -43.41666666666665719, 32.22484141524756751 ) ) ;
#30664=CARTESIAN_POINT ( 'NONE',  ( 7.567941867304904591, -45.59895833381128227, 27.28240155936039812 ) ) ;
#30669=PLANE ( 'NONE',  #36056 ) ;
#30671=CARTESIAN_POINT ( 'NONE',  ( 7.757384923554904610, -47.70833333333332149, 27.17302655983835180 ) ) ;
#30672=CARTESIAN_POINT ( 'NONE',  ( 0.9468279798049132889, -46.89062500047794657, 29.19375250200204164 ) ) ;
#30684=CARTESIAN_POINT ( 'NONE',  ( 0.7573849235549120484, -47.15208333428923737, 31.21447844416572792 ) ) ;
#30686=DIRECTION ( 'NONE',  ( -0.000000000000000000, -1.000000000000000000, -0.000000000000000000 ) ) ;
#30693=CARTESIAN_POINT ( 'NONE',  ( 7.056226735115116888, -44.89116796313548008, 27.04284938014511042 ) ) ;
#30699=CARTESIAN_POINT ( 'NONE',  ( 3.799078257082286303, -49.80860757437761066, 25.69375250017361978 ) ) ;
#30709=ORIENTED_EDGE ( 'NONE', *, *, #11153, .F. ) ;
#30715=CARTESIAN_POINT ( 'NONE',  ( 2.602106451679909505, -42.80729166714461797, 32.06077891596451224 ) ) ;
#30722=CARTESIAN_POINT ( 'NONE',  ( 7.757384923554905498, -46.28062499990440415, 29.19375250200204164 ) ) ;
#30729=CARTESIAN_POINT ( 'NONE',  ( 0.7573849235549120484, -42.15208333428924448, 31.21447844416572792 ) ) ;
#30743=CARTESIAN_POINT ( 'NONE',  ( 6.372183304109785063, -51.51591946026449165, 32.03308327703522451 ) ) ;
#30754=DIRECTION ( 'NONE',  ( 0.000000000000000000, 0.7071067811865500152, 0.7071067811865451302 ) ) ;
#30763=CARTESIAN_POINT ( 'NONE',  ( 0.9468279798049124008, -49.84895833381128227, 31.10510344464368515 ) ) ;
#30770=ORIENTED_EDGE ( 'NONE', *, *, #40673, .F. ) ;
#30774=ORIENTED_EDGE ( 'NONE', *, *, #35068, .F. ) ;
#30775=CARTESIAN_POINT ( 'NONE',  ( 1.455248144731663862, -50.14168143211132644, 31.34052213912019624 ) ) ;
#30779=CARTESIAN_POINT ( 'NONE',  ( 4.257384923554907274, -45.37499999999999289, 32.69375250200203453 ) ) ;
#30781=CARTESIAN_POINT ( 'NONE',  ( 4.257384923554908163, -49.06875000095590167, 33.23520438632941421 ) ) ;
#30804=CARTESIAN_POINT ( 'NONE',  ( 6.429593709541657987, -43.01487609322006733, 31.98728835514268098 ) ) ;
#30817=CARTESIAN_POINT ( 'NONE',  ( 7.493559478630777093, -48.91284038367965081, 27.78533377108028546 ) ) ;
#30823=EDGE_CURVE ( 'NONE', #6186, #3034, #26421, .T. ) ;
#30827=VERTEX_POINT ( 'NONE', #23013 ) ;
#30830=CARTESIAN_POINT ( 'NONE',  ( 0.9468279798049125118, -46.30312500047794799, 29.19375250200204164 ) ) ;
#30833=CARTESIAN_POINT ( 'NONE',  ( 2.507384923554911715, -51.58333333333332149, 26.16266358875650866 ) ) ;
#30861=CARTESIAN_POINT ( 'NONE',  ( 2.507384923554909495, -51.41666666666665719, 32.22484141524756751 ) ) ;
#30864=CARTESIAN_POINT ( 'NONE',  ( 2.602106451679909505, -47.71979166714461229, 32.06077891596451224 ) ) ;
#30869=CARTESIAN_POINT ( 'NONE',  ( 0.7573849235549120484, -44.45833333333332149, 31.21447844416572792 ) ) ;
#30874=CARTESIAN_POINT ( 'NONE',  ( 5.912663395429904156, -46.72395833381128227, 32.06077891596451224 ) ) ;
#30876=CARTESIAN_POINT ( 'NONE',  ( 0.9468279798049134000, -46.84479166714460519, 27.28240155936039102 ) ) ;
#30878=VERTEX_POINT ( 'NONE', #37061 ) ;
#30882=AXIS2_PLACEMENT_3D ( 'NONE', #9947, #13331, #35869 ) ;
#30886=CARTESIAN_POINT ( 'NONE',  ( 7.757384923554902834, -43.79166666666665009, 31.21447844416572792 ) ) ;
#30887=CARTESIAN_POINT ( 'NONE',  ( 5.912663395429907709, -49.05729166714461087, 26.32672608803957459 ) ) ;
#30898=CARTESIAN_POINT ( 'NONE',  ( 6.007384923554904610, -48.02708333428923737, 32.22484141524757462 ) ) ;
#30908=VECTOR ( 'NONE', #20808, 1000.000000000000000 ) ;
#30925=DIRECTION ( 'NONE',  ( -0.000000000000000000, -1.000000000000000000, -0.000000000000000000 ) ) ;
#30935=CARTESIAN_POINT ( 'NONE',  ( 0.7573849235549120484, -42.98895833323773275, 31.21447844416572792 ) ) ;
#30941=CARTESIAN_POINT ( 'NONE',  ( 5.912663395429905044, -50.63645833381128369, 32.06077891596451224 ) ) ;
#30974=VECTOR ( 'NONE', #40871, 1000.000000000000000 ) ;
#30975=CARTESIAN_POINT ( 'NONE',  ( 0.9468279798049143992, -50.93229166714461797, 27.28240155936039812 ) ) ;
#30978=CARTESIAN_POINT ( 'NONE',  ( 3.339836747840908338, -45.08897923605952940, 32.60236842661326762 ) ) ;
#30980=CARTESIAN_POINT ( 'NONE',  ( 0.9468279798049134000, -51.84479166714461229, 27.28240155936039102 ) ) ;
#30982=ORIENTED_EDGE ( 'NONE', *, *, #23246, .F. ) ;
#30988=ORIENTED_EDGE ( 'NONE', *, *, #3138, .F. ) ;
#30992=CARTESIAN_POINT ( 'NONE',  ( 6.007384923554904610, -49.52708333428924448, 32.22484141524757462 ) ) ;
#30993=CARTESIAN_POINT ( 'NONE',  ( 0.9468279798049124008, -43.34895833381126806, 31.10510344464368515 ) ) ;
#31039=CARTESIAN_POINT ( 'NONE',  ( 7.567941867304904591, -43.09479166714462650, 31.10510344464368870 ) ) ;
#31069=CARTESIAN_POINT ( 'NONE',  ( 7.567941867304905479, -48.01145833381128369, 27.28240155936039812 ) ) ;
#31074=CARTESIAN_POINT ( 'NONE',  ( 4.257384923554909051, -44.12499999999999289, 25.15230061767466552 ) ) ;
#31076=CARTESIAN_POINT ( 'NONE',  ( 4.259130602765983653, -49.31879156463290315, 25.69375245050801482 ) ) ;
#31079=CARTESIAN_POINT ( 'NONE',  ( 7.567941867304904591, -45.64062500047794657, 29.19375250200204164 ) ) ;
#31081=CARTESIAN_POINT ( 'NONE',  ( 7.567941867304902814, -47.09479166714461229, 31.10510344464368870 ) ) ;
#31089=CARTESIAN_POINT ( 'NONE',  ( 0.7573849235549138248, -45.54166666666666430, 27.17302655983835180 ) ) ;
#31090=CARTESIAN_POINT ( 'NONE',  ( 0.9468279798049132889, -47.89062500047795368, 29.19375250200204164 ) ) ;
#31101=CARTESIAN_POINT ( 'NONE',  ( 4.257384923554909051, -46.81875000095590877, 25.15230061767466552 ) ) ;
#31124=( BOUNDED_CURVE ( )  B_SPLINE_CURVE ( 2, ( #9337, #2737, #41456, #38255, #12307, #22509, #32084, #25291, #2951, #9117, #22096 ),
 .UNSPECIFIED., .F., .T. ) 
 B_SPLINE_CURVE_WITH_KNOTS ( ( 3, 2, 2, 2, 2, 3 ),
 ( 0.9690535848485367643, 0.9733731527426199293, 0.9818372671142949759, 0.9903013814859699115, 0.9987654958576448472, 1.000000000000000000 ),
 .UNSPECIFIED. ) 
 CURVE ( )  GEOMETRIC_REPRESENTATION_ITEM ( )  RATIONAL_B_SPLINE_CURVE ( ( 0.9330413444503765641, 0.9316275349052289823, 1.000000000000000000, 0.8660254037844387076, 1.000000000000000000, 0.8660254037844387076, 1.000000000000000000, 0.8660254037844387076, 1.000000000000000000, 0.9804595985059533225, 0.9666191923300708755 ) ) 
 REPRESENTATION_ITEM ( '' )  );
#31133=ORIENTED_EDGE ( 'NONE', *, *, #35068, .T. ) ;
#31137=CARTESIAN_POINT ( 'NONE',  ( 7.757384923554904610, -44.23895833323773275, 27.17302655983835180 ) ) ;
#31142=CARTESIAN_POINT ( 'NONE',  ( 4.257384923554909051, -50.92812500047794799, 25.37105061671875461 ) ) ;
#31144=CARTESIAN_POINT ( 'NONE',  ( 7.757384923554902834, -51.79166666666665719, 31.21447844416572792 ) ) ;
#31173=CARTESIAN_POINT ( 'NONE',  ( 2.602106451679909505, -50.80729166714461797, 32.06077891596451224 ) ) ;
#31177=CARTESIAN_POINT ( 'NONE',  ( 3.798520181849344368, -45.07850937961683258, 32.69375254844382539 ) ) ;
#31186=CARTESIAN_POINT ( 'NONE',  ( 4.257384923554909051, -51.65562499990439704, 25.15230061767466552 ) ) ;
#31188=ORIENTED_EDGE ( 'NONE', *, *, #1747, .F. ) ;
#31193=CARTESIAN_POINT ( 'NONE',  ( 7.757384923554905498, -50.44375000095590167, 29.19375250200204164 ) ) ;
#31198=CARTESIAN_POINT ( 'NONE',  ( 4.241713284453144439, -46.81837696332602405, 25.69378535447121692 ) ) ;
#31223=CARTESIAN_POINT ( 'NONE',  ( 3.802449417361787543, -46.30793265705226247, 25.72156802559478450 ) ) ;
#31230=CARTESIAN_POINT ( 'NONE',  ( 4.257364759755165373, -44.56955858896998279, 32.69375250189113302 ) ) ;
#31232=ORIENTED_EDGE ( 'NONE', *, *, #35309, .T. ) ;
#31241=CARTESIAN_POINT ( 'NONE',  ( 7.567941867304904591, -44.59479166714461940, 31.10510344464368870 ) ) ;
#31259=AXIS2_PLACEMENT_3D ( 'NONE', #6484, #39211, #32622 ) ;
#31260=DIRECTION ( 'NONE',  ( -9.912705577010631430E-15, -1.000000000000000000, 0.000000000000000000 ) ) ;
#31263=CARTESIAN_POINT ( 'NONE',  ( 5.596891108316200736, -45.53674051686331126, 32.43203633017721188 ) ) ;
#31270=CARTESIAN_POINT ( 'NONE',  ( 7.567941867304904591, -47.09479166714461940, 31.10510344464368870 ) ) ;
#31277=CARTESIAN_POINT ( 'NONE',  ( 4.284371476184930749, -49.31939242627632325, 25.69384145547750364 ) ) ;
#31281=CARTESIAN_POINT ( 'NONE',  ( 2.602106451679912169, -43.97395833381127517, 26.32672608803957459 ) ) ;
#31282=CARTESIAN_POINT ( 'NONE',  ( 5.912663395429907709, -48.96979166714461940, 26.32672608803957459 ) ) ;
#31290=CARTESIAN_POINT ( 'NONE',  ( 7.757384923554904610, -44.20833333333332149, 27.17302655983835180 ) ) ;
#31291=CARTESIAN_POINT ( 'NONE',  ( 0.9468279798049132889, -47.39062500047794657, 29.19375250200204164 ) ) ;
#31297=CARTESIAN_POINT ( 'NONE',  ( 7.757384923554905498, -51.94375000095590877, 29.19375250200204164 ) ) ;
#31302=ORIENTED_EDGE ( 'NONE', *, *, #10796, .T. ) ;
#31303=CARTESIAN_POINT ( 'NONE',  ( 7.757384923554902834, -47.98541666762257307, 31.21447844416572792 ) ) ;
#31312=EDGE_CURVE ( 'NONE', #15555, #219, #11591, .T. ) ;
#31325=CARTESIAN_POINT ( 'NONE',  ( 6.017065685135239761, -51.02680624116784713, 32.21963292116841160 ) ) ;
#31336=CARTESIAN_POINT ( 'NONE',  ( 2.602106451679912169, -42.47395833381127517, 26.32672608803957459 ) ) ;
#31339=CARTESIAN_POINT ( 'NONE',  ( 5.648012918662308479, -44.53809828264917314, 32.42458750365793918 ) ) ;
#31344=CARTESIAN_POINT ( 'NONE',  ( 0.7573849235549129366, -42.53062499990439704, 29.19375250200204164 ) ) ;
#31350=CARTESIAN_POINT ( 'NONE',  ( 2.602106451679911281, -50.38645833381128369, 26.32672608803957459 ) ) ;
#31369=CARTESIAN_POINT ( 'NONE',  ( 7.757384923554904610, -43.20833333333332860, 27.17302655983835180 ) ) ;
#31383=CARTESIAN_POINT ( 'NONE',  ( 7.567941867304904591, -50.64062500047794657, 29.19375250200204164 ) ) ;
#31384=DIRECTION ( 'NONE',  ( 0.000000000000000000, 0.000000000000000000, -1.000000000000000000 ) ) ;
#31394=CARTESIAN_POINT ( 'NONE',  ( 7.757384923554904610, -52.23895833323772564, 27.17302655983835180 ) ) ;
#31401=CARTESIAN_POINT ( 'NONE',  ( 4.257384923554908163, -47.06875000095590877, 33.23520438632941421 ) ) ;
#31411=AXIS2_PLACEMENT_3D ( 'NONE', #18978, #6424, #8773 ) ;
#31414=ORIENTED_EDGE ( 'NONE', *, *, #39671, .T. ) ;
#31430=ORIENTED_EDGE ( 'NONE', *, *, #4201, .F. ) ;
#31432=CARTESIAN_POINT ( 'NONE',  ( 3.131892251441531716, -46.29179487483612121, 25.87168539890677010 ) ) ;
#31449=CARTESIAN_POINT ( 'NONE',  ( 5.912663395429905044, -43.63645833381128369, 32.06077891596451224 ) ) ;
#31466=CARTESIAN_POINT ( 'NONE',  ( 9.589638516698011372, 3.250000000000000444, 31.84134197688108614 ) ) ;
#31485=CARTESIAN_POINT ( 'NONE',  ( 7.511084758432211572, -49.41442238476833637, 27.90373615180509859 ) ) ;
#31489=CARTESIAN_POINT ( 'NONE',  ( 7.567941867304902814, -42.68229166714461797, 31.10510344464368870 ) ) ;
#31491=CARTESIAN_POINT ( 'NONE',  ( 2.602106451679909505, -46.21979166714461229, 32.06077891596451224 ) ) ;
#31494=ORIENTED_EDGE ( 'NONE', *, *, #31312, .F. ) ;
#31500=CARTESIAN_POINT ( 'NONE',  ( 0.7573849235549129366, -44.99999999999999289, 29.19375250200204164 ) ) ;
#31501=CARTESIAN_POINT ( 'NONE',  ( 4.257384923554908163, -47.26562500047794657, 33.01645438728532866 ) ) ;
#31513=CARTESIAN_POINT ( 'NONE',  ( 7.757384923554902834, -45.48541666762258018, 31.21447844416572792 ) ) ;
#31528=AXIS2_PLACEMENT_3D ( 'NONE', #16990, #826, #39100 ) ;
#31530=EDGE_LOOP ( 'NONE', ( #14567, #8339, #37940, #17452 ) ) ;
#31532=CARTESIAN_POINT ( 'NONE',  ( 4.257397009801616505, -51.06825406007883572, 32.69375250196129912 ) ) ;
#31537=CARTESIAN_POINT ( 'NONE',  ( 0.7573849235549138248, -50.54166666666665009, 27.17302655983835180 ) ) ;
#31543=CARTESIAN_POINT ( 'NONE',  ( 5.912663395429907709, -50.55729166714461797, 26.32672608803957459 ) ) ;
#31546=CARTESIAN_POINT ( 'NONE',  ( 4.257351432995529983, -51.31874920356175096, 25.69375250216227613 ) ) ;
#31548=ORIENTED_EDGE ( 'NONE', *, *, #39777, .F. ) ;
#31549=CARTESIAN_POINT ( 'NONE',  ( 4.257384923554909051, -52.12499999999999289, 25.15230061767466552 ) ) ;
#31555=CARTESIAN_POINT ( 'NONE',  ( 4.257384923554908163, -49.67812500047794799, 33.01645438728532866 ) ) ;
#31560=( BOUNDED_CURVE ( )  B_SPLINE_CURVE ( 2, ( #37562, #8415, #34372, #5230, #30132, #10779, #7591, #20567, #15444 ),
 .UNSPECIFIED., .F., .T. ) 
 B_SPLINE_CURVE_WITH_KNOTS ( ( 3, 2, 2, 2, 3 ),
 ( 0.3624999999999999889, 0.3666666666666666408, 0.3750000000000000000, 0.3833333333333333592, 0.3875000000000000111 ),
 .UNSPECIFIED. ) 
 CURVE ( )  GEOMETRIC_REPRESENTATION_ITEM ( )  RATIONAL_B_SPLINE_CURVE ( ( 0.9330127018922194093, 0.9330127018922194093, 1.000000000000000000, 0.8660254037844387076, 1.000000000000000000, 0.8660254037844387076, 1.000000000000000000, 0.9330127018922194093, 0.9330127018922194093 ) ) 
 REPRESENTATION_ITEM ( '' )  );
#31584=CARTESIAN_POINT ( 'NONE',  ( 7.757384923554902834, -49.79166666666666430, 31.21447844416572792 ) ) ;
#31592=CARTESIAN_POINT ( 'NONE',  ( 0.9468279798049132889, -48.89062500047794657, 29.19375250200204164 ) ) ;
#31602=ORIENTED_EDGE ( 'NONE', *, *, #8321, .T. ) ;
#31605=VERTEX_POINT ( 'NONE', #40968 ) ;
#31606=CARTESIAN_POINT ( 'NONE',  ( 6.007384923554904610, -50.86395833323773985, 32.22484141524757462 ) ) ;
#31611=CARTESIAN_POINT ( 'NONE',  ( 4.257384923554909051, -52.75000000000000000, 29.19375250200204164 ) ) ;
#31613=CARTESIAN_POINT ( 'NONE',  ( 7.757384923554902834, -45.98541666762256597, 31.21447844416572792 ) ) ;
#31629=CARTESIAN_POINT ( 'NONE',  ( 2.975064734268261013, -42.40508397444173738, 32.45039488375558534 ) ) ;
#31660=CARTESIAN_POINT ( 'NONE',  ( 0.9468279798049115126, -42.76145833381128369, 31.10510344464368515 ) ) ;
#31676=CARTESIAN_POINT ( 'NONE',  ( 7.567941867304904591, -52.09687500047795083, 29.19375250200204164 ) ) ;
#31679=CARTESIAN_POINT ( 'NONE',  ( 6.047306821037369495, -45.52612841636603491, 32.20174059608238792 ) ) ;
#31684=CARTESIAN_POINT ( 'NONE',  ( 0.8481207947551614446, -45.71286666659644737, 28.38056543031974144 ) ) ;
#31691=B_SPLINE_CURVE_WITH_KNOTS ( 'NONE', 3,
 ( #11340, #30699, #24327, #37296, #8150, #4955, #15164, #7952, #8568, #37096, #41115, #24127, #17937, #11144, #20918, #5370, #27711, #11962 ),
 .UNSPECIFIED., .F., .F.,
 ( 4, 2, 2, 2, 2, 2, 2, 2, 4 ),
 ( 0.2158354339498903540, 0.2190079507112604462, 0.2221804674726305662, 0.2253529842340006584, 0.2285255009953707783, 0.2316980177567408705, 0.2348705345181109627, 0.2380430512794810827, 0.2412155680408511749 ),
 .UNSPECIFIED. ) ;
#31696=CARTESIAN_POINT ( 'NONE',  ( 4.257384923554909051, -44.01562500047795368, 25.37105061671875461 ) ) ;
#31698=CARTESIAN_POINT ( 'NONE',  ( 0.9468279798049125118, -44.30312500047794799, 29.19375250200204164 ) ) ;
#31706=CARTESIAN_POINT ( 'NONE',  ( 7.757384923554905498, -44.24999999999999289, 29.19375250200204164 ) ) ;
#31707=CARTESIAN_POINT ( 'NONE',  ( 4.257384923554908163, -45.26562500047794657, 33.01645438728532866 ) ) ;
#31713=VERTEX_POINT ( 'NONE', #2672 ) ;
#31714=CARTESIAN_POINT ( 'NONE',  ( 4.257384923554909051, -52.75000000000000000, 29.19375250200204164 ) ) ;
#31738=CARTESIAN_POINT ( 'NONE',  ( 4.257384923554915268, -50.62499999999999289, 25.69375250200204519 ) ) ;
#31740=CARTESIAN_POINT ( 'NONE',  ( 0.7573849235549138248, -50.04166666666666430, 27.17302655983835180 ) ) ;
#31741=ORIENTED_EDGE ( 'NONE', *, *, #30823, .T. ) ;
#31743=CARTESIAN_POINT ( 'NONE',  ( 7.757384923554904610, -52.20833333333332149, 27.17302655983835180 ) ) ;
#31746=CARTESIAN_POINT ( 'NONE',  ( 0.9468279798049143992, -51.43229166714461087, 27.28240155936039812 ) ) ;
#31748=EDGE_CURVE ( 'NONE', #3504, #15341, #16913, .T. ) ;
#31751=CARTESIAN_POINT ( 'NONE',  ( 2.988924387615277567, -51.09848659133997728, 32.45705540233709030 ) ) ;
#31754=CARTESIAN_POINT ( 'NONE',  ( 2.507384923554911715, -42.61395833323773275, 26.16266358875650866 ) ) ;
#31758=CARTESIAN_POINT ( 'NONE',  ( 1.977167814859891903, -43.76104308209522742, 26.49414436081093527 ) ) ;
#31759=CARTESIAN_POINT ( 'NONE',  ( 6.007384923554904610, -43.83333333333332149, 32.22484141524757462 ) ) ;
#31760=CARTESIAN_POINT ( 'NONE',  ( 4.257384923554909051, -48.92812500047794089, 25.37105061671875461 ) ) ;
#31762=CARTESIAN_POINT ( 'NONE',  ( 0.7703132268595052068, -48.68739665648579518, 29.49440967775994338 ) ) ;
#31764=CARTESIAN_POINT ( 'NONE',  ( 0.7573849235549129366, -51.19375000095590167, 29.19375250200204164 ) ) ;
#31766=CARTESIAN_POINT ( 'NONE',  ( 3.319562750045990107, -44.89732909936924443, 32.69375250200203453 ) ) ;
#31792=CARTESIAN_POINT ( 'NONE',  ( 7.567941867304904591, -48.14062500047794657, 29.19375250200204164 ) ) ;
#31793=CARTESIAN_POINT ( 'NONE',  ( 4.630631976088899648, 3.250000000000000444, 35.13541431052434660 ) ) ;
#31804=CARTESIAN_POINT ( 'NONE',  ( 0.7573849235549129366, -50.03062499990439704, 29.19375250200204164 ) ) ;
#31812=DIRECTION ( 'NONE',  ( 0.000000000000000000, 0.000000000000000000, -1.000000000000000000 ) ) ;
#31814=CARTESIAN_POINT ( 'NONE',  ( 6.007384923554907274, -45.86041666762256597, 26.16266358875650866 ) ) ;
#31819=CARTESIAN_POINT ( 'NONE',  ( 0.7624760980444902358, -46.68542997757474211, 29.54201422816098699 ) ) ;
#31835=CARTESIAN_POINT ( 'NONE',  ( 0.7573849235549120484, -51.95833333333331439, 31.21447844416572792 ) ) ;
#31845=DIRECTION ( 'NONE',  ( 0.000000000000000000, 1.000000000000000000, 0.000000000000000000 ) ) ;
#31846=CARTESIAN_POINT ( 'NONE',  ( 2.507384923554909495, -45.41666666666665719, 32.22484141524756751 ) ) ;
#31847=ORIENTED_EDGE ( 'NONE', *, *, #28074, .T. ) ;
#31858=CARTESIAN_POINT ( 'NONE',  ( 2.372320183003732819, -42.40340286041580242, 32.14587784476420040 ) ) ;
#31860=DIRECTION ( 'NONE',  ( -0.000000000000000000, -1.000000000000000000, -0.000000000000000000 ) ) ;
#31867=CARTESIAN_POINT ( 'NONE',  ( 2.602106451679911281, -42.38645833381128369, 26.32672608803957459 ) ) ;
#31902=CARTESIAN_POINT ( 'NONE',  ( 4.566262630962159896, -49.32609532412836018, 25.70686728123175513 ) ) ;
#31905=CARTESIAN_POINT ( 'NONE',  ( 4.257384923554908163, -43.26562500047793947, 33.01645438728532866 ) ) ;
#31906=CARTESIAN_POINT ( 'NONE',  ( 0.9468279798049134000, -45.34479166714460519, 27.28240155936039102 ) ) ;
#31910=ORIENTED_EDGE ( 'NONE', *, *, #25931, .F. ) ;
#31914=CARTESIAN_POINT ( 'NONE',  ( 4.981696770752847669, -47.05394536447444409, 32.63577378521301853 ) ) ;
#31915=CARTESIAN_POINT ( 'NONE',  ( 0.7573849235549120484, -51.15208333428923737, 31.21447844416572792 ) ) ;
#31916=CARTESIAN_POINT ( 'NONE',  ( 5.912663395429904156, -44.72395833381127517, 32.06077891596451224 ) ) ;
#31952=CARTESIAN_POINT ( 'NONE',  ( 7.666291933273527981, -47.42227851001823069, 28.27764512132818453 ) ) ;
#31953=FACE_OUTER_BOUND ( 'NONE', #23084, .T. ) ;
#31954=CARTESIAN_POINT ( 'NONE',  ( 0.7573849235549120484, -50.45833333333332149, 31.21447844416572792 ) ) ;
#31957=CARTESIAN_POINT ( 'NONE',  ( 5.195207097063835988, -52.14732909936925864, 25.69375250200204519 ) ) ;
#31959=CARTESIAN_POINT ( 'NONE',  ( 4.284214406423948240, -43.31933079769611084, 25.69384887586323885 ) ) ;
#31960=CARTESIAN_POINT ( 'NONE',  ( 4.257372105343447011, -50.31874971046479317, 25.69375250202551797 ) ) ;
#31967=EDGE_CURVE ( 'NONE', #3008, #38358, #41639, .T. ) ;
#31968=CARTESIAN_POINT ( 'NONE',  ( 4.257384923554908163, -50.87499999999999289, 33.23520438632941421 ) ) ;
#31970=EDGE_LOOP ( 'NONE', ( #28206, #12625, #28296, #17122 ) ) ;
#31971=CARTESIAN_POINT ( 'NONE',  ( 3.050655012925588938, -43.78966723313836695, 25.89924362069784536 ) ) ;
#31974=CARTESIAN_POINT ( 'NONE',  ( 2.602106451679911281, -47.88645833381128369, 26.32672608803957459 ) ) ;
#31996=CARTESIAN_POINT ( 'NONE',  ( 7.757384923554905498, -46.74999999999999289, 29.19375250200204164 ) ) ;
#32005=CARTESIAN_POINT ( 'NONE',  ( 5.195207097063837764, -49.85267090063073425, 32.69375250200203453 ) ) ;
#32012=CARTESIAN_POINT ( 'NONE',  ( 0.9468279798049124008, -46.84895833381128227, 31.10510344464368515 ) ) ;
#32017=CARTESIAN_POINT ( 'NONE',  ( 0.9468279798049125118, -49.30312500047794799, 29.19375250200204164 ) ) ;
#32024=CARTESIAN_POINT ( 'NONE',  ( 4.257384923554909051, -50.15562499990440415, 25.15230061767466552 ) ) ;
#32030=CARTESIAN_POINT ( 'NONE',  ( 7.757384923554904610, -45.40208333428923737, 27.17302655983835180 ) ) ;
#32057=CARTESIAN_POINT ( 'NONE',  ( 0.9136105642906394708, -48.17044274842007923, 30.23501800516578086 ) ) ;
#32060=CARTESIAN_POINT ( 'NONE',  ( 5.195207097063836876, -49.14732909936924443, 25.69375250200204519 ) ) ;
#32062=CARTESIAN_POINT ( 'NONE',  ( 7.567941867304905479, -45.55312500047794799, 29.19375250200204164 ) ) ;
#32064=CARTESIAN_POINT ( 'NONE',  ( 4.257384923554909051, -52.75000000000000000, 25.69375250200204519 ) ) ;
#32071=CARTESIAN_POINT ( 'NONE',  ( 6.506253628337590911, -47.87284184352929373, 26.46881620347950914 ) ) ;
#32084=CARTESIAN_POINT ( 'NONE',  ( 0.7573849235549129366, -42.19375000095590167, 29.19375250200204164 ) ) ;
#32085=EDGE_CURVE ( 'NONE', #8243, #5298, #35928, .T. ) ;
#32098=EDGE_CURVE ( 'NONE', #13809, #24350, #41340, .T. ) ;
#32109=CARTESIAN_POINT ( 'NONE',  ( 0.9558958105716168774, -45.72067047236829751, 28.02848205438306550 ) ) ;
#32116=ORIENTED_EDGE ( 'NONE', *, *, #41216, .T. ) ;
#32117=CARTESIAN_POINT ( 'NONE',  ( 1.206120912854053540, -42.73365604860700273, 27.41901229945968410 ) ) ;
#32121=CARTESIAN_POINT ( 'NONE',  ( 0.9468279798049143992, -44.43229166714461797, 27.28240155936039812 ) ) ;
#32122=CARTESIAN_POINT ( 'NONE',  ( 7.567941867304902814, -46.09479166714460519, 31.10510344464368870 ) ) ;
#32125=ORIENTED_EDGE ( 'NONE', *, *, #22474, .F. ) ;
#32130=CARTESIAN_POINT ( 'NONE',  ( 0.9468279798049143992, -44.43229166714461797, 27.28240155936039457 ) ) ;
#32135=CARTESIAN_POINT ( 'NONE',  ( 7.567941867304904591, -52.14062500047794657, 29.19375250200204164 ) ) ;
#32138=DIRECTION ( 'NONE',  ( 0.000000000000000000, 1.000000000000000000, 0.000000000000000000 ) ) ;
#32167=CARTESIAN_POINT ( 'NONE',  ( 4.240754906655594070, -47.31837508946153292, 25.69378953248939723 ) ) ;
#32169=CARTESIAN_POINT ( 'NONE',  ( 7.757384923554902834, -49.29166666666665719, 31.21447844416572792 ) ) ;
#32175=CARTESIAN_POINT ( 'NONE',  ( 6.691081713580485868, -43.37909447820656084, 26.67607607971740080 ) ) ;
#32176=EDGE_CURVE ( 'NONE', #27686, #5921, #11080, .T. ) ;
#32177=CARTESIAN_POINT ( 'NONE',  ( 0.9468279798049132889, -50.89062500047794657, 29.19375250200204164 ) ) ;
#32183=CARTESIAN_POINT ( 'NONE',  ( 7.757384923554902834, -49.79166666666666430, 31.21447844416572792 ) ) ;
#32186=EDGE_LOOP ( 'NONE', ( #17390, #29885, #1468, #26435 ) ) ;
#32190=CARTESIAN_POINT ( 'NONE',  ( 5.912663395429905044, -49.13645833381128369, 32.06077891596451224 ) ) ;
#32193=CARTESIAN_POINT ( 'NONE',  ( 3.131825107731939895, -48.79179323582845740, 25.87170854983249768 ) ) ;
#32197=AXIS2_PLACEMENT_3D ( 'NONE', #30239, #40022, #40234 ) ;
#32210=CARTESIAN_POINT ( 'NONE',  ( 4.257384923554909051, -42.62499999999998579, 25.69375250200204519 ) ) ;
#32224=CARTESIAN_POINT ( 'NONE',  ( 2.602106451679912169, -46.97395833381128227, 26.32672608803957459 ) ) ;
#32229=CARTESIAN_POINT ( 'NONE',  ( 0.9468279798049125118, -49.80312500047794799, 29.19375250200204164 ) ) ;
#32231=ADVANCED_FACE ( 'NONE', ( #10262 ), #4302, .T. ) ;
#32232=EDGE_LOOP ( 'NONE', ( #11111, #36512, #29664, #26547 ) ) ;
#32235=CARTESIAN_POINT ( 'NONE',  ( 4.257384923554909051, -48.15562499990439704, 25.15230061767466552 ) ) ;
#32239=ORIENTED_EDGE ( 'NONE', *, *, #37946, .T. ) ;
#32244=CARTESIAN_POINT ( 'NONE',  ( 7.757384923554905498, -44.44375000095590877, 29.19375250200204164 ) ) ;
#32261=CARTESIAN_POINT ( 'NONE',  ( 1.765678960124132058, -51.63301209361243593, 31.69401234789160426 ) ) ;
#32278=CARTESIAN_POINT ( 'NONE',  ( 0.7925677550570877639, -46.18304082929345356, 29.69407040337475934 ) ) ;
#32279=CARTESIAN_POINT ( 'NONE',  ( 4.257384923554909051, -44.92812500047794799, 25.37105061671875461 ) ) ;
#32288=CARTESIAN_POINT ( 'NONE',  ( 7.392940846217376460, -47.98354782368367211, 30.81072105521446858 ) ) ;
#32297=CARTESIAN_POINT ( 'NONE',  ( 1.386599435876713970, -50.74252487936125533, 27.19158134142977801 ) ) ;
#32310=LINE ( 'NONE', #35080, #29520 ) ;
#32318=CARTESIAN_POINT ( 'NONE',  ( 4.257440696971988459, -46.81875132889357616, 25.69375250244642572 ) ) ;
#32333=CARTESIAN_POINT ( 'NONE',  ( 3.044482980332702038, -42.29615616597443051, 32.27411873898412153 ) ) ;
#32334=CARTESIAN_POINT ( 'NONE',  ( 5.912663395429907709, -44.96979166714461940, 26.32672608803957459 ) ) ;
#32340=CARTESIAN_POINT ( 'NONE',  ( 3.884137871020911792, 3.250000000000000444, 23.25209069347974022 ) ) ;
#32341=CARTESIAN_POINT ( 'NONE',  ( 7.567941867304904591, -45.14062500047794657, 29.19375250200204164 ) ) ;
#32343=EDGE_CURVE ( 'NONE', #16189, #34951, #6649, .T. ) ;
#32373=CARTESIAN_POINT ( 'NONE',  ( 7.567941867304905479, -50.05312500047794799, 29.19375250200204164 ) ) ;
#32374=CARTESIAN_POINT ( 'NONE',  ( 6.408295570290712284, -47.51587488792748815, 31.99258853213691367 ) ) ;
#32376=CYLINDRICAL_SURFACE ( 'NONE', #32823, 3.499999999999996003 ) ;
#32377=CARTESIAN_POINT ( 'NONE',  ( 7.757384923554902834, -50.29166666666665719, 31.21447844416572792 ) ) ;
#32383=CARTESIAN_POINT ( 'NONE',  ( 4.304386015085131412, -43.31976768839259506, 25.69402288447800231 ) ) ;
#32384=CARTESIAN_POINT ( 'NONE',  ( 4.257384923554909051, -51.01562500047795368, 25.37105061671875461 ) ) ;
#32387=CARTESIAN_POINT ( 'NONE',  ( 1.494419065784665435, -51.24557276935230021, 26.99862735487317522 ) ) ;
#32390=CARTESIAN_POINT ( 'NONE',  ( 7.757384923554902834, -49.29166666666665719, 31.21447844416572792 ) ) ;
#32429=CARTESIAN_POINT ( 'NONE',  ( 7.567941867304902814, -48.18229166714461087, 31.10510344464368870 ) ) ;
#32433=( BOUNDED_CURVE ( )  B_SPLINE_CURVE ( 2, ( #14644, #33139, #23798, #7414, #36762, #40161, #17824, #27404, #14429 ),
 .UNSPECIFIED., .F., .F. ) 
 B_SPLINE_CURVE_WITH_KNOTS ( ( 3, 2, 2, 2, 3 ),
 ( 0.8125000000000000000, 0.8166666666666666519, 0.8249999999999999556, 0.8333333333333333703, 0.8375000000000000222 ),
 .UNSPECIFIED. ) 
 CURVE ( )  GEOMETRIC_REPRESENTATION_ITEM ( )  RATIONAL_B_SPLINE_CURVE ( ( 0.9330127018922194093, 0.9330127018922194093, 1.000000000000000000, 0.8660254037844387076, 1.000000000000000000, 0.8660254037844387076, 1.000000000000000000, 0.9330127018922194093, 0.9330127018922194093 ) ) 
 REPRESENTATION_ITEM ( '' )  );
#32434=CARTESIAN_POINT ( 'NONE',  ( 7.567941867304905479, -49.55312500047794799, 29.19375250200204164 ) ) ;
#32440=ORIENTED_EDGE ( 'NONE', *, *, #38523, .F. ) ;
#32441=CARTESIAN_POINT ( 'NONE',  ( 6.007384923554907274, -48.19729166657106845, 26.16266358875650866 ) ) ;
#32447=CARTESIAN_POINT ( 'NONE',  ( 2.507384923554909495, -45.11041666762257307, 32.22484141524756751 ) ) ;
#32450=CARTESIAN_POINT ( 'NONE',  ( 0.7573849235549129366, -42.99999999999999289, 29.19375250200204164 ) ) ;
#32482=CARTESIAN_POINT ( 'NONE',  ( 4.257384923554908163, -45.67812500047795510, 33.01645438728532866 ) ) ;
#32485=CARTESIAN_POINT ( 'NONE',  ( 7.757384923554904610, -48.70833333333332860, 27.17302655983835180 ) ) ;
#32489=CARTESIAN_POINT ( 'NONE',  ( 6.372282230720123231, -51.87158340019668401, 26.35449158890256172 ) ) ;
#32491=CARTESIAN_POINT ( 'NONE',  ( 7.295370301032107818, -47.90241897267697624, 27.45470661398015721 ) ) ;
#32496=CARTESIAN_POINT ( 'NONE',  ( 2.975067305262454553, -42.09928137282000904, 32.45038596706375955 ) ) ;
#32498=ORIENTED_EDGE ( 'NONE', *, *, #37827, .T. ) ;
#32500=CARTESIAN_POINT ( 'NONE',  ( 4.196626944815459836, -50.81741602284468939, 25.69420483695395063 ) ) ;
#32521=CARTESIAN_POINT ( 'NONE',  ( 6.105373279903271388, -45.36179365262180596, 26.18250205547671428 ) ) ;
#32531=ORIENTED_EDGE ( 'NONE', *, *, #10282, .F. ) ;
#32532=CARTESIAN_POINT ( 'NONE',  ( 0.7980480038115749242, -42.68002150036057429, 29.84937254714089505 ) ) ;
#32535=CARTESIAN_POINT ( 'NONE',  ( 2.602106451679909505, -42.71979166714461940, 32.06077891596451224 ) ) ;
#32541=CARTESIAN_POINT ( 'NONE',  ( 7.148858676424105774, -46.99362368181897409, 31.19091422836696736 ) ) ;
#32542=CARTESIAN_POINT ( 'NONE',  ( 5.912663395429907709, -46.55729166714461087, 26.32672608803957459 ) ) ;
#32545=CARTESIAN_POINT ( 'NONE',  ( 7.757384923554905498, -52.24999999999999289, 29.19375250200204164 ) ) ;
#32547=ORIENTED_EDGE ( 'NONE', *, *, #40981, .T. ) ;
#32571=CARTESIAN_POINT ( 'NONE',  ( 2.274660987513316801, -47.27171007459156016, 26.26399451953406938 ) ) ;
#32574=CARTESIAN_POINT ( 'NONE',  ( 0.7573849235549120484, -47.45833333333332149, 31.21447844416572792 ) ) ;
#32583=CARTESIAN_POINT ( 'NONE',  ( 4.257384923554909051, -48.51562500047794657, 25.37105061671875461 ) ) ;
#32589=CARTESIAN_POINT ( 'NONE',  ( 6.007384923554904610, -51.33333333333332149, 32.22484141524757462 ) ) ;
#32591=VERTEX_POINT ( 'NONE', #39947 ) ;
#32593=CARTESIAN_POINT ( 'NONE',  ( 3.511128953535865627, -43.58702483971842412, 32.62938241260086158 ) ) ;
#32597=CARTESIAN_POINT ( 'NONE',  ( 2.102699810575468842, -48.76514646618790039, 26.39683416679749683 ) ) ;
#32601=CARTESIAN_POINT ( 'NONE',  ( 4.257384923554908163, -51.56875000095590877, 33.23520438632941421 ) ) ;
#32604=EDGE_CURVE ( 'NONE', #9278, #38450, #32433, .T. ) ;
#32615=CARTESIAN_POINT ( 'NONE',  ( 5.195207097063836876, -46.64732909936926575, 25.69375250200204519 ) ) ;
#32617=CARTESIAN_POINT ( 'NONE',  ( 4.257384923554908163, -43.06875000095590167, 33.23520438632941421 ) ) ;
#32622=DIRECTION ( 'NONE',  ( 0.000000000000000000, 0.000000000000000000, 1.000000000000000000 ) ) ;
#32631=CARTESIAN_POINT ( 'NONE',  ( 7.567941867304904591, -45.14062500047794657, 29.19375250200204164 ) ) ;
#32635=CARTESIAN_POINT ( 'NONE',  ( 0.9468279798049117346, -51.26145833381129080, 31.10510344464368515 ) ) ;
#32638=VECTOR ( 'NONE', #32802, 1000.000000000000000 ) ;
#32639=EDGE_LOOP ( 'NONE', ( #8158, #40692, #21389, #22867 ) ) ;
#32642=CARTESIAN_POINT ( 'NONE',  ( 6.007384923554907274, -48.69729166657106845, 26.16266358875650866 ) ) ;
#32648=CARTESIAN_POINT ( 'NONE',  ( 0.7573849235549138248, -44.23541666762257307, 27.17302655983835180 ) ) ;
#32649=DIRECTION ( 'NONE',  ( -0.000000000000000000, -1.000000000000000000, -0.000000000000000000 ) ) ;
#32654=AXIS2_PLACEMENT_3D ( 'NONE', #38606, #18207, #31384 ) ;
#32659=CYLINDRICAL_SURFACE ( 'NONE', #20446, 3.499999999999996003 ) ;
#32674=( BOUNDED_CURVE ( )  B_SPLINE_CURVE ( 2, ( #9210, #22184, #18575, #12183, #6016, #38766, #41334, #21553, #19202 ),
 .UNSPECIFIED., .F., .T. ) 
 B_SPLINE_CURVE_WITH_KNOTS ( ( 3, 2, 2, 2, 3 ),
 ( 0.08749999999999999445, 0.09166666666666666019, 0.1000000000000000056, 0.1083333333333333370, 0.1125000000000000028 ),
 .UNSPECIFIED. ) 
 CURVE ( )  GEOMETRIC_REPRESENTATION_ITEM ( )  RATIONAL_B_SPLINE_CURVE ( ( 0.9330127018922194093, 0.9330127018922194093, 1.000000000000000000, 0.8660254037844387076, 1.000000000000000000, 0.8660254037844387076, 1.000000000000000000, 0.9330127018922194093, 0.9330127018922194093 ) ) 
 REPRESENTATION_ITEM ( '' )  );
#32687=CARTESIAN_POINT ( 'NONE',  ( 2.602106451679909505, -45.21979166714461940, 32.06077891596451224 ) ) ;
#32706=CARTESIAN_POINT ( 'NONE',  ( 4.257384923554908163, -43.37499999999999289, 33.23520438632941421 ) ) ;
#32719=LINE ( 'NONE', #23376, #24146 ) ;
#32741=CARTESIAN_POINT ( 'NONE',  ( 5.912663395429905044, -43.13645833381128369, 32.06077891596451224 ) ) ;
#32752=ORIENTED_EDGE ( 'NONE', *, *, #27200, .T. ) ;
#32769=CARTESIAN_POINT ( 'NONE',  ( 3.884137871020911792, 3.250000000000000444, 23.25209069347974022 ) ) ;
#32776=CARTESIAN_POINT ( 'NONE',  ( 6.007384923554907274, -44.16666666666665719, 26.16266358875650866 ) ) ;
#32781=CARTESIAN_POINT ( 'NONE',  ( 7.757384923554905498, -47.24999999999999289, 29.19375250200204164 ) ) ;
#32787=CARTESIAN_POINT ( 'NONE',  ( 7.702211816419376689, -43.46356349646075756, 30.00351623572547766 ) ) ;
#32788=CARTESIAN_POINT ( 'NONE',  ( 0.9468279798049132889, -48.89062500047794657, 29.19375250200204164 ) ) ;
#32794=CARTESIAN_POINT ( 'NONE',  ( 7.757384923554905498, -49.24999999999998579, 29.19375250200204164 ) ) ;
#32802=DIRECTION ( 'NONE',  ( -0.000000000000000000, 1.000000000000000000, -0.000000000000000000 ) ) ;
#32807=CARTESIAN_POINT ( 'NONE',  ( 7.757384923554904610, -48.90208333428923737, 27.17302655983835180 ) ) ;
#32821=CARTESIAN_POINT ( 'NONE',  ( 0.7579436417219144184, -44.70543366251542494, 28.71274750898724193 ) ) ;
#32823=AXIS2_PLACEMENT_3D ( 'NONE', #28755, #12607, #38549 ) ;
#32836=CARTESIAN_POINT ( 'NONE',  ( 0.9468279798049132889, -44.39062500047794657, 29.19375250200204164 ) ) ;
#32841=CARTESIAN_POINT ( 'NONE',  ( 0.9468279798049134000, -51.34479166714461940, 27.28240155936039102 ) ) ;
#32848=VERTEX_POINT ( 'NONE', #24846 ) ;
#32849=CARTESIAN_POINT ( 'NONE',  ( 4.257384923554909051, -47.15562499990440415, 25.15230061767466552 ) ) ;
#32854=( BOUNDED_CURVE ( )  B_SPLINE_CURVE ( 2, ( #14856, #27418, #21028, #4451, #11248, #24230, #11649, #34004, #24645 ),
 .UNSPECIFIED., .F., .F. ) 
 B_SPLINE_CURVE_WITH_KNOTS ( ( 3, 2, 2, 2, 3 ),
 ( 0.3125000000000000000, 0.3166666666666666519, 0.3250000000000000111, 0.3333333333333333148, 0.3375000000000000222 ),
 .UNSPECIFIED. ) 
 CURVE ( )  GEOMETRIC_REPRESENTATION_ITEM ( )  RATIONAL_B_SPLINE_CURVE ( ( 0.9330127018922194093, 0.9330127018922194093, 1.000000000000000000, 0.8660254037844387076, 1.000000000000000000, 0.8660254037844387076, 1.000000000000000000, 0.9330127018922189652, 0.9330127018922194093 ) ) 
 REPRESENTATION_ITEM ( '' )  );
#32856=CARTESIAN_POINT ( 'NONE',  ( 0.7573849235549138248, -44.23541666762257307, 27.17302655983835180 ) ) ;
#32857=CARTESIAN_POINT ( 'NONE',  ( 4.257384923554909051, -44.31875000095590167, 25.15230061767466552 ) ) ;
#32859=CARTESIAN_POINT ( 'NONE',  ( 4.257384923554909051, -52.75000000000000000, 29.19375250200204164 ) ) ;
#32863=DIRECTION ( 'NONE',  ( 0.000000000000000000, 0.000000000000000000, -1.000000000000000000 ) ) ;
#32874=LINE ( 'NONE', #16723, #277 ) ;
#32886=DIRECTION ( 'NONE',  ( 0.000000000000000000, 0.000000000000000000, -1.000000000000000000 ) ) ;
#32897=CARTESIAN_POINT ( 'NONE',  ( 0.9468279798049115126, -44.26145833381128369, 31.10510344464368515 ) ) ;
#32900=CARTESIAN_POINT ( 'NONE',  ( 7.646970427069875065, -43.96908339966790891, 30.24268751510847864 ) ) ;
#32907=CARTESIAN_POINT ( 'NONE',  ( 0.7864210216417277799, -42.40301867742068254, 28.66401044670079656 ) ) ;
#32909=ORIENTED_EDGE ( 'NONE', *, *, #18690, .T. ) ;
#32911=CARTESIAN_POINT ( 'NONE',  ( 4.257450628761716871, -44.31875150865747770, 25.69375250261877852 ) ) ;
#32916=CARTESIAN_POINT ( 'NONE',  ( 1.886331150558369973, -50.62704302584038629, 31.82335533226972402 ) ) ;
#32917=CARTESIAN_POINT ( 'NONE',  ( 7.757384923554905498, -42.74999999999999289, 29.19375250200204164 ) ) ;
#32935=CARTESIAN_POINT ( 'NONE',  ( 0.7573849235549138248, -52.04166666666666430, 27.17302655983835180 ) ) ;
#32943=LINE ( 'NONE', #3809, #2236 ) ;
#32965=CARTESIAN_POINT ( 'NONE',  ( 0.9468279798049115126, -48.76145833381128369, 31.10510344464368515 ) ) ;
#32981=DIRECTION ( 'NONE',  ( -0.000000000000000000, 1.000000000000000000, -0.000000000000000000 ) ) ;
#32996=CARTESIAN_POINT ( 'NONE',  ( 5.912663395429907709, -51.46979166714461940, 26.32672608803957459 ) ) ;
#33000=CARTESIAN_POINT ( 'NONE',  ( 6.007384923554904610, -48.33333333333332860, 32.22484141524757462 ) ) ;
#33007=CARTESIAN_POINT ( 'NONE',  ( 2.602106451679912169, -48.47395833381128227, 26.32672608803957459 ) ) ;
#33013=CARTESIAN_POINT ( 'NONE',  ( 0.7573849235549120484, -46.95833333333332860, 31.21447844416572792 ) ) ;
#33014=CARTESIAN_POINT ( 'NONE',  ( 7.567941867304904591, -50.64062500047794657, 29.19375250200204164 ) ) ;
#33017=CARTESIAN_POINT ( 'NONE',  ( 1.380291233058039468, -43.24462811607192947, 27.13824365383018034 ) ) ;
#33019=AXIS2_PLACEMENT_3D ( 'NONE', #41197, #9065, #31812 ) ;
#33024=CARTESIAN_POINT ( 'NONE',  ( 7.757384923554902834, -49.98541666762256597, 31.21447844416572792 ) ) ;
#33025=DIRECTION ( 'NONE',  ( -0.000000000000000000, -1.000000000000000000, -0.000000000000000000 ) ) ;
#33039=CARTESIAN_POINT ( 'NONE',  ( 2.507384923554911715, -42.27708333428924448, 26.16266358875650866 ) ) ;
#33051=CARTESIAN_POINT ( 'NONE',  ( 4.257384923554909051, -45.01562500047794657, 25.37105061671875461 ) ) ;
#33055=CARTESIAN_POINT ( 'NONE',  ( 2.602106451679909505, -46.71979166714461229, 32.06077891596451224 ) ) ;
#33061=CARTESIAN_POINT ( 'NONE',  ( 6.007384923554904610, -48.86395833323773275, 32.22484141524757462 ) ) ;
#33067=CARTESIAN_POINT ( 'NONE',  ( 2.507384923554911715, -43.27708333428924448, 26.16266358875650866 ) ) ;
#33068=CARTESIAN_POINT ( 'NONE',  ( 0.7573849235549129366, -44.69375000095590877, 29.19375250200204164 ) ) ;
#33106=CARTESIAN_POINT ( 'NONE',  ( 7.567941867304904591, -42.59479166714461940, 31.10510344464368870 ) ) ;
#33109=CARTESIAN_POINT ( 'NONE',  ( 6.682523805623921120, -44.00951815195804073, 31.73597709666643141 ) ) ;
#33112=CARTESIAN_POINT ( 'NONE',  ( 7.757384923554905498, -51.94375000095590877, 29.19375250200204164 ) ) ;
#33116=CARTESIAN_POINT ( 'NONE',  ( 6.376635500632452214, -48.36847624911926147, 26.37210924251540334 ) ) ;
#33121=CARTESIAN_POINT ( 'NONE',  ( 4.249644215247149859, -44.31856560387248578, 25.69375882900124353 ) ) ;
#33124=ORIENTED_EDGE ( 'NONE', *, *, #38902, .T. ) ;
#33125=CARTESIAN_POINT ( 'NONE',  ( 1.188754915763054365, -50.73385423774777081, 27.50134581855857974 ) ) ;
#33126=CARTESIAN_POINT ( 'NONE',  ( 2.507384923554911715, -43.58333333333332149, 26.16266358875650866 ) ) ;
#33139=CARTESIAN_POINT ( 'NONE',  ( 3.319562750045980337, -44.10267090063073425, 25.69375250200204519 ) ) ;
#33147=CARTESIAN_POINT ( 'NONE',  ( 3.319562750045992328, -44.60267090063072004, 25.69375250200203453 ) ) ;
#33153=CARTESIAN_POINT ( 'NONE',  ( 7.741328013343518499, -42.40485061181025372, 29.88190759173290445 ) ) ;
#33173=CARTESIAN_POINT ( 'NONE',  ( 7.567941867304905479, -45.51145833381128369, 27.28240155936039812 ) ) ;
#33177=CARTESIAN_POINT ( 'NONE',  ( 7.768069135323538710, -45.94960511981035012, 29.55150996576983502 ) ) ;
#33181=EDGE_CURVE ( 'NONE', #9899, #18063, #25241, .T. ) ;
#33197=CARTESIAN_POINT ( 'NONE',  ( 2.507384923554911715, -47.58333333333332149, 26.16266358875650866 ) ) ;
#33208=CARTESIAN_POINT ( 'NONE',  ( 2.507384923554909495, -48.41666666666665719, 32.22484141524756751 ) ) ;
#33209=VECTOR ( 'NONE', #19614, 1000.000000000000000 ) ;
#33211=CARTESIAN_POINT ( 'NONE',  ( 7.520758616830159227, -49.41500114339262240, 27.92840989375582694 ) ) ;
#33215=CARTESIAN_POINT ( 'NONE',  ( 0.9468279798049124008, -49.34895833381128938, 31.10510344464368515 ) ) ;
#33223=EDGE_CURVE ( 'NONE', #15067, #34704, #36797, .T. ) ;
#33224=CARTESIAN_POINT ( 'NONE',  ( 0.7573849235549120484, -47.45833333333332149, 31.21447844416572792 ) ) ;
#33225=CARTESIAN_POINT ( 'NONE',  ( 4.257384923554908163, -50.26562500047794657, 33.01645438728532866 ) ) ;
#33229=CARTESIAN_POINT ( 'NONE',  ( 3.319562750045992328, -43.60267090063072715, 25.69375250200203453 ) ) ;
#33235=CARTESIAN_POINT ( 'NONE',  ( 7.757384923554902834, -49.48541666762258018, 31.21447844416572792 ) ) ;
#33248=CARTESIAN_POINT ( 'NONE',  ( 3.481433358349435903, -44.58792978037810428, 32.63022876192368216 ) ) ;
#33261=CARTESIAN_POINT ( 'NONE',  ( 7.567941867304904591, -44.64062500047794657, 29.19375250200204164 ) ) ;
#33267=CARTESIAN_POINT ( 'NONE',  ( 2.602106451679911281, -46.38645833381128369, 26.32672608803957459 ) ) ;
#33270=VECTOR ( 'NONE', #13768, 1000.000000000000000 ) ;
#33274=CARTESIAN_POINT ( 'NONE',  ( 2.507384923554909495, -44.44729166657106845, 32.22484141524756751 ) ) ;
#33280=CARTESIAN_POINT ( 'NONE',  ( 0.7573849235549120484, -43.15208333428923737, 31.21447844416572792 ) ) ;
#33295=CARTESIAN_POINT ( 'NONE',  ( 7.308687758396453127, -51.48365426750596896, 30.96842329551577322 ) ) ;
#33296=CONICAL_SURFACE ( 'NONE', #31259, 5.000000000000004441, 0.7853981633974447263 ) ;
#33308=CARTESIAN_POINT ( 'NONE',  ( 7.718484326199413381, -50.92797427890979378, 28.44730271930353638 ) ) ;
#33319=CARTESIAN_POINT ( 'NONE',  ( 7.567941867304904591, -44.09479166714461940, 31.10510344464368870 ) ) ;
#33321=CARTESIAN_POINT ( 'NONE',  ( 7.254949279491025749, -43.98887283137035098, 31.02391549170027218 ) ) ;
#33326=CARTESIAN_POINT ( 'NONE',  ( 4.739762682521476478, -47.82930547655452358, 25.69375250483230388 ) ) ;
#33327=CARTESIAN_POINT ( 'NONE',  ( 5.696835491221758474, -42.40548779855203065, 26.00058663007760629 ) ) ;
#33331=CARTESIAN_POINT ( 'NONE',  ( 4.030611185511456362, -44.31336593506429722, 25.70000143559817474 ) ) ;
#33332=FACE_OUTER_BOUND ( 'NONE', #10408, .T. ) ;
#33340=CARTESIAN_POINT ( 'NONE',  ( 0.7573849235549129366, -42.49999999999998579, 29.19375250200204164 ) ) ;
#33341=CARTESIAN_POINT ( 'NONE',  ( 7.567941867304904591, -43.64062500047794657, 29.19375250200204164 ) ) ;
#33362=AXIS2_PLACEMENT_3D ( 'NONE', #30458, #33860, #34069 ) ;
#33374=B_SPLINE_CURVE_WITH_KNOTS ( 'NONE', 3,
 ( #36225, #7310, #23910, #23258, #39850, #26668, #501, #3691, #13900, #39628, #36878, #27091, #40272, #14327, #36447, #10711, #20282, #32821, #17096, #10926, #23697, #39412, #7739, #24123, #16679, #33248, #7098, #23484 ),
 .UNSPECIFIED., .F., .F.,
 ( 4, 2, 1, 1, 1, 1, 2, 2, 2, 2, 2, 2, 2, 2, 2, 4 ),
 ( 0.7236819825814452267, 0.7236989986770716587, 0.7237160147726980908, 0.7237500469639509548, 0.7238181113464566829, 0.7239542401114681391, 0.7242264976414910516, 0.7247710127015368764, 0.7258600428216285261, 0.7280381030618118254, 0.7302161633019952358, 0.7323942235421785352, 0.7345722837823618345, 0.7367503440225451339, 0.7389284042627284332, 0.7411064645029117326 ),
 .UNSPECIFIED. ) ;
#33383=CARTESIAN_POINT ( 'NONE',  ( 2.602106451679909505, -42.21979166714461940, 32.06077891596451224 ) ) ;
#33387=ORIENTED_EDGE ( 'NONE', *, *, #20926, .T. ) ;
#33389=CARTESIAN_POINT ( 'NONE',  ( 0.9468279798049134000, -46.84479166714461940, 27.28240155936039457 ) ) ;
#33401=EDGE_CURVE ( 'NONE', #25326, #24091, #7993, .T. ) ;
#33407=CYLINDRICAL_SURFACE ( 'NONE', #22760, 3.499999999999996003 ) ;
#33423=CARTESIAN_POINT ( 'NONE',  ( 0.9468279798049125118, -47.30312500047795510, 29.19375250200204164 ) ) ;
#33427=CARTESIAN_POINT ( 'NONE',  ( 6.007384923554907274, -46.16666666666666430, 26.16266358875650866 ) ) ;
#33433=CARTESIAN_POINT ( 'NONE',  ( 7.567941867304902814, -48.68229166714461087, 31.10510344464368870 ) ) ;
#33443=CARTESIAN_POINT ( 'NONE',  ( 4.257384923554908163, -48.87499999999999289, 33.23520438632941421 ) ) ;
#33444=CARTESIAN_POINT ( 'NONE',  ( 0.9468279798049143992, -51.93229166714461797, 27.28240155936039457 ) ) ;
#33454=CARTESIAN_POINT ( 'NONE',  ( 4.257384923554908163, -49.06875000095590167, 33.23520438632941421 ) ) ;
#33481=CARTESIAN_POINT ( 'NONE',  ( 4.257384923554908163, -45.26562500047794657, 33.01645438728532866 ) ) ;
#33494=CARTESIAN_POINT ( 'NONE',  ( 0.7573849235549138248, -46.57229166657106134, 27.17302655983835180 ) ) ;
#33499=CARTESIAN_POINT ( 'NONE',  ( 7.757384923554904610, -50.70833333333332860, 27.17302655983835180 ) ) ;
#33500=CARTESIAN_POINT ( 'NONE',  ( 4.257384923554909051, -42.81875000095590167, 25.15230061767466552 ) ) ;
#33524=DIRECTION ( 'NONE',  ( -0.000000000000000000, -1.000000000000000000, -0.000000000000000000 ) ) ;
#33530=CARTESIAN_POINT ( 'NONE',  ( 2.507384923554911715, -49.58333333333332860, 26.16266358875650866 ) ) ;
#33541=CARTESIAN_POINT ( 'NONE',  ( 4.257384923554909051, -42.92812500047794799, 25.37105061671875461 ) ) ;
#33550=CARTESIAN_POINT ( 'NONE',  ( 4.901091380491914506, -42.40552430322542676, 25.74167270518923090 ) ) ;
#33556=CARTESIAN_POINT ( 'NONE',  ( 3.798484211909033625, -50.07776677093000472, 32.69375257899697829 ) ) ;
#33562=CARTESIAN_POINT ( 'NONE',  ( 2.507384923554909495, -48.11041666762257307, 32.22484141524756751 ) ) ;
#33563=CARTESIAN_POINT ( 'NONE',  ( 4.257384923554909051, -43.51562500047794657, 25.37105061671875106 ) ) ;
#33566=ADVANCED_BREP_SHAPE_REPRESENTATION ( '', ( #9789, #40442 ), #20062 ) ;
#33573=EDGE_CURVE ( 'NONE', #30506, #42017, #30623, .T. ) ;
#33585=CARTESIAN_POINT ( 'NONE',  ( 6.429743964611982499, -42.87153940944079977, 26.40295371858088203 ) ) ;
#33590=CARTESIAN_POINT ( 'NONE',  ( 2.117285105995408312, -47.76771817149271016, 26.38652452850220342 ) ) ;
#33607=EDGE_LOOP ( 'NONE', ( #22855, #22171 ) ) ;
#33613=CARTESIAN_POINT ( 'NONE',  ( 4.257384923554909051, -44.92812500047794799, 25.37105061671875461 ) ) ;
#33632=LINE ( 'NONE', #30428, #25245 ) ;
#33647=CARTESIAN_POINT ( 'NONE',  ( 2.602106451679909505, -49.71979166714461940, 32.06077891596451224 ) ) ;
#33651=CARTESIAN_POINT ( 'NONE',  ( 6.007384923554907274, -45.66666666666666430, 26.16266358875650866 ) ) ;
#33655=CARTESIAN_POINT ( 'NONE',  ( 1.905276626636873250, -49.25914492844805892, 26.57022745839099187 ) ) ;
#33658=CARTESIAN_POINT ( 'NONE',  ( 0.9468279798049132889, -46.89062500047794657, 29.19375250200204164 ) ) ;
#33663=EDGE_CURVE ( 'NONE', #2260, #14568, #6264, .T. ) ;
#33665=CARTESIAN_POINT ( 'NONE',  ( 7.757384923554904610, -46.70833333333332149, 27.17302655983835180 ) ) ;
#33666=CARTESIAN_POINT ( 'NONE',  ( 4.257384923554909051, -49.51562500047794657, 25.37105061671875106 ) ) ;
#33668=CARTESIAN_POINT ( 'NONE',  ( 4.257384923554909051, -51.62499999999998579, 25.69375250200204519 ) ) ;
#33669=CARTESIAN_POINT ( 'NONE',  ( 1.289309761921198394, -43.14893514176918643, 31.05506935064319407 ) ) ;
#33675=CARTESIAN_POINT ( 'NONE',  ( 0.7573849235549120484, -49.15208333428923737, 31.21447844416572792 ) ) ;
#33686=CARTESIAN_POINT ( 'NONE',  ( 7.757383744053147900, -44.95343329788197195, 29.65190966090601066 ) ) ;
#33713=CARTESIAN_POINT ( 'NONE',  ( 0.7573849235549120484, -44.98895833323773275, 31.21447844416572792 ) ) ;
#33719=CARTESIAN_POINT ( 'NONE',  ( 4.257384923554908163, -42.56875000095590877, 33.23520438632941421 ) ) ;
#33721=EDGE_CURVE ( 'NONE', #35642, #15555, #6476, .T. ) ;
#33733=EDGE_CURVE ( 'NONE', #15360, #16017, #3171, .T. ) ;
#33735=EDGE_CURVE ( 'NONE', #34895, #30878, #28994, .T. ) ;
#33751=ORIENTED_EDGE ( 'NONE', *, *, #21921, .T. ) ;
#33754=CARTESIAN_POINT ( 'NONE',  ( 0.9468279798049143992, -51.43229166714461087, 27.28240155936039812 ) ) ;
#33762=CARTESIAN_POINT ( 'NONE',  ( 7.283176337120700339, -48.39867698522031958, 27.37785602537703866 ) ) ;
#33767=CARTESIAN_POINT ( 'NONE',  ( 0.9943990741236247155, -50.16481584641859826, 30.46038702800344211 ) ) ;
#33773=CARTESIAN_POINT ( 'NONE',  ( 4.257384923554909051, -49.81875000095590167, 25.15230061767466552 ) ) ;
#33811=CYLINDRICAL_SURFACE ( 'NONE', #11499, 3.499999999999996003 ) ;
#33813=EDGE_CURVE ( 'NONE', #20633, #8243, #33374, .T. ) ;
#33819=CARTESIAN_POINT ( 'NONE',  ( 2.602106451679909505, -47.21979166714461229, 32.06077891596451224 ) ) ;
#33846=CARTESIAN_POINT ( 'NONE',  ( 2.602106451679911281, -47.88645833381128369, 26.32672608803957459 ) ) ;
#33850=CARTESIAN_POINT ( 'NONE',  ( 4.257384923554908163, -43.87499999999999289, 33.23520438632941421 ) ) ;
#33853=CARTESIAN_POINT ( 'NONE',  ( 2.825841481552758161, -49.28433521735315992, 25.98023396579986155 ) ) ;
#33856=CARTESIAN_POINT ( 'NONE',  ( 7.567941867304902814, -45.68229166714462508, 31.10510344464368870 ) ) ;
#33860=DIRECTION ( 'NONE',  ( -0.000000000000000000, -1.000000000000000000, -0.000000000000000000 ) ) ;
#33864=CARTESIAN_POINT ( 'NONE',  ( 0.7573849235549120484, -47.95833333333332149, 31.21447844416572792 ) ) ;
#33865=CARTESIAN_POINT ( 'NONE',  ( 7.567941867304904591, -51.64062500047794657, 29.19375250200204164 ) ) ;
#33868=CARTESIAN_POINT ( 'NONE',  ( 0.7448355260715008308, -43.18374443052685052, 29.66230108841206459 ) ) ;
#33875=CARTESIAN_POINT ( 'NONE',  ( 6.007384923554907274, -45.86041666762256597, 26.16266358875650866 ) ) ;
#33885=CARTESIAN_POINT ( 'NONE',  ( 7.315634222575569723, -44.98463209841393962, 30.95642403997497993 ) ) ;
#33903=CARTESIAN_POINT ( 'NONE',  ( 0.9468279798049143992, -42.93229166714461797, 27.28240155936039812 ) ) ;
#33910=CARTESIAN_POINT ( 'NONE',  ( 6.007384923554907274, -44.69729166657106845, 26.16266358875650866 ) ) ;
#33914=EDGE_LOOP ( 'NONE', ( #37833, #32531, #24807, #4726 ) ) ;
#33919=CARTESIAN_POINT ( 'NONE',  ( 2.507384923554909495, -42.61041666762257307, 32.22484141524756751 ) ) ;
#33935=CARTESIAN_POINT ( 'NONE',  ( 7.716727510017761027, -51.45747821635845298, 29.84935540268410747 ) ) ;
#33955=CARTESIAN_POINT ( 'NONE',  ( 7.567941867304904591, -51.64062500047794657, 29.19375250200204164 ) ) ;
#33975=CARTESIAN_POINT ( 'NONE',  ( 4.257384923554909051, -50.31875000095590877, 25.15230061767466552 ) ) ;
#33976=CARTESIAN_POINT ( 'NONE',  ( 2.815360438258434961, -42.30192363818449763, 32.18390116252139421 ) ) ;
#33982=SHAPE_REPRESENTATION ( '7 mm Screw', ( #40442 ), #20062 ) ;
#33998=CARTESIAN_POINT ( 'NONE',  ( 4.257403850124284794, -43.06798715535520472, 32.69375250190384463 ) ) ;
#34004=CARTESIAN_POINT ( 'NONE',  ( 3.319562750045984334, -48.89732909936925154, 32.69375250200203453 ) ) ;
#34006=EDGE_LOOP ( 'NONE', ( #23844, #32547 ) ) ;
#34008=CARTESIAN_POINT ( 'NONE',  ( 4.257384923554909051, -42.40485061181025372, 32.69375250200203453 ) ) ;
#34012=CARTESIAN_POINT ( 'NONE',  ( 6.653511442190654712, -49.00956846899784836, 31.74587780870622566 ) ) ;
#34023=ORIENTED_EDGE ( 'NONE', *, *, #24934, .F. ) ;
#34027=CARTESIAN_POINT ( 'NONE',  ( 5.912663395429905044, -45.13645833381128369, 32.06077891596451224 ) ) ;
#34054=CARTESIAN_POINT ( 'NONE',  ( 0.9468279798049115126, -48.26145833381129080, 31.10510344464368515 ) ) ;
#34059=CARTESIAN_POINT ( 'NONE',  ( 6.007384923554904610, -45.83333333333332149, 32.22484141524757462 ) ) ;
#34063=ORIENTED_EDGE ( 'NONE', *, *, #10621, .T. ) ;
#34064=CARTESIAN_POINT ( 'NONE',  ( 4.257384923554909051, -47.01562500047794657, 25.37105061671875461 ) ) ;
#34066=CARTESIAN_POINT ( 'NONE',  ( 7.567941867304905479, -47.05312500047795510, 29.19375250200204164 ) ) ;
#34068=ORIENTED_EDGE ( 'NONE', *, *, #22040, .T. ) ;
#34069=DIRECTION ( 'NONE',  ( 0.000000000000000000, 0.000000000000000000, -1.000000000000000000 ) ) ;
#34072=CARTESIAN_POINT ( 'NONE',  ( 7.757384923554904610, -45.70833333333332149, 27.17302655983835180 ) ) ;
#34073=CARTESIAN_POINT ( 'NONE',  ( 7.567941867304904591, -49.14062500047794657, 29.19375250200204164 ) ) ;
#34084=CARTESIAN_POINT ( 'NONE',  ( 0.7573849235549138248, -48.23541666762256597, 27.17302655983835180 ) ) ;
#34102=CARTESIAN_POINT ( 'NONE',  ( 4.257351432995529983, -51.31874920356175096, 25.69375250216227613 ) ) ;
#34105=( BOUNDED_CURVE ( )  B_SPLINE_CURVE ( 2, ( #39181, #3256, #35162, #22609, #16239, #29180, #28569, #38984, #35791 ),
 .UNSPECIFIED., .F., .F. ) 
 B_SPLINE_CURVE_WITH_KNOTS ( ( 3, 2, 2, 2, 3 ),
 ( 0.6875000000000000000, 0.6916666666666666519, 0.6999999999999999556, 0.7083333333333333703, 0.7125000000000000222 ),
 .UNSPECIFIED. ) 
 CURVE ( )  GEOMETRIC_REPRESENTATION_ITEM ( )  RATIONAL_B_SPLINE_CURVE ( ( 0.9330127018922194093, 0.9330127018922194093, 1.000000000000000000, 0.8660254037844387076, 1.000000000000000000, 0.8660254037844387076, 1.000000000000000000, 0.9330127018922194093, 0.9330127018922194093 ) ) 
 REPRESENTATION_ITEM ( '' )  );
#34111=CARTESIAN_POINT ( 'NONE',  ( 2.602106451679912169, -43.47395833381127517, 26.32672608803957459 ) ) ;
#34118=CARTESIAN_POINT ( 'NONE',  ( 7.757384923554904610, -45.73895833323773275, 27.17302655983835180 ) ) ;
#34125=CARTESIAN_POINT ( 'NONE',  ( 0.9468279798049115126, -50.76145833381128369, 31.10510344464368515 ) ) ;
#34127=ORIENTED_EDGE ( 'NONE', *, *, #1717, .F. ) ;
#34151=CARTESIAN_POINT ( 'NONE',  ( 4.257384923554919709, -49.37499999999997868, 32.69375250200203453 ) ) ;
#34158=CARTESIAN_POINT ( 'NONE',  ( 0.9468279798049143992, -50.43229166714461087, 27.28240155936039812 ) ) ;
#34161=CARTESIAN_POINT ( 'NONE',  ( 1.204833007978848292, -45.23607320638263474, 27.42104723068166194 ) ) ;
#34173=EDGE_CURVE ( 'NONE', #27786, #8274, #7525, .T. ) ;
#34177=CARTESIAN_POINT ( 'NONE',  ( 0.7573849235549120484, -48.65208333428924448, 31.21447844416572792 ) ) ;
#34178=CARTESIAN_POINT ( 'NONE',  ( 7.567941867304902814, -43.68229166714462508, 31.10510344464368870 ) ) ;
#34200=CARTESIAN_POINT ( 'NONE',  ( 7.539778254675991498, -42.91446893368956950, 27.93780033891722780 ) ) ;
#34208=EDGE_CURVE ( 'NONE', #2420, #39859, #38750, .T. ) ;
#34226=CARTESIAN_POINT ( 'NONE',  ( 4.257384923554909051, -42.42812500047794799, 25.37105061671875461 ) ) ;
#34232=DIRECTION ( 'NONE',  ( -0.000000000000000000, -1.000000000000000000, -0.000000000000000000 ) ) ;
#34247=LINE ( 'NONE', #31676, #14228 ) ;
#34259=CARTESIAN_POINT ( 'NONE',  ( 4.257384923554908163, -48.67812500047794089, 33.01645438728532866 ) ) ;
#34263=DIRECTION ( 'NONE',  ( 0.000000000000000000, 0.000000000000000000, -1.000000000000000000 ) ) ;
#34264=CARTESIAN_POINT ( 'NONE',  ( 4.257384923554909051, -45.12499999999998579, 25.15230061767466552 ) ) ;
#34266=CARTESIAN_POINT ( 'NONE',  ( 3.521103250694149089, -42.80116572181899670, 25.76910142005831972 ) ) ;
#34269=CARTESIAN_POINT ( 'NONE',  ( 0.9468279798049132889, -46.39062500047794657, 29.19375250200204164 ) ) ;
#34271=CARTESIAN_POINT ( 'NONE',  ( 7.567941867304905479, -48.05312500047795510, 29.19375250200204164 ) ) ;
#34274=DIRECTION ( 'NONE',  ( 0.000000000000000000, 0.000000000000000000, 1.000000000000000000 ) ) ;
#34275=VECTOR ( 'NONE', #23109, 1000.000000000000000 ) ;
#34278=CARTESIAN_POINT ( 'NONE',  ( 0.7573849235549138248, -44.54166666666666430, 27.17302655983835180 ) ) ;
#34279=CARTESIAN_POINT ( 'NONE',  ( 0.9468279798049143992, -48.43229166714461087, 27.28240155936039457 ) ) ;
#34280=ORIENTED_EDGE ( 'NONE', *, *, #8672, .T. ) ;
#34281=CARTESIAN_POINT ( 'NONE',  ( 4.257384923554907274, -48.37499999999998579, 32.69375250200203453 ) ) ;
#34282=LINE ( 'NONE', #40660, #30974 ) ;
#34290=CARTESIAN_POINT ( 'NONE',  ( 6.007384923554904610, -47.02708333428923737, 32.22484141524757462 ) ) ;
#34293=( NAMED_UNIT ( * ) PLANE_ANGLE_UNIT ( ) SI_UNIT ( $, .RADIAN. ) );
#34303=VECTOR ( 'NONE', #34232, 1000.000000000000000 ) ;
#34321=CARTESIAN_POINT ( 'NONE',  ( 0.9468279798049132889, -42.39062500047794657, 29.19375250200204164 ) ) ;
#34325=CARTESIAN_POINT ( 'NONE',  ( 7.583220342300430517, -44.41826972659180939, 28.01107894801861775 ) ) ;
#34330=CARTESIAN_POINT ( 'NONE',  ( 6.007384923554907274, -44.19729166657106845, 26.16266358875650866 ) ) ;
#34337=CARTESIAN_POINT ( 'NONE',  ( 2.732841365560914060, -42.10504865709861377, 32.35500875273027077 ) ) ;
#34347=CARTESIAN_POINT ( 'NONE',  ( 9.589638516698011372, 3.250000000000000444, 31.84134197688108614 ) ) ;
#34353=( BOUNDED_CURVE ( )  B_SPLINE_CURVE ( 2, ( #42112, #26159, #3591, #19761, #12966, #29964, #23163, #20194, #6371 ),
 .UNSPECIFIED., .F., .T. ) 
 B_SPLINE_CURVE_WITH_KNOTS ( ( 3, 2, 2, 2, 3 ),
 ( 0.4874999999999999889, 0.4916666666666666408, 0.5000000000000000000, 0.5083333333333333037, 0.5124999999999999556 ),
 .UNSPECIFIED. ) 
 CURVE ( )  GEOMETRIC_REPRESENTATION_ITEM ( )  RATIONAL_B_SPLINE_CURVE ( ( 0.9330127018922194093, 0.9330127018922194093, 1.000000000000000000, 0.8660254037844387076, 1.000000000000000000, 0.8660254037844387076, 1.000000000000000000, 0.9330127018922202975, 0.9330127018922194093 ) ) 
 REPRESENTATION_ITEM ( '' )  );
#34371=CARTESIAN_POINT ( 'NONE',  ( 0.9468279798049132889, -51.39062500047794657, 29.19375250200204164 ) ) ;
#34372=CARTESIAN_POINT ( 'NONE',  ( 2.507384923554911715, -48.58333333333332860, 26.16266358875650866 ) ) ;
#34374=CARTESIAN_POINT ( 'NONE',  ( 1.455406808252675654, -45.14140222971946059, 31.34072148585644868 ) ) ;
#34382=CARTESIAN_POINT ( 'NONE',  ( 4.257384923554908163, -50.90562499990440415, 33.23520438632941421 ) ) ;
#34388=CARTESIAN_POINT ( 'NONE',  ( 4.257384923554908163, -50.56875000095590167, 33.23520438632941421 ) ) ;
#34389=DIRECTION ( 'NONE',  ( 0.000000000000000000, 0.000000000000000000, 1.000000000000000000 ) ) ;
#34393=CARTESIAN_POINT ( 'NONE',  ( 0.8223168492497393567, -46.70836192712452828, 28.52251983146150138 ) ) ;
#34416=CARTESIAN_POINT ( 'NONE',  ( 1.294725397210737317, -48.23774902177894575, 27.28043105152917391 ) ) ;
#34420=CARTESIAN_POINT ( 'NONE',  ( 4.256052897247872835, -46.31871828613508058, 25.69375247191860367 ) ) ;
#34423=CARTESIAN_POINT ( 'NONE',  ( 7.668661145120916345, -48.96640557130209004, 30.11937791270323572 ) ) ;
#34430=CYLINDRICAL_SURFACE ( 'NONE', #38186, 3.499999999999996003 ) ;
#34436=CARTESIAN_POINT ( 'NONE',  ( 4.257384923554909051, -44.42812500047794799, 25.37105061671875461 ) ) ;
#34440=FACE_OUTER_BOUND ( 'NONE', #8070, .T. ) ;
#34443=VERTEX_POINT ( 'NONE', #30596 ) ;
#34450=CYLINDRICAL_SURFACE ( 'NONE', #34740, 3.499999999999996003 ) ;
#34464=CARTESIAN_POINT ( 'NONE',  ( 7.567941867304905479, -46.55312500047795510, 29.19375250200204164 ) ) ;
#34475=CARTESIAN_POINT ( 'NONE',  ( 2.602106451679912169, -42.97395833381127517, 26.32672608803957459 ) ) ;
#34476=CARTESIAN_POINT ( 'NONE',  ( 4.257384923554909051, -47.92812500047795510, 25.37105061671875106 ) ) ;
#34479=DIRECTION ( 'NONE',  ( -0.4447208605404113779, 0.000000000000000000, 0.8956692225370903593 ) ) ;
#34484=CARTESIAN_POINT ( 'NONE',  ( 7.757384923554904610, -44.70833333333332860, 27.17302655983835180 ) ) ;
#34485=CARTESIAN_POINT ( 'NONE',  ( 5.912663395429907709, -47.55729166714461087, 26.32672608803957459 ) ) ;
#34491=CARTESIAN_POINT ( 'NONE',  ( 4.257393644456948678, -47.56839819610503639, 32.69375250198117300 ) ) ;
#34497=CARTESIAN_POINT ( 'NONE',  ( 4.257384923554908163, -47.56875000095590877, 33.23520438632941421 ) ) ;
#34528=CARTESIAN_POINT ( 'NONE',  ( 7.567941867304904591, -42.59895833381128227, 27.28240155936039812 ) ) ;
#34532=CARTESIAN_POINT ( 'NONE',  ( 3.044481415175604333, -42.20865620537255580, 32.27411812269912161 ) ) ;
#34535=CARTESIAN_POINT ( 'NONE',  ( 7.757384923554905498, -44.28062499990439704, 29.19375250200204164 ) ) ;
#34539=ORIENTED_EDGE ( 'NONE', *, *, #33181, .F. ) ;
#34542=CARTESIAN_POINT ( 'NONE',  ( 7.567941867304905479, -50.51145833381129080, 27.28240155936039812 ) ) ;
#34573=CARTESIAN_POINT ( 'NONE',  ( 4.257384923554908163, -50.26562500047794657, 33.01645438728532866 ) ) ;
#34576=CARTESIAN_POINT ( 'NONE',  ( 2.503710620883555116, -45.27814742846257445, 26.13071302519840700 ) ) ;
#34585=CARTESIAN_POINT ( 'NONE',  ( 4.257384923554909051, -49.65562499990439704, 25.15230061767466552 ) ) ;
#34593=CARTESIAN_POINT ( 'NONE',  ( 2.507384923554909495, -47.61041666762257307, 32.22484141524756751 ) ) ;
#34599=( BOUNDED_CURVE ( )  B_SPLINE_CURVE ( 2, ( #8263, #1055, #18050, #35048, #2085, #25489, #37611, #32060, #5703 ),
 .UNSPECIFIED., .F., .F. ) 
 B_SPLINE_CURVE_WITH_KNOTS ( ( 3, 2, 2, 2, 3 ),
 ( 0.2875000000000000333, 0.2916666666666666852, 0.2999999999999999889, 0.3083333333333333481, 0.3125000000000000000 ),
 .UNSPECIFIED. ) 
 CURVE ( )  GEOMETRIC_REPRESENTATION_ITEM ( )  RATIONAL_B_SPLINE_CURVE ( ( 0.9330127018922194093, 0.9330127018922198534, 1.000000000000000000, 0.8660254037844387076, 1.000000000000000000, 0.8660254037844387076, 1.000000000000000000, 0.9330127018922194093, 0.9330127018922194093 ) ) 
 REPRESENTATION_ITEM ( '' )  );
#34615=CARTESIAN_POINT ( 'NONE',  ( 6.007384923554907274, -42.66666666666665719, 26.16266358875650866 ) ) ;
#34620=CARTESIAN_POINT ( 'NONE',  ( 3.407513008591248393, -48.08628814135286689, 32.62314779344220739 ) ) ;
#34624=FACE_OUTER_BOUND ( 'NONE', #32639, .T. ) ;
#34627=CARTESIAN_POINT ( 'NONE',  ( 6.406496052514045303, -49.01680837995324680, 31.95651883406101135 ) ) ;
#34633=CARTESIAN_POINT ( 'NONE',  ( 4.257384923554909051, 0.8500000000000035305, 29.19375250200204164 ) ) ;
#34642=CARTESIAN_POINT ( 'NONE',  ( 0.9468279798049134000, -43.34479166714461229, 27.28240155936039457 ) ) ;
#34656=CARTESIAN_POINT ( 'NONE',  ( 4.257384923554909051, -52.75000000000000000, 29.19375250200204164 ) ) ;
#34682=CARTESIAN_POINT ( 'NONE',  ( 4.257384923554908163, -44.26562500047795368, 33.01645438728532866 ) ) ;
#34683=CARTESIAN_POINT ( 'NONE',  ( 7.567941867304902814, -44.09479166714461940, 31.10510344464368870 ) ) ;
#34691=CARTESIAN_POINT ( 'NONE',  ( 0.7573849235549129366, -45.49999999999999289, 29.19375250200204164 ) ) ;
#34692=CARTESIAN_POINT ( 'NONE',  ( 7.567941867304902814, -47.18229166714461087, 31.10510344464368870 ) ) ;
#34695=AXIS2_PLACEMENT_3D ( 'NONE', #36089, #12927, #792 ) ;
#34697=DIRECTION ( 'NONE',  ( -0.000000000000000000, -1.000000000000000000, -0.000000000000000000 ) ) ;
#34704=VERTEX_POINT ( 'NONE', #15062 ) ;
#34705=CARTESIAN_POINT ( 'NONE',  ( 0.7573849235549129366, -47.19375000095590877, 29.19375250200204164 ) ) ;
#34718=( BOUNDED_CURVE ( )  B_SPLINE_CURVE ( 2, ( #13098, #29459, #22882, #19482, #32450, #36054, #3114, #13511, #26082 ),
 .UNSPECIFIED., .F., .T. ) 
 B_SPLINE_CURVE_WITH_KNOTS ( ( 3, 2, 2, 2, 3 ),
 ( 0.9124999999999999778, 0.9166666666666666297, 0.9250000000000000444, 0.9333333333333333481, 0.9375000000000000000 ),
 .UNSPECIFIED. ) 
 CURVE ( )  GEOMETRIC_REPRESENTATION_ITEM ( )  RATIONAL_B_SPLINE_CURVE ( ( 0.9330127018922194093, 0.9330127018922194093, 1.000000000000000000, 0.8660254037844387076, 1.000000000000000000, 0.8660254037844387076, 1.000000000000000000, 0.9330127018922194093, 0.9330127018922194093 ) ) 
 REPRESENTATION_ITEM ( '' )  );
#34725=CARTESIAN_POINT ( 'NONE',  ( 4.257384923554909939, 7.250000000000000000, 21.03247289836684786 ) ) ;
#34726=CARTESIAN_POINT ( 'NONE',  ( 7.757384923554905498, -52.24999999999999289, 29.19375250200204164 ) ) ;
#34729=CARTESIAN_POINT ( 'NONE',  ( 6.007384923554904610, -50.83333333333332860, 32.22484141524757462 ) ) ;
#34736=CARTESIAN_POINT ( 'NONE',  ( 4.712978608380411494, -50.32861131734955507, 25.72165364851379721 ) ) ;
#34740=AXIS2_PLACEMENT_3D ( 'NONE', #34656, #24890, #8708 ) ;
#34743=CARTESIAN_POINT ( 'NONE',  ( 6.955504822719134950, -42.34138404992432925, 34.01771537441437943 ) ) ;
#34745=ORIENTED_EDGE ( 'NONE', *, *, #32085, .F. ) ;
#34748=CARTESIAN_POINT ( 'NONE',  ( 7.757384923554904610, -43.70833333333332149, 27.17302655983835180 ) ) ;
#34749=CARTESIAN_POINT ( 'NONE',  ( 0.9468279798049115126, -48.26145833381129080, 31.10510344464368515 ) ) ;
#34766=CARTESIAN_POINT ( 'NONE',  ( 7.757384923554902834, -43.29166666666665719, 31.21447844416572792 ) ) ;
#34775=CARTESIAN_POINT ( 'NONE',  ( 5.195207097063836876, -49.64732909936924443, 25.69375250200204519 ) ) ;
#34783=CARTESIAN_POINT ( 'NONE',  ( 4.257384923554908163, -48.26562500047794657, 33.01645438728532866 ) ) ;
#34797=CARTESIAN_POINT ( 'NONE',  ( 6.007384923554904610, -50.36395833323773985, 32.22484141524757462 ) ) ;
#34801=ORIENTED_EDGE ( 'NONE', *, *, #8714, .T. ) ;
#34804=CARTESIAN_POINT ( 'NONE',  ( 6.007384923554904610, -46.52708333428923737, 32.22484141524757462 ) ) ;
#34838=LINE ( 'NONE', #25699, #19154 ) ;
#34841=CARTESIAN_POINT ( 'NONE',  ( 4.257384923554907274, -44.37499999999999289, 32.69375250200203453 ) ) ;
#34847=CARTESIAN_POINT ( 'NONE',  ( 2.975067305262454997, -42.09928137282000904, 32.45038596706375955 ) ) ;
#34852=( BOUNDED_SURFACE ( )  B_SPLINE_SURFACE ( 1, 2, ( 
 ( #28781, #3265, #16250, #69, #26029, #9876, #35800, #6662, #19628, #32601, #9016, #5833, #3466, #16457, #41354, #12206, #21993, #34965, #31764, #2634, #16871, #36210, #36001, #10485, #4528, #29621, #702, #13674, #20060, #13257, #29407, #30048, #20698, #921, #4317, #13458, #4099, #17082, #13888, #10069, #10913, #23244, #26655, #23899, #7082, #26867, #16663, #33024, #10274, #27078, #20268, #39839, #10700, #3890, #29835, #23684, #36646, #36867, #7511, #33235, #40044, #20487, #39615, #6868, #7727, #3677, #23470, #33675, #488, #33454, #36433, #7298, #17299, #32807, #30263, #26243, #275, #39192, #1134, #23032, #19840, #14105, #26442, #39398, #14738, #21112, #37486, #8133, #17713, #34084, #24311, #4942, #11734, #24730, #30898, #31303, #27905, #15149, #37281, #17921, #1342, #24109, #14530, #21528, #1758, #34497, #27697, #41096, #40259, #5355, #40667, #11525, #37081, #24517, #34705, #30684, #8340, #21320, #34290, #14315, #17508, #18131, #8757, #31101, #18332, #1550, #5154, #1955, #14936, #11128, #11945, #11325, #40879, #24940, #37693, #8550, #4735, #2163, #40470, #28112, #37898, #21731, #30472, #27294, #7936, #20903, #33875, #27502, #25144, #41305, #8966, #38109, #2382, #18546, #21939, #31513, #28319, #5570, #12152, #15371, #26700, #10321, #17129, #6914, #7552, #29454, #40089, #325, #19892, #36909, #10956, #26915, #36047, #17342, #13304, #23942, #39662, #36478, #7132, #36260, #7771, #26287, #29883, #30091, #20744, #32856, #3513, #23516, #26492, #39235, #16707, #3722, #23081, #29667, #10116, #4362, #16916, #531, #20104, #749, #13722, #13504, #16504, #7341, #30304, #20313, #39447, #23294, #33067, #3934, #966, #33280, #39878, #4145, #13935, #10740, #23726, #36690, #20529, #33500, #1177, #14144, #27120, #1798, #33919, #33719, #5198, #20946, #4570, #24775, #2214, #1593, #17758, #30514, #27741, #30729, #41144, #34337, #24983 ),
 ( #40924, #37739, #11568, #24562, #14571, #40512, #28155, #40711, #4777, #8178, #8382, #17549, #2001, #37525, #8596, #14779, #24353, #14985, #21569, #18174, #11369, #37944, #1383, #11990, #21362, #37323, #14358, #31142, #7977, #5402, #21150, #34125, #4984, #17963, #30941, #27949, #11779, #34542, #27334, #18381, #31350, #11171, #15193, #8806, #40302, #24155, #37124, #9651, #28776, #28986, #9225, #5828, #15617, #41983, #3831, #12628, #23184, #31555, #22401, #36150, #22198, #12832, #25816, #15833, #29773, #25400, #38780, #9434, #16045, #3054, #32190, #9012, #34958, #16810, #7022, #31760, #20000, #38361, #12416, #32965, #35166, #636, #13610, #25607, #26594, #6031, #38153, #28575, #39552, #21778, #38568, #34749, #2425, #35379, #5619, #19007, #18592, #15412, #41771, #28365, #31974, #41350, #6242, #12201, #25193, #21989, #18800, #2630, #41563, #2842, #19219, #17655, #27021, #1077, #4676, #14050, #33819, #30620, #14253, #1486, #10849, #26811, #27232, #7449, #14676, #33389, #858, #7878, #40195, #14464, #23622, #39778, #4473, #17454, #24048, #11066, #37017, #27636, #30830, #30413, #20636, #10645, #10429, #20845, #36581, #23408, #27438, #21050, #20425, #4255, #7241, #1283, #17239, #17858, #40405, #1694, #7664, #33173, #4879, #29984, #30200, #11266, #39984, #24249, #37218, #8073, #34027, #23836, #36803, #36373, #20211, #33613, #4039, #17022, #13830, #8906, #5507, #2526, #21664, #31241, #21878, #15510, #12088, #34436, #2736, #37425, #5929, #18482, #2103, #21258, #38044, #14875, #12306, #5296, #40819, #41032, #15088, #18269, #11883, #34854, #37836, #8282, #31449, #8484, #18068, #28050, #21462, #2319, #11464, #34642, #28466, #15306, #5720, #24875, #24669, #31039, #8692, #28261, #41244, #24455, #25080, #41455, #18699, #31660, #25290, #37629, #38254, #9116, #22095, #35069, #18901, #34226, #31867, #15721, #40607, #5087, #1893, #27843, #11671 ) ),
 .UNSPECIFIED., .F., .F., .T. ) 
 B_SPLINE_SURFACE_WITH_KNOTS ( ( 2, 2 ),
 ( 3, 2, 2, 2, 2, 2, 2, 2, 2, 2, 2, 2, 2, 2, 2, 2, 2, 2, 2, 2, 2, 2, 2, 2, 2, 2, 2, 2, 2, 2, 2, 2, 2, 2, 2, 2, 2, 2, 2, 2, 2, 2, 2, 2, 2, 2, 2, 2, 2, 2, 2, 2, 2, 2, 2, 2, 2, 2, 2, 2, 2, 2, 2, 2, 2, 2, 2, 2, 2, 2, 2, 2, 2, 2, 2, 2, 2, 2, 2, 2, 2, 2, 2, 2, 2, 2, 2, 2, 2, 2, 2, 2, 2, 2, 2, 2, 2, 2, 2, 2, 2, 2, 2, 2, 2, 2, 2, 2, 2, 2, 2, 2, 2, 2, 2, 2, 2, 2, 2, 3 ),
 ( 0.000000000000000000, 1.000000000000000000 ),
 ( 0.000000000000000000, 0.008333333333333333218, 0.01666666666666666644, 0.02500000000000000139, 0.03333333333333333287, 0.04166666666666666435, 0.05000000000000000278, 0.05833333333333333426, 0.06666666666666666574, 0.07499999999999999722, 0.08333333333333332871, 0.09166666666666666019, 0.1000000000000000056, 0.1083333333333333370, 0.1166666666666666685, 0.1250000000000000000, 0.1333333333333333315, 0.1416666666666666630, 0.1499999999999999944, 0.1583333333333333259, 0.1666666666666666574, 0.1749999999999999889, 0.1833333333333333204, 0.1916666666666666796, 0.2000000000000000111, 0.2083333333333333426, 0.2166666666666666741, 0.2250000000000000056, 0.2333333333333333370, 0.2416666666666666685, 0.2500000000000000000, 0.2583333333333333592, 0.2666666666666666630, 0.2750000000000000222, 0.2833333333333333259, 0.2916666666666666852, 0.2999999999999999889, 0.3083333333333333481, 0.3166666666666666519, 0.3250000000000000111, 0.3333333333333333148, 0.3416666666666666741, 0.3499999999999999778, 0.3583333333333333370, 0.3666666666666666408, 0.3750000000000000000, 0.3833333333333333592, 0.3916666666666666630, 0.4000000000000000222, 0.4083333333333333259, 0.4166666666666666852, 0.4249999999999999889, 0.4333333333333333481, 0.4416666666666666519, 0.4500000000000000111, 0.4583333333333333148, 0.4666666666666666741, 0.4749999999999999778, 0.4833333333333333370, 0.4916666666666666408, 0.5000000000000000000, 0.5083333333333333037, 0.5166666666666667185, 0.5250000000000000222, 0.5333333333333333259, 0.5416666666666666297, 0.5500000000000000444, 0.5583333333333333481, 0.5666666666666666519, 0.5749999999999999556, 0.5833333333333333703, 0.5916666666666666741, 0.5999999999999999778, 0.6083333333333332815, 0.6166666666666666963, 0.6250000000000000000, 0.6333333333333333037, 0.6416666666666667185, 0.6500000000000000222, 0.6583333333333333259, 0.6666666666666666297, 0.6750000000000000444, 0.6833333333333333481, 0.6916666666666666519, 0.6999999999999999556, 0.7083333333333333703, 0.7166666666666666741, 0.7249999999999999778, 0.7333333333333332815, 0.7416666666666666963, 0.7500000000000000000, 0.7583333333333333037, 0.7666666666666667185, 0.7750000000000000222, 0.7833333333333333259, 0.7916666666666666297, 0.8000000000000000444, 0.8083333333333333481, 0.8166666666666666519, 0.8249999999999999556, 0.8333333333333333703, 0.8416666666666666741, 0.8499999999999999778, 0.8583333333333332815, 0.8666666666666666963, 0.8750000000000000000, 0.8833333333333333037, 0.8916666666666667185, 0.9000000000000000222, 0.9083333333333333259, 0.9166666666666666297, 0.9250000000000000444, 0.9333333333333333481, 0.9416666666666666519, 0.9499999999999999556, 0.9583333333333333703, 0.9666666666666666741, 0.9749999999999999778, 0.9833333333333332815, 0.9845487975508080414 ),
 .UNSPECIFIED. ) 
 GEOMETRIC_REPRESENTATION_ITEM ( )  RATIONAL_B_SPLINE_SURFACE ( (
 ( 1.000000000000000000, 0.8660254037844387076, 1.000000000000000000, 0.8660254037844387076, 1.000000000000000000, 0.8660254037844387076, 1.000000000000000000, 0.8660254037844387076, 1.000000000000000000, 0.8660254037844387076, 1.000000000000000000, 0.8660254037844387076, 1.000000000000000000, 0.8660254037844387076, 1.000000000000000000, 0.8660254037844387076, 1.000000000000000000, 0.8660254037844387076, 1.000000000000000000, 0.8660254037844387076, 1.000000000000000000, 0.8660254037844387076, 1.000000000000000000, 0.8660254037844387076, 1.000000000000000000, 0.8660254037844387076, 1.000000000000000000, 0.8660254037844387076, 1.000000000000000000, 0.8660254037844387076, 1.000000000000000000, 0.8660254037844387076, 1.000000000000000000, 0.8660254037844387076, 1.000000000000000000, 0.8660254037844387076, 1.000000000000000000, 0.8660254037844387076, 1.000000000000000000, 0.8660254037844387076, 1.000000000000000000, 0.8660254037844387076, 1.000000000000000000, 0.8660254037844387076, 1.000000000000000000, 0.8660254037844387076, 1.000000000000000000, 0.8660254037844387076, 1.000000000000000000, 0.8660254037844387076, 1.000000000000000000, 0.8660254037844387076, 1.000000000000000000, 0.8660254037844387076, 1.000000000000000000, 0.8660254037844387076, 1.000000000000000000, 0.8660254037844387076, 1.000000000000000000, 0.8660254037844387076, 1.000000000000000000, 0.8660254037844387076, 1.000000000000000000, 0.8660254037844387076, 1.000000000000000000, 0.8660254037844387076, 1.000000000000000000, 0.8660254037844387076, 1.000000000000000000, 0.8660254037844387076, 1.000000000000000000, 0.8660254037844387076, 1.000000000000000000, 0.8660254037844387076, 1.000000000000000000, 0.8660254037844387076, 1.000000000000000000, 0.8660254037844387076, 1.000000000000000000, 0.8660254037844387076, 1.000000000000000000, 0.8660254037844387076, 1.000000000000000000, 0.8660254037844387076, 1.000000000000000000, 0.8660254037844387076, 1.000000000000000000, 0.8660254037844387076, 1.000000000000000000, 0.8660254037844387076, 1.000000000000000000, 0.8660254037844387076, 1.000000000000000000, 0.8660254037844387076, 1.000000000000000000, 0.8660254037844387076, 1.000000000000000000, 0.8660254037844387076, 1.000000000000000000, 0.8660254037844387076, 1.000000000000000000, 0.8660254037844387076, 1.000000000000000000, 0.8660254037844387076, 1.000000000000000000, 0.8660254037844387076, 1.000000000000000000, 0.8660254037844387076, 1.000000000000000000, 0.8660254037844387076, 1.000000000000000000, 0.8660254037844387076, 1.000000000000000000, 0.8660254037844387076, 1.000000000000000000, 0.8660254037844387076, 1.000000000000000000, 0.8660254037844387076, 1.000000000000000000, 0.8660254037844387076, 1.000000000000000000, 0.8660254037844387076, 1.000000000000000000, 0.8660254037844387076, 1.000000000000000000, 0.8660254037844387076, 1.000000000000000000, 0.8660254037844387076, 1.000000000000000000, 0.8660254037844387076, 1.000000000000000000, 0.8660254037844387076, 1.000000000000000000, 0.8660254037844387076, 1.000000000000000000, 0.8660254037844387076, 1.000000000000000000, 0.8660254037844387076, 1.000000000000000000, 0.8660254037844387076, 1.000000000000000000, 0.8660254037844387076, 1.000000000000000000, 0.8660254037844387076, 1.000000000000000000, 0.8660254037844387076, 1.000000000000000000, 0.8660254037844387076, 1.000000000000000000, 0.8660254037844387076, 1.000000000000000000, 0.8660254037844387076, 1.000000000000000000, 0.8660254037844387076, 1.000000000000000000, 0.8660254037844387076, 1.000000000000000000, 0.8660254037844387076, 1.000000000000000000, 0.8660254037844387076, 1.000000000000000000, 0.8660254037844387076, 1.000000000000000000, 0.8660254037844387076, 1.000000000000000000, 0.8660254037844387076, 1.000000000000000000, 0.8660254037844387076, 1.000000000000000000, 0.8660254037844387076, 1.000000000000000000, 0.8660254037844387076, 1.000000000000000000, 0.8660254037844387076, 1.000000000000000000, 0.8660254037844387076, 1.000000000000000000, 0.8660254037844387076, 1.000000000000000000, 0.8660254037844387076, 1.000000000000000000, 0.8660254037844387076, 1.000000000000000000, 0.8660254037844387076, 1.000000000000000000, 0.8660254037844387076, 1.000000000000000000, 0.8660254037844387076, 1.000000000000000000, 0.8660254037844387076, 1.000000000000000000, 0.8660254037844387076, 1.000000000000000000, 0.8660254037844387076, 1.000000000000000000, 0.8660254037844387076, 1.000000000000000000, 0.8660254037844387076, 1.000000000000000000, 0.8660254037844387076, 1.000000000000000000, 0.8660254037844387076, 1.000000000000000000, 0.8660254037844387076, 1.000000000000000000, 0.8660254037844387076, 1.000000000000000000, 0.8660254037844387076, 1.000000000000000000, 0.8660254037844387076, 1.000000000000000000, 0.8660254037844387076, 1.000000000000000000, 0.8660254037844387076, 1.000000000000000000, 0.8660254037844387076, 1.000000000000000000, 0.8660254037844387076, 1.000000000000000000, 0.8660254037844387076, 1.000000000000000000, 0.8660254037844387076, 1.000000000000000000, 0.8660254037844387076, 1.000000000000000000, 0.8660254037844387076, 1.000000000000000000, 0.8660254037844387076, 1.000000000000000000, 0.8660254037844387076, 1.000000000000000000, 0.8660254037844387076, 1.000000000000000000, 0.8660254037844387076, 1.000000000000000000, 0.8660254037844387076, 1.000000000000000000, 0.9804590406699229543, 0.9666184021816470739),
 ( 1.000000000000000000, 0.8660254037844387076, 1.000000000000000000, 0.8660254037844387076, 1.000000000000000000, 0.8660254037844387076, 1.000000000000000000, 0.8660254037844387076, 1.000000000000000000, 0.8660254037844387076, 1.000000000000000000, 0.8660254037844387076, 1.000000000000000000, 0.8660254037844387076, 1.000000000000000000, 0.8660254037844387076, 1.000000000000000000, 0.8660254037844387076, 1.000000000000000000, 0.8660254037844387076, 1.000000000000000000, 0.8660254037844387076, 1.000000000000000000, 0.8660254037844387076, 1.000000000000000000, 0.8660254037844387076, 1.000000000000000000, 0.8660254037844387076, 1.000000000000000000, 0.8660254037844387076, 1.000000000000000000, 0.8660254037844387076, 1.000000000000000000, 0.8660254037844387076, 1.000000000000000000, 0.8660254037844387076, 1.000000000000000000, 0.8660254037844387076, 1.000000000000000000, 0.8660254037844387076, 1.000000000000000000, 0.8660254037844387076, 1.000000000000000000, 0.8660254037844387076, 1.000000000000000000, 0.8660254037844387076, 1.000000000000000000, 0.8660254037844387076, 1.000000000000000000, 0.8660254037844387076, 1.000000000000000000, 0.8660254037844387076, 1.000000000000000000, 0.8660254037844387076, 1.000000000000000000, 0.8660254037844387076, 1.000000000000000000, 0.8660254037844387076, 1.000000000000000000, 0.8660254037844387076, 1.000000000000000000, 0.8660254037844387076, 1.000000000000000000, 0.8660254037844387076, 1.000000000000000000, 0.8660254037844387076, 1.000000000000000000, 0.8660254037844387076, 1.000000000000000000, 0.8660254037844387076, 1.000000000000000000, 0.8660254037844387076, 1.000000000000000000, 0.8660254037844387076, 1.000000000000000000, 0.8660254037844387076, 1.000000000000000000, 0.8660254037844387076, 1.000000000000000000, 0.8660254037844387076, 1.000000000000000000, 0.8660254037844387076, 1.000000000000000000, 0.8660254037844387076, 1.000000000000000000, 0.8660254037844387076, 1.000000000000000000, 0.8660254037844387076, 1.000000000000000000, 0.8660254037844387076, 1.000000000000000000, 0.8660254037844387076, 1.000000000000000000, 0.8660254037844387076, 1.000000000000000000, 0.8660254037844387076, 1.000000000000000000, 0.8660254037844387076, 1.000000000000000000, 0.8660254037844387076, 1.000000000000000000, 0.8660254037844387076, 1.000000000000000000, 0.8660254037844387076, 1.000000000000000000, 0.8660254037844387076, 1.000000000000000000, 0.8660254037844387076, 1.000000000000000000, 0.8660254037844387076, 1.000000000000000000, 0.8660254037844387076, 1.000000000000000000, 0.8660254037844387076, 1.000000000000000000, 0.8660254037844387076, 1.000000000000000000, 0.8660254037844387076, 1.000000000000000000, 0.8660254037844387076, 1.000000000000000000, 0.8660254037844387076, 1.000000000000000000, 0.8660254037844387076, 1.000000000000000000, 0.8660254037844387076, 1.000000000000000000, 0.8660254037844387076, 1.000000000000000000, 0.8660254037844387076, 1.000000000000000000, 0.8660254037844387076, 1.000000000000000000, 0.8660254037844387076, 1.000000000000000000, 0.8660254037844387076, 1.000000000000000000, 0.8660254037844387076, 1.000000000000000000, 0.8660254037844387076, 1.000000000000000000, 0.8660254037844387076, 1.000000000000000000, 0.8660254037844387076, 1.000000000000000000, 0.8660254037844387076, 1.000000000000000000, 0.8660254037844387076, 1.000000000000000000, 0.8660254037844387076, 1.000000000000000000, 0.8660254037844387076, 1.000000000000000000, 0.8660254037844387076, 1.000000000000000000, 0.8660254037844387076, 1.000000000000000000, 0.8660254037844387076, 1.000000000000000000, 0.8660254037844387076, 1.000000000000000000, 0.8660254037844387076, 1.000000000000000000, 0.8660254037844387076, 1.000000000000000000, 0.8660254037844387076, 1.000000000000000000, 0.8660254037844387076, 1.000000000000000000, 0.8660254037844387076, 1.000000000000000000, 0.8660254037844387076, 1.000000000000000000, 0.8660254037844387076, 1.000000000000000000, 0.8660254037844387076, 1.000000000000000000, 0.8660254037844387076, 1.000000000000000000, 0.8660254037844387076, 1.000000000000000000, 0.8660254037844387076, 1.000000000000000000, 0.8660254037844387076, 1.000000000000000000, 0.8660254037844387076, 1.000000000000000000, 0.8660254037844387076, 1.000000000000000000, 0.8660254037844387076, 1.000000000000000000, 0.8660254037844387076, 1.000000000000000000, 0.8660254037844387076, 1.000000000000000000, 0.8660254037844387076, 1.000000000000000000, 0.8660254037844387076, 1.000000000000000000, 0.8660254037844387076, 1.000000000000000000, 0.8660254037844387076, 1.000000000000000000, 0.8660254037844387076, 1.000000000000000000, 0.8660254037844387076, 1.000000000000000000, 0.8660254037844387076, 1.000000000000000000, 0.8660254037844387076, 1.000000000000000000, 0.8660254037844387076, 1.000000000000000000, 0.8660254037844387076, 1.000000000000000000, 0.8660254037844387076, 1.000000000000000000, 0.8660254037844387076, 1.000000000000000000, 0.8660254037844387076, 1.000000000000000000, 0.8660254037844387076, 1.000000000000000000, 0.8660254037844387076, 1.000000000000000000, 0.8660254037844387076, 1.000000000000000000, 0.8660254037844387076, 1.000000000000000000, 0.8660254037844387076, 1.000000000000000000, 0.8660254037844387076, 1.000000000000000000, 0.8660254037844387076, 1.000000000000000000, 0.8660254037844387076, 1.000000000000000000, 0.9804590406699229543, 0.9666184021816470739) ) ) 
 REPRESENTATION_ITEM ( '' )  SURFACE ( )  );
#34854=CARTESIAN_POINT ( 'NONE',  ( 0.9468279798049115126, -43.76145833381129080, 31.10510344464368515 ) ) ;
#34868=DIRECTION ( 'NONE',  ( 0.000000000000000000, 0.000000000000000000, 1.000000000000000000 ) ) ;
#34876=CARTESIAN_POINT ( 'NONE',  ( 7.392950100533060009, -45.48354733423890650, 30.81070377214582479 ) ) ;
#34888=CARTESIAN_POINT ( 'NONE',  ( 4.252805270801227167, -42.81864096330718183, 25.69375469310395488 ) ) ;
#34891=CARTESIAN_POINT ( 'NONE',  ( 5.912663395429904156, -44.22395833381127517, 32.06077891596451224 ) ) ;
#34892=CARTESIAN_POINT ( 'NONE',  ( 4.257384923554908163, -44.67812500047794799, 33.01645438728532866 ) ) ;
#34895=VERTEX_POINT ( 'NONE', #26316 ) ;
#34901=B_SPLINE_CURVE_WITH_KNOTS ( 'NONE', 3,
 ( #8417, #18000, #27581, #37774, #28192, #34576, #37980, #5440, #34161, #1423, #27372, #11605, #5019, #14396, #34374, #8839, #5232, #30978, #31177, #30555 ),
 .UNSPECIFIED., .F., .F.,
 ( 4, 2, 2, 2, 2, 2, 2, 2, 2, 4 ),
 ( 0.6728975559533459938, 0.6744858100587988181, 0.6760740641642516424, 0.6792505723751571800, 0.6824270805860628286, 0.6856035887969684772, 0.6887800970078740148, 0.6919566052187796634, 0.6951331134296852010, 0.6983096216405908496 ),
 .UNSPECIFIED. ) ;
#34902=CARTESIAN_POINT ( 'NONE',  ( 6.007384923554904610, -45.33333333333332149, 32.22484141524757462 ) ) ;
#34903=CARTESIAN_POINT ( 'NONE',  ( 7.567941867304904591, -44.14062500047794657, 29.19375250200204164 ) ) ;
#34914=VERTEX_POINT ( 'NONE', #25689 ) ;
#34915=EDGE_CURVE ( 'NONE', #37688, #34930, #22797, .T. ) ;
#34921=CARTESIAN_POINT ( 'NONE',  ( 7.344996782761040066, -42.40485064068575838, 27.54531907653889888 ) ) ;
#34928=CARTESIAN_POINT ( 'NONE',  ( 2.507384923554911715, -44.58333333333332149, 26.16266358875650866 ) ) ;
#34930=VERTEX_POINT ( 'NONE', #143 ) ;
#34935=CARTESIAN_POINT ( 'NONE',  ( 0.7573849235549129366, -50.49999999999998579, 29.19375250200204164 ) ) ;
#34939=CARTESIAN_POINT ( 'NONE',  ( 6.007384923554904610, -49.83333333333332860, 32.22484141524757462 ) ) ;
#34946=FACE_OUTER_BOUND ( 'NONE', #16919, .T. ) ;
#34949=CARTESIAN_POINT ( 'NONE',  ( 3.273854170859787693, -51.09124992744848015, 32.55537303407952265 ) ) ;
#34951=VERTEX_POINT ( 'NONE', #19297 ) ;
#34952=CARTESIAN_POINT ( 'NONE',  ( 4.257384923554908163, -43.90562499990439704, 33.23520438632941421 ) ) ;
#34958=CARTESIAN_POINT ( 'NONE',  ( 7.567941867304905479, -49.05312500047794799, 29.19375250200204164 ) ) ;
#34965=CARTESIAN_POINT ( 'NONE',  ( 0.7573849235549138248, -51.23541666762257307, 27.17302655983835180 ) ) ;
#34967=( BOUNDED_CURVE ( )  B_SPLINE_CURVE ( 2, ( #36166, #29790, #36820, #654, #1907, #8919, #8296, #37645, #24471 ),
 .UNSPECIFIED., .F., .T. ) 
 B_SPLINE_CURVE_WITH_KNOTS ( ( 3, 2, 2, 2, 3 ),
 ( 0.6375000000000000666, 0.6416666666666667185, 0.6500000000000000222, 0.6583333333333333259, 0.6624999999999999778 ),
 .UNSPECIFIED. ) 
 CURVE ( )  GEOMETRIC_REPRESENTATION_ITEM ( )  RATIONAL_B_SPLINE_CURVE ( ( 0.9330127018922194093, 0.9330127018922202975, 1.000000000000000000, 0.8660254037844387076, 1.000000000000000000, 0.8660254037844387076, 1.000000000000000000, 0.9330127018922194093, 0.9330127018922194093 ) ) 
 REPRESENTATION_ITEM ( '' )  );
#34979=B_SPLINE_CURVE_WITH_KNOTS ( 'NONE', 3,
 ( #16766, #3782, #26550, #3162, #32500, #35490, #6348, #36321, #22723, #19952, #9548, #6762, #20166, #19530, #35701, #29299, #590, #7193, #3367, #6564, #32297, #10381, #23358, #33125, #168, #13149, #13564, #26136, #39090, #29727, #32916, #26341, #10169, #23137, #36105, #22506, #9971, #19320, #3990, #22933, #28887, #41883, #12733, #25713, #19736 ),
 .UNSPECIFIED., .F., .F.,
 ( 4, 2, 1, 1, 1, 2, 2, 2, 2, 2, 1, 2, 2, 1, 2, 2, 2, 2, 2, 2, 2, 1, 1, 2, 2, 4 ),
 ( 0.1142655424711453982, 0.1143151768299472959, 0.1143648111887491797, 0.1144640799063529751, 0.1146626173415605660, 0.1150596922119757476, 0.1158538419528061109, 0.1174421414344668235, 0.1206187403977882627, 0.1214128901386186260, 0.1218099650090338076, 0.1220085024442414123, 0.1221077711618452216, 0.1222070398794490170, 0.1237953393611099101, 0.1269719383244317101, 0.1301485372877534963, 0.1333251362510752824, 0.1365017352143970963, 0.1366010039320008917, 0.1366506382908027895, 0.1367002726496046872, 0.1368988100848122780, 0.1372958849552274596, 0.1380900346960578784, 0.1396783341777186604 ),
 .UNSPECIFIED. ) ;
#34998=CARTESIAN_POINT ( 'NONE',  ( 4.257384923554909051, -48.51562500047794657, 25.37105061671875461 ) ) ;
#35011=CARTESIAN_POINT ( 'NONE',  ( 2.507384923554909495, -50.44729166657106845, 32.22484141524756751 ) ) ;
#35016=CARTESIAN_POINT ( 'NONE',  ( 6.685936661271660419, -42.50616591954211998, 31.73830848607751065 ) ) ;
#35017=CARTESIAN_POINT ( 'NONE',  ( 4.257384923554908163, -46.06875000095590167, 33.23520438632941421 ) ) ;
#35022=CARTESIAN_POINT ( 'NONE',  ( 2.797560644556914333, -46.78379106196243953, 25.99132192116024953 ) ) ;
#35044=DIRECTION ( 'NONE',  ( -0.000000000000000000, -1.000000000000000000, -0.000000000000000000 ) ) ;
#35048=CARTESIAN_POINT ( 'NONE',  ( 7.757384923554902834, -49.29166666666665719, 31.21447844416572792 ) ) ;
#35058=CARTESIAN_POINT ( 'NONE',  ( 2.485950939324101494, -42.40384087725178830, 32.21535556624471042 ) ) ;
#35068=EDGE_CURVE ( 'NONE', #38450, #41408, #30375, .T. ) ;
#35069=CARTESIAN_POINT ( 'NONE',  ( 7.567941867304905479, -42.51145833381128369, 27.28240155936039812 ) ) ;
#35070=CARTESIAN_POINT ( 'NONE',  ( 4.257384923554909051, -52.75000000000000000, 29.19375250200204164 ) ) ;
#35080=CARTESIAN_POINT ( 'NONE',  ( 4.257384923554909051, -52.75000000000000000, 32.69375250200203453 ) ) ;
#35091=CARTESIAN_POINT ( 'NONE',  ( 4.257387320252103535, -45.81875005579910720, 25.69375250200286587 ) ) ;
#35092=FACE_OUTER_BOUND ( 'NONE', #10842, .T. ) ;
#35097=CARTESIAN_POINT ( 'NONE',  ( 2.507384923554909495, -42.41666666666665719, 32.22484141524756751 ) ) ;
#35099=CARTESIAN_POINT ( 'NONE',  ( 4.365830480168198413, -49.32133042246917398, 25.69519247950255192 ) ) ;
#35103=CARTESIAN_POINT ( 'NONE',  ( 7.567941867304902814, -44.68229166714461087, 31.10510344464368870 ) ) ;
#35104=CARTESIAN_POINT ( 'NONE',  ( 0.9468279798049125118, -43.80312500047794799, 29.19375250200204164 ) ) ;
#35107=ORIENTED_EDGE ( 'NONE', *, *, #4201, .T. ) ;
#35111=CARTESIAN_POINT ( 'NONE',  ( 7.583238789974591221, -46.91827116733026770, 28.01113066627620896 ) ) ;
#35112=CARTESIAN_POINT ( 'NONE',  ( 0.7573849235549129366, -51.69375000095590877, 29.19375250200204164 ) ) ;
#35113=CARTESIAN_POINT ( 'NONE',  ( 4.257384923554908163, -45.76562500047794657, 33.01645438728532866 ) ) ;
#35115=VERTEX_POINT ( 'NONE', #35794 ) ;
#35140=DIRECTION ( 'NONE',  ( -0.9304521565929098070, -7.336905175921679416E-05, -0.3664133989206526665 ) ) ;
#35147=CARTESIAN_POINT ( 'NONE',  ( 7.315643228361929040, -47.40153320638913215, 27.43109658693729358 ) ) ;
#35149=CARTESIAN_POINT ( 'NONE',  ( 2.507384923554911715, -50.08333333333332860, 26.16266358875650866 ) ) ;
#35155=CARTESIAN_POINT ( 'NONE',  ( 2.602106451679912169, -51.47395833381127517, 26.32672608803957459 ) ) ;
#35161=CARTESIAN_POINT ( 'NONE',  ( 7.757384923554904610, -43.23895833323773985, 27.17302655983835180 ) ) ;
#35162=CARTESIAN_POINT ( 'NONE',  ( 6.007384923554904610, -45.33333333333332149, 32.22484141524757462 ) ) ;
#35164=CARTESIAN_POINT ( 'NONE',  ( 4.230666204590698420, -43.81811390707072462, 25.69383968087121417 ) ) ;
#35166=CARTESIAN_POINT ( 'NONE',  ( 2.602106451679909505, -48.71979166714461229, 32.06077891596451224 ) ) ;
#35192=CARTESIAN_POINT ( 'NONE',  ( 6.007384923554907274, -49.66666666666665719, 26.16266358875650866 ) ) ;
#35199=CARTESIAN_POINT ( 'NONE',  ( 7.567941867304904591, -47.14062500047794657, 29.19375250200204164 ) ) ;
#35205=CARTESIAN_POINT ( 'NONE',  ( 4.257384923554909051, -49.42812500047794799, 25.37105061671875106 ) ) ;
#35210=ORIENTED_EDGE ( 'NONE', *, *, #32604, .F. ) ;
#35212=ORIENTED_EDGE ( 'NONE', *, *, #5555, .F. ) ;
#35213=CARTESIAN_POINT ( 'NONE',  ( 0.7573849235549129366, -50.53062499990439704, 29.19375250200204164 ) ) ;
#35221=CARTESIAN_POINT ( 'NONE',  ( 6.007384923554904610, -45.52708333428923737, 32.22484141524757462 ) ) ;
#35239=CARTESIAN_POINT ( 'NONE',  ( 4.257443491160582738, -48.81875139542229647, 25.69375250249206744 ) ) ;
#35243=DIRECTION ( 'NONE',  ( -0.000000000000000000, -1.000000000000000000, -0.000000000000000000 ) ) ;
#35250=CARTESIAN_POINT ( 'NONE',  ( 4.037187617231746017, -48.31388150381858537, 25.69895137907446170 ) ) ;
#35253=CARTESIAN_POINT ( 'NONE',  ( 3.352527606997028009, -46.29715949474996251, 25.80500581153880901 ) ) ;
#35254=CARTESIAN_POINT ( 'NONE',  ( 0.9468279798049134000, -46.84479166714461940, 27.28240155936039457 ) ) ;
#35264=CARTESIAN_POINT ( 'NONE',  ( 7.793954306294632595, -47.94835252463290232, 29.32910464497915370 ) ) ;
#35279=ORIENTED_EDGE ( 'NONE', *, *, #2802, .F. ) ;
#35297=CARTESIAN_POINT ( 'NONE',  ( 7.421832352517290232, -45.40891969023569885, 27.69830307752114962 ) ) ;
#35301=DIRECTION ( 'NONE',  ( -0.8956692225370904703, 0.000000000000000000, -0.4447208605404110449 ) ) ;
#35302=EDGE_CURVE ( 'NONE', #6132, #7185, #40378, .T. ) ;
#35309=EDGE_CURVE ( 'NONE', #41408, #30506, #29240, .T. ) ;
#35312=CARTESIAN_POINT ( 'NONE',  ( 7.567941867304904591, -43.59895833381127517, 27.28240155936039812 ) ) ;
#35313=CARTESIAN_POINT ( 'NONE',  ( 0.9468279798049117346, -45.76145833381128369, 31.10510344464368515 ) ) ;
#35319=CIRCLE ( 'NONE', #8813, 3.499999999999996003 ) ;
#35322=CARTESIAN_POINT ( 'NONE',  ( 4.257384923554909051, -51.31875000095590167, 25.15230061767466552 ) ) ;
#35323=CARTESIAN_POINT ( 'NONE',  ( 5.912663395429907709, -46.05729166714461797, 26.32672608803957459 ) ) ;
#35358=CARTESIAN_POINT ( 'NONE',  ( 4.254944989491495022, -47.31869499472690421, 25.69375248929269517 ) ) ;
#35359=CARTESIAN_POINT ( 'NONE',  ( 4.257384923554909051, -45.12499999999999289, 25.69375250200204519 ) ) ;
#35360=CARTESIAN_POINT ( 'NONE',  ( 7.757384923554904610, -49.70833333333332149, 27.17302655983835180 ) ) ;
#35365=CARTESIAN_POINT ( 'NONE',  ( 6.885009689064624183, -43.38568315324871350, 26.88142593785315881 ) ) ;
#35366=CARTESIAN_POINT ( 'NONE',  ( 7.567941867304904591, -52.09895833381127517, 27.28240155936039812 ) ) ;
#35370=VECTOR ( 'NONE', #29165, 1000.000000000000000 ) ;
#35373=CARTESIAN_POINT ( 'NONE',  ( 0.7573849235549138248, -49.54166666666665719, 27.17302655983835180 ) ) ;
#35376=CARTESIAN_POINT ( 'NONE',  ( 6.682445546082279364, -46.50952088477494328, 31.73605054791583413 ) ) ;
#35377=AXIS2_PLACEMENT_3D ( 'NONE', #32859, #32649, #7134 ) ;
#35379=CARTESIAN_POINT ( 'NONE',  ( 4.257384923554908163, -48.17812500047794799, 33.01645438728532866 ) ) ;
#35415=CARTESIAN_POINT ( 'NONE',  ( 2.602106451679909505, -48.80729166714461087, 32.06077891596451224 ) ) ;
#35420=CARTESIAN_POINT ( 'NONE',  ( 0.9468279798049134000, -49.84479166714460519, 27.28240155936039102 ) ) ;
#35427=CARTESIAN_POINT ( 'NONE',  ( 4.257384923554908163, -48.90562499990439704, 33.23520438632941421 ) ) ;
#35434=CARTESIAN_POINT ( 'NONE',  ( 0.7573849235549138248, -47.73541666762256597, 27.17302655983835180 ) ) ;
#35451=CARTESIAN_POINT ( 'NONE',  ( 1.206093040196101862, -51.65384531282380465, 30.96844000906150640 ) ) ;
#35453=CARTESIAN_POINT ( 'NONE',  ( 4.257403298629887978, -44.81875042683200405, 25.69375250205027683 ) ) ;
#35468=CARTESIAN_POINT ( 'NONE',  ( 0.7724060611602301396, -46.18687804144114040, 29.51837255232013391 ) ) ;
#35469=CARTESIAN_POINT ( 'NONE',  ( 0.9468279798049115126, -46.26145833381128369, 31.10510344464368515 ) ) ;
#35490=CARTESIAN_POINT ( 'NONE',  ( 4.136155496112086993, -50.81608724235463370, 25.69555478825351713 ) ) ;
#35497=ADVANCED_FACE ( 'NONE', ( #8332 ), #18536, .T. ) ;
#35512=AXIS2_PLACEMENT_3D ( 'NONE', #24120, #13897, #11138 ) ;
#35519=CARTESIAN_POINT ( 'NONE',  ( 4.257384923554909939, -42.40485061181025372, 24.19375250200203453 ) ) ;
#35527=CARTESIAN_POINT ( 'NONE',  ( 2.815360438258911024, -42.30192363818446921, 32.18390116252165711 ) ) ;
#35528=CARTESIAN_POINT ( 'NONE',  ( 7.567941867304902814, -45.59479166714460519, 31.10510344464368870 ) ) ;
#35533=CARTESIAN_POINT ( 'NONE',  ( 5.153033967715066943, -46.84000311361305080, 25.80093935396179106 ) ) ;
#35535=CARTESIAN_POINT ( 'NONE',  ( 4.257384923554909051, -46.01562500047794657, 25.37105061671875106 ) ) ;
#35538=DIRECTION ( 'NONE',  ( -0.000000000000000000, -1.000000000000000000, -0.000000000000000000 ) ) ;
#35567=CARTESIAN_POINT ( 'NONE',  ( 0.9468279798049134000, -50.34479166714461229, 27.28240155936039457 ) ) ;
#35568=CARTESIAN_POINT ( 'NONE',  ( 7.315634259221303282, -47.48463200227685377, 30.95642397868804352 ) ) ;
#35571=CARTESIAN_POINT ( 'NONE',  ( 4.257384923554909051, -49.12499999999997868, 25.15230061767466552 ) ) ;
#35577=CARTESIAN_POINT ( 'NONE',  ( 6.928826966835949008, -43.38725845226926481, 26.93243026423213138 ) ) ;
#35578=CARTESIAN_POINT ( 'NONE',  ( 7.759609236289341183, -50.45305226777395546, 29.63307212121470258 ) ) ;
#35584=EDGE_LOOP ( 'NONE', ( #31430, #14976, #18327, #7067 ) ) ;
#35586=CARTESIAN_POINT ( 'NONE',  ( 4.257384923554908163, -51.37499999999999289, 33.23520438632941421 ) ) ;
#35592=LINE ( 'NONE', #19424, #32638 ) ;
#35594=ADVANCED_FACE ( 'NONE', ( #8126 ), #14929, .F. ) ;
#35595=CARTESIAN_POINT ( 'NONE',  ( 0.7724106439088681553, -48.68687697413623283, 29.51842172147032173 ) ) ;
#35602=CARTESIAN_POINT ( 'NONE',  ( 4.257384923554909051, -43.12499999999999289, 25.69375250200204519 ) ) ;
#35610=CARTESIAN_POINT ( 'NONE',  ( 2.301907257965456477, -44.11584960288523405, 32.14355117958316299 ) ) ;
#35627=CARTESIAN_POINT ( 'NONE',  ( 5.912663395429904156, -49.22395833381128227, 32.06077891596451224 ) ) ;
#35632=CARTESIAN_POINT ( 'NONE',  ( 2.602106451679911281, -49.88645833381128369, 26.32672608803957459 ) ) ;
#35639=ORIENTED_EDGE ( 'NONE', *, *, #26030, .T. ) ;
#35640=CARTESIAN_POINT ( 'NONE',  ( 7.757384923554905498, -48.78062499990439704, 29.19375250200204164 ) ) ;
#35642=VERTEX_POINT ( 'NONE', #41088 ) ;
#35647=CARTESIAN_POINT ( 'NONE',  ( 6.007384923554904610, -44.02708333428924448, 32.22484141524757462 ) ) ;
#35649=EDGE_CURVE ( 'NONE', #5244, #34914, #34282, .T. ) ;
#35651=FACE_OUTER_BOUND ( 'NONE', #16241, .T. ) ;
#35664=CARTESIAN_POINT ( 'NONE',  ( 1.021887384784587960, -51.72425290344845905, 27.80507674858692013 ) ) ;
#35674=CARTESIAN_POINT ( 'NONE',  ( 4.257384923554909051, -52.75000000000000000, 32.69375250200203453 ) ) ;
#35684=CARTESIAN_POINT ( 'NONE',  ( 7.567941867304905479, -46.05312500047794799, 29.19375250200204164 ) ) ;
#35688=CARTESIAN_POINT ( 'NONE',  ( 2.507384923554909495, -49.91666666666665719, 32.22484141524756751 ) ) ;
#35701=CARTESIAN_POINT ( 'NONE',  ( 1.642764208070758736, -50.75229895296082105, 26.86491975672425880 ) ) ;
#35720=( BOUNDED_CURVE ( )  B_SPLINE_CURVE ( 1, ( #5501, #34847 ),
 .UNSPECIFIED., .F., .T. ) 
 B_SPLINE_CURVE_WITH_KNOTS ( ( 2, 2 ),
 ( 0.000000000000000000, 1.000000000000000000 ),
 .UNSPECIFIED. ) 
 CURVE ( )  GEOMETRIC_REPRESENTATION_ITEM ( )  RATIONAL_B_SPLINE_CURVE ( ( 0.9666184021816470739, 0.9666184021816470739 ) ) 
 REPRESENTATION_ITEM ( '' )  );
#35725=CARTESIAN_POINT ( 'NONE',  ( 1.090860818190589443, -45.65903362182103820, 30.68488849496016613 ) ) ;
#35733=CARTESIAN_POINT ( 'NONE',  ( 2.848597930937599276, -42.78459229268327135, 25.97873062568895008 ) ) ;
#35737=CARTESIAN_POINT ( 'NONE',  ( 5.912663395429907709, -42.46979166714461940, 26.32672608803957459 ) ) ;
#35745=CARTESIAN_POINT ( 'NONE',  ( 4.257384923554908163, -44.26562500047794657, 33.01645438728532866 ) ) ;
#35747=CYLINDRICAL_SURFACE ( 'NONE', #10604, 3.499999999999996003 ) ;
#35756=ADVANCED_FACE ( 'NONE', ( #22774 ), #6608, .T. ) ;
#35773=CARTESIAN_POINT ( 'NONE',  ( 7.567941867304905479, -51.05312500047794799, 29.19375250200204164 ) ) ;
#35774=CARTESIAN_POINT ( 'NONE',  ( 4.257403086791381241, -47.31875042192206848, 25.69375250204917194 ) ) ;
#35776=DIRECTION ( 'NONE',  ( -0.000000000000000000, -1.000000000000000000, -0.000000000000000000 ) ) ;
#35777=CARTESIAN_POINT ( 'NONE',  ( 2.507384923554909495, -46.91666666666665719, 32.22484141524756751 ) ) ;
#35783=CARTESIAN_POINT ( 'NONE',  ( 0.9468279798049132889, -50.39062500047794657, 29.19375250200204164 ) ) ;
#35788=ADVANCED_FACE ( 'NONE', ( #18751 ), #35747, .T. ) ;
#35790=CARTESIAN_POINT ( 'NONE',  ( 2.507384923554911715, -51.58333333333332149, 26.16266358875650866 ) ) ;
#35791=CARTESIAN_POINT ( 'NONE',  ( 4.257384923554909051, -45.12499999999999289, 25.69375250200204519 ) ) ;
#35793=CARTESIAN_POINT ( 'NONE',  ( 3.115321842959296816, -43.59608592851759568, 32.50322301832370897 ) ) ;
#35794=CARTESIAN_POINT ( 'NONE',  ( 4.257387527570275054, -50.81875003717480155, 25.69375250200301508 ) ) ;
#35800=CARTESIAN_POINT ( 'NONE',  ( 0.7573849235549129366, -51.69375000095590877, 29.19375250200204164 ) ) ;
#35809=EDGE_CURVE ( 'NONE', #40970, #27947, #24203, .T. ) ;
#35813=CARTESIAN_POINT ( 'NONE',  ( 2.507384923554909495, -42.41666666666665719, 32.22484141524756751 ) ) ;
#35815=CARTESIAN_POINT ( 'NONE',  ( 2.732834802411810315, -42.10504881336407124, 32.35500496349436617 ) ) ;
#35825=EDGE_LOOP ( 'NONE', ( #13607, #30248, #37168, #27474 ) ) ;
#35827=CARTESIAN_POINT ( 'NONE',  ( 0.9468279798049124008, -44.34895833381128227, 31.10510344464368515 ) ) ;
#35831=CARTESIAN_POINT ( 'NONE',  ( 5.912663395429907709, -50.96979166714461940, 26.32672608803957459 ) ) ;
#35839=CARTESIAN_POINT ( 'NONE',  ( 6.007384923554904610, -48.36395833323773275, 32.22484141524757462 ) ) ;
#35842=ORIENTED_EDGE ( 'NONE', *, *, #31312, .T. ) ;
#35845=CARTESIAN_POINT ( 'NONE',  ( 4.257384923554908163, -44.56875000095590167, 33.23520438632941421 ) ) ;
#35848=DIRECTION ( 'NONE',  ( -0.000000000000000000, -1.000000000000000000, -0.000000000000000000 ) ) ;
#35869=DIRECTION ( 'NONE',  ( 0.000000000000000000, 0.000000000000000000, -1.000000000000000000 ) ) ;
#35872=PRODUCT_DEFINITION ( 'UNKNOWN', '', #360, #9725 ) ;
#35880=CARTESIAN_POINT ( 'NONE',  ( 5.912663395429907709, -46.46979166714461229, 26.32672608803957459 ) ) ;
#35887=CARTESIAN_POINT ( 'NONE',  ( 4.257384923554919709, -49.37499999999998579, 32.69375250200203453 ) ) ;
#35920=CARTESIAN_POINT ( 'NONE',  ( 7.141116384809826023, -45.39530867958075788, 27.19568708426420756 ) ) ;
#35928=B_SPLINE_CURVE_WITH_KNOTS ( 'NONE', 3,
 ( #18369, #1989, #40910, #31339, #24765, #7967, #20936, #15182, #37729, #8373, #17537, #21353, #34325, #5188, #30503, #4767, #8585, #1584, #27536, #40501, #25392, #22392 ),
 .UNSPECIFIED., .F., .F.,
 ( 4, 2, 2, 2, 2, 2, 2, 2, 2, 2, 4 ),
 ( 0.7411064645029117326, 0.7431914339988144880, 0.7452764034947172433, 0.7473613729906199987, 0.7494463424865227541, 0.7536162814783282649, 0.7577862204701337756, 0.7619561594619392864, 0.7661260984537447971, 0.7702960374455503079, 0.7744659764373558186 ),
 .UNSPECIFIED. ) ;
#35932=ORIENTED_EDGE ( 'NONE', *, *, #14574, .F. ) ;
#35935=ORIENTED_EDGE ( 'NONE', *, *, #10851, .T. ) ;
#35940=CIRCLE ( 'NONE', #41394, 10.16127960363519200 ) ;
#35942=CARTESIAN_POINT ( 'NONE',  ( 7.567941867304902814, -42.68229166714461797, 31.10510344464368870 ) ) ;
#35949=CARTESIAN_POINT ( 'NONE',  ( 7.374923099282485239, -45.98051806613123915, 30.84718824629389999 ) ) ;
#35973=CARTESIAN_POINT ( 'NONE',  ( 0.9468279798049125118, -51.80312500047794799, 29.19375250200204164 ) ) ;
#35974=CARTESIAN_POINT ( 'NONE',  ( 1.870583340620199264, -47.26031568512630088, 26.58628413181216388 ) ) ;
#35977=CARTESIAN_POINT ( 'NONE',  ( 4.257384923554908163, -47.87499999999999289, 33.23520438632941421 ) ) ;
#35981=CARTESIAN_POINT ( 'NONE',  ( 4.686746240094798566, -43.32811266212801371, 25.71852251062355066 ) ) ;
#35982=CARTESIAN_POINT ( 'NONE',  ( 0.9468279798049124008, -48.34895833381128227, 31.10510344464368515 ) ) ;
#35990=CARTESIAN_POINT ( 'NONE',  ( 4.257384923554909051, -49.62499999999998579, 25.15230061767466552 ) ) ;
#35994=CARTESIAN_POINT ( 'NONE',  ( 4.466504575671382149, -46.32372902637065692, 25.69375709167842459 ) ) ;
#36001=CARTESIAN_POINT ( 'NONE',  ( 6.007384923554904610, -51.02708333428923737, 32.22484141524757462 ) ) ;
#36017=CARTESIAN_POINT ( 'NONE',  ( 4.257384923554909051, -52.75000000000000000, 32.69375250200203453 ) ) ;
#36019=CARTESIAN_POINT ( 'NONE',  ( 0.7573849235549129366, -42.69375000095590167, 29.19375250200204164 ) ) ;
#36031=CARTESIAN_POINT ( 'NONE',  ( 0.9468279798049132889, -45.39062500047794657, 29.19375250200204164 ) ) ;
#36035=CARTESIAN_POINT ( 'NONE',  ( 0.9468279798049117346, -49.76145833381129080, 31.10510344464368515 ) ) ;
#36040=CARTESIAN_POINT ( 'NONE',  ( 0.7573849235549129366, -49.03062499990439704, 29.19375250200204164 ) ) ;
#36047=CARTESIAN_POINT ( 'NONE',  ( 2.507384923554911715, -44.77708333428923737, 26.16266358875650866 ) ) ;
#36048=CARTESIAN_POINT ( 'NONE',  ( 4.257384923554909051, -43.31875000095590877, 25.15230061767466552 ) ) ;
#36054=CARTESIAN_POINT ( 'NONE',  ( 0.7573849235549120484, -42.95833333333332149, 31.21447844416572792 ) ) ;
#36056=AXIS2_PLACEMENT_3D ( 'NONE', #1742, #34479, #24095 ) ;
#36066=ADVANCED_FACE ( 'NONE', ( #26385 ), #20803, .T. ) ;
#36087=( BOUNDED_CURVE ( )  B_SPLINE_CURVE ( 2, ( #12758, #38704, #28285, #28698, #8930, #3189, #38277, #22750, #42115 ),
 .UNSPECIFIED., .F., .F. ) 
 B_SPLINE_CURVE_WITH_KNOTS ( ( 3, 2, 2, 2, 3 ),
 ( 0.1125000000000000028, 0.1166666666666666685, 0.1250000000000000000, 0.1333333333333333315, 0.1375000000000000111 ),
 .UNSPECIFIED. ) 
 CURVE ( )  GEOMETRIC_REPRESENTATION_ITEM ( )  RATIONAL_B_SPLINE_CURVE ( ( 0.9330127018922194093, 0.9330127018922194093, 1.000000000000000000, 0.8660254037844387076, 1.000000000000000000, 0.8660254037844387076, 1.000000000000000000, 0.9330127018922191873, 0.9330127018922194093 ) ) 
 REPRESENTATION_ITEM ( '' )  );
#36088=CARTESIAN_POINT ( 'NONE',  ( 5.912663395429907709, -44.46979166714461940, 26.32672608803957459 ) ) ;
#36089=CARTESIAN_POINT ( 'NONE',  ( 4.257384923554909051, -52.75000000000000000, 29.19375250200204164 ) ) ;
#36096=CARTESIAN_POINT ( 'NONE',  ( 5.939179107072726005, -42.40493028696902655, 26.12131136397108122 ) ) ;
#36105=CARTESIAN_POINT ( 'NONE',  ( 2.954307522837973821, -50.59977588314119146, 32.44214854978327622 ) ) ;
#36106=CARTESIAN_POINT ( 'NONE',  ( 4.257384923554908163, -51.06875000095590167, 33.23520438632941421 ) ) ;
#36137=DIRECTION ( 'NONE',  ( 0.000000000000000000, 0.000000000000000000, -1.000000000000000000 ) ) ;
#36141=EDGE_LOOP ( 'NONE', ( #9483, #35210, #36944, #39974 ) ) ;
#36143=CARTESIAN_POINT ( 'NONE',  ( 2.602106451679911281, -43.38645833381128369, 26.32672608803957459 ) ) ;
#36147=ORIENTED_EDGE ( 'NONE', *, *, #24668, .F. ) ;
#36150=CARTESIAN_POINT ( 'NONE',  ( 7.567941867304904591, -49.59479166714461940, 31.10510344464368870 ) ) ;
#36158=ORIENTED_EDGE ( 'NONE', *, *, #34173, .T. ) ;
#36166=CARTESIAN_POINT ( 'NONE',  ( 4.257384923554931255, -45.87499999999999289, 32.69375250200203453 ) ) ;
#36174=CARTESIAN_POINT ( 'NONE',  ( 0.7573849235549120484, -47.45833333333331439, 31.21447844416572792 ) ) ;
#36184=CARTESIAN_POINT ( 'NONE',  ( 7.757384923554902834, -46.79166666666665009, 31.21447844416572792 ) ) ;
#36189=ORIENTED_EDGE ( 'NONE', *, *, #37687, .T. ) ;
#36191=CARTESIAN_POINT ( 'NONE',  ( 7.567941867304904591, -50.09895833381128227, 27.28240155936039812 ) ) ;
#36198=CARTESIAN_POINT ( 'NONE',  ( 7.757384923554904610, -51.20833333333332149, 27.17302655983835180 ) ) ;
#36200=CARTESIAN_POINT ( 'NONE',  ( 7.567941867304902814, -51.68229166714461797, 31.10510344464368870 ) ) ;
#36202=CARTESIAN_POINT ( 'NONE',  ( 6.125453936774286845, -46.36454606508638676, 26.21522882242696539 ) ) ;
#36210=CARTESIAN_POINT ( 'NONE',  ( 4.257384923554908163, -51.06875000095590167, 33.23520438632941421 ) ) ;
#36225=CARTESIAN_POINT ( 'NONE',  ( 4.257403298629887978, -44.81875042683200405, 25.69375250205027683 ) ) ;
#36228=CARTESIAN_POINT ( 'NONE',  ( 7.757384923554905498, -42.44375000095590167, 29.19375250200204164 ) ) ;
#36237=VERTEX_POINT ( 'NONE', #15257 ) ;
#36240=CARTESIAN_POINT ( 'NONE',  ( 7.567941867304902814, -45.68229166714462508, 31.10510344464368870 ) ) ;
#36245=CARTESIAN_POINT ( 'NONE',  ( 7.567941867304905479, -47.01145833381128369, 27.28240155936039457 ) ) ;
#36252=CARTESIAN_POINT ( 'NONE',  ( 4.257384923554908163, -47.40562499990440415, 33.23520438632941421 ) ) ;
#36258=CARTESIAN_POINT ( 'NONE',  ( 4.257384923554913492, -50.87499999999999289, 32.69375250200203453 ) ) ;
#36260=CARTESIAN_POINT ( 'NONE',  ( 7.757384923554902834, -44.48541666762257307, 31.21447844416572792 ) ) ;
#36261=CARTESIAN_POINT ( 'NONE',  ( 0.7573849235549138248, -43.23541666762256597, 27.17302655983835180 ) ) ;
#36270=VECTOR ( 'NONE', #15704, 1000.000000000000000 ) ;
#36277=FACE_OUTER_BOUND ( 'NONE', #14614, .T. ) ;
#36301=CARTESIAN_POINT ( 'NONE',  ( 2.602106451679909505, -42.71979166714461940, 32.06077891596451224 ) ) ;
#36310=CARTESIAN_POINT ( 'NONE',  ( 5.570482214165196844, -42.40564318603090044, 25.94644527578753568 ) ) ;
#36316=CYLINDRICAL_SURFACE ( 'NONE', #10349, 3.499999999999996003 ) ;
#36320=VERTEX_POINT ( 'NONE', #28631 ) ;
#36321=CARTESIAN_POINT ( 'NONE',  ( 3.914940514142779104, -50.81120769890308964, 25.70989993530573514 ) ) ;
#36323=CARTESIAN_POINT ( 'NONE',  ( 4.257384923554908163, -42.87499999999998579, 33.23520438632941421 ) ) ;
#36328=LINE ( 'NONE', #23144, #37019 ) ;
#36349=CARTESIAN_POINT ( 'NONE',  ( 7.628043933517778541, -42.40485061181026083, 28.07568509841475546 ) ) ;
#36350=ADVANCED_FACE ( 'NONE', ( #21414 ), #25037, .T. ) ;
#36366=CARTESIAN_POINT ( 'NONE',  ( 4.257384923554909051, -42.92812500047794799, 25.37105061671875106 ) ) ;
#36373=CARTESIAN_POINT ( 'NONE',  ( 7.567941867304905479, -45.01145833381127659, 27.28240155936039812 ) ) ;
#36377=CARTESIAN_POINT ( 'NONE',  ( 0.7573849235549129366, -46.99999999999999289, 29.19375250200204164 ) ) ;
#36396=CARTESIAN_POINT ( 'NONE',  ( 4.257384923554907274, -47.37499999999997868, 32.69375250200203453 ) ) ;
#36404=CARTESIAN_POINT ( 'NONE',  ( 0.9468279798049115126, -51.26145833381129080, 31.10510344464368515 ) ) ;
#36408=CARTESIAN_POINT ( 'NONE',  ( 0.7573849235549120484, -46.45833333333332149, 31.21447844416572792 ) ) ;
#36411=CARTESIAN_POINT ( 'NONE',  ( 1.912347250484089045, -49.12514338919282864, 31.86328731366423028 ) ) ;
#36415=CARTESIAN_POINT ( 'NONE',  ( 0.9468279798049132889, -49.89062500047794657, 29.19375250200204164 ) ) ;
#36421=CARTESIAN_POINT ( 'NONE',  ( 4.022337185794650161, -51.07321660178499911, 32.69375252158948797 ) ) ;
#36423=CARTESIAN_POINT ( 'NONE',  ( 0.7573849235549129366, -48.49999999999998579, 29.19375250200204164 ) ) ;
#36424=CARTESIAN_POINT ( 'NONE',  ( 2.602106451679909505, -51.30729166714461797, 32.06077891596451224 ) ) ;
#36426=DIRECTION ( 'NONE',  ( 0.000000000000000000, 0.000000000000000000, -1.000000000000000000 ) ) ;
#36427=CARTESIAN_POINT ( 'NONE',  ( 2.507384923554909495, -43.41666666666665719, 32.22484141524756751 ) ) ;
#36433=CARTESIAN_POINT ( 'NONE',  ( 6.007384923554904610, -49.02708333428924448, 32.22484141524757462 ) ) ;
#36438=EDGE_CURVE ( 'NONE', #42017, #5487, #34718, .T. ) ;
#36447=CARTESIAN_POINT ( 'NONE',  ( 1.870581894489232289, -44.76031558984450953, 26.58628540082867175 ) ) ;
#36449=CARTESIAN_POINT ( 'NONE',  ( 7.757384923554902834, -42.98541666762257307, 31.21447844416572792 ) ) ;
#36461=CARTESIAN_POINT ( 'NONE',  ( 5.912663395429904156, -44.72395833381127517, 32.06077891596451224 ) ) ;
#36465=CARTESIAN_POINT ( 'NONE',  ( 7.567941867304902814, -47.59479166714461940, 31.10510344464368870 ) ) ;
#36469=ORIENTED_EDGE ( 'NONE', *, *, #38523, .T. ) ;
#36471=ORIENTED_EDGE ( 'NONE', *, *, #23828, .T. ) ;
#36472=CARTESIAN_POINT ( 'NONE',  ( 2.507384923554911715, -46.61395833323773275, 26.16266358875650866 ) ) ;
#36478=CARTESIAN_POINT ( 'NONE',  ( 4.257384923554908163, -44.56875000095590167, 33.23520438632941421 ) ) ;
#36503=ADVANCED_FACE ( 'NONE', ( #35651 ), #39040, .T. ) ;
#36506=LINE ( 'NONE', #24179, #25146 ) ;
#36512=ORIENTED_EDGE ( 'NONE', *, *, #41840, .T. ) ;
#36516=CARTESIAN_POINT ( 'NONE',  ( 4.257384923554909051, -43.42812500047794799, 25.37105061671875461 ) ) ;
#36518=CARTESIAN_POINT ( 'NONE',  ( 7.087979860583421221, -43.99564048638154645, 31.27508303546088797 ) ) ;
#36524=CARTESIAN_POINT ( 'NONE',  ( 5.541042667647866793, -48.53789635396825730, 32.45763764383298167 ) ) ;
#36529=CARTESIAN_POINT ( 'NONE',  ( 1.671638852430305411, -50.25505450884538305, 26.79388609245120989 ) ) ;
#36537=CARTESIAN_POINT ( 'NONE',  ( 2.507384923554909495, -51.11041666762257307, 32.22484141524756751 ) ) ;
#36567=CARTESIAN_POINT ( 'NONE',  ( 7.757384961028803261, -49.95204393943907206, 29.65190111932105310 ) ) ;
#36576=CARTESIAN_POINT ( 'NONE',  ( 4.257384923554908163, -43.67812500047794799, 33.01645438728532866 ) ) ;
#36578=ORIENTED_EDGE ( 'NONE', *, *, #9288, .T. ) ;
#36581=CARTESIAN_POINT ( 'NONE',  ( 7.567941867304905479, -46.05312500047794799, 29.19375250200204164 ) ) ;
#36590=CARTESIAN_POINT ( 'NONE',  ( 4.574051475328506200, -46.06117277321997960, 32.68319779149754822 ) ) ;
#36602=FACE_OUTER_BOUND ( 'NONE', #38042, .T. ) ;
#36611=CARTESIAN_POINT ( 'NONE',  ( 0.7573849235549129366, -47.49999999999999289, 29.19375250200204164 ) ) ;
#36618=CARTESIAN_POINT ( 'NONE',  ( 2.602106451679911281, -47.38645833381128369, 26.32672608803957459 ) ) ;
#36622=CARTESIAN_POINT ( 'NONE',  ( 4.257384923554908163, -46.37499999999999289, 33.23520438632941421 ) ) ;
#36630=CARTESIAN_POINT ( 'NONE',  ( 0.9468279798049143992, -49.43229166714461797, 27.28240155936039812 ) ) ;
#36636=CARTESIAN_POINT ( 'NONE',  ( 2.507384923554909495, -47.41666666666665719, 32.22484141524756751 ) ) ;
#36637=CARTESIAN_POINT ( 'NONE',  ( 4.257384923554908163, -50.76562500047794657, 33.01645438728532866 ) ) ;
#36646=CARTESIAN_POINT ( 'NONE',  ( 2.507384923554909495, -49.61041666762257307, 32.22484141524756751 ) ) ;
#36650=DIRECTION ( 'NONE',  ( 1.000000000000000000, 0.000000000000000000, 0.000000000000000000 ) ) ;
#36658=CARTESIAN_POINT ( 'NONE',  ( 6.020048897627405360, -45.02629908165823736, 32.25200616058559433 ) ) ;
#36662=( NAMED_UNIT ( * ) PLANE_ANGLE_UNIT ( ) SI_UNIT ( $, .RADIAN. ) );
#36674=CARTESIAN_POINT ( 'NONE',  ( 2.602106451679912169, -46.47395833381128227, 26.32672608803957459 ) ) ;
#36679=ORIENTED_EDGE ( 'NONE', *, *, #7756, .F. ) ;
#36683=CARTESIAN_POINT ( 'NONE',  ( 7.757384923554904610, -45.23895833323773275, 27.17302655983835180 ) ) ;
#36690=CARTESIAN_POINT ( 'NONE',  ( 7.757384923554904610, -42.90208333428923737, 27.17302655983835180 ) ) ;
#36691=CARTESIAN_POINT ( 'NONE',  ( 4.257384923554909051, -52.75000000000000000, 25.69375250200204519 ) ) ;
#36716=CARTESIAN_POINT ( 'NONE',  ( 6.862802036380048598, -51.00372451303416454, 31.56725528789729296 ) ) ;
#36723=ORIENTED_EDGE ( 'NONE', *, *, #7384, .T. ) ;
#36728=CARTESIAN_POINT ( 'NONE',  ( 5.912663395429905044, -43.63645833381128369, 32.06077891596451224 ) ) ;
#36736=CARTESIAN_POINT ( 'NONE',  ( 7.134068699747403208, -48.49088158314165753, 31.23766642972787722 ) ) ;
#36741=CARTESIAN_POINT ( 'NONE',  ( 0.8592114759074219732, -50.17509471985675873, 30.04264708290657637 ) ) ;
#36748=CARTESIAN_POINT ( 'NONE',  ( 7.757384923554904610, -49.40208333428924448, 27.17302655983835180 ) ) ;
#36749=CARTESIAN_POINT ( 'NONE',  ( 2.602106451679909505, -43.80729166714461797, 32.06077891596451224 ) ) ;
#36752=CARTESIAN_POINT ( 'NONE',  ( 4.257384923554909051, -52.75000000000000000, 29.19375250200204164 ) ) ;
#36762=CARTESIAN_POINT ( 'NONE',  ( 0.7573849235549129366, -43.99999999999999289, 29.19375250200204164 ) ) ;
#36777=CARTESIAN_POINT ( 'NONE',  ( 3.319562750045980337, -45.60267090063072715, 25.69375250200204519 ) ) ;
#36784=CARTESIAN_POINT ( 'NONE',  ( 6.408298352349073745, -49.86965721751273861, 26.39491848767952575 ) ) ;
#36797=( BOUNDED_CURVE ( )  B_SPLINE_CURVE ( 2, ( #10343, #4165, #40323, #24170, #20124, #14161, #23741, #17569, #27349 ),
 .UNSPECIFIED., .F., .F. ) 
 B_SPLINE_CURVE_WITH_KNOTS ( ( 3, 2, 2, 2, 3 ),
 ( 0.3875000000000000111, 0.3916666666666666630, 0.4000000000000000222, 0.4083333333333333259, 0.4125000000000000333 ),
 .UNSPECIFIED. ) 
 CURVE ( )  GEOMETRIC_REPRESENTATION_ITEM ( )  RATIONAL_B_SPLINE_CURVE ( ( 0.9330127018922194093, 0.9330127018922194093, 1.000000000000000000, 0.8660254037844387076, 1.000000000000000000, 0.8660254037844387076, 1.000000000000000000, 0.9330127018922189652, 0.9330127018922194093 ) ) 
 REPRESENTATION_ITEM ( '' )  );
#36803=CARTESIAN_POINT ( 'NONE',  ( 7.567941867304905479, -45.05312500047794799, 29.19375250200204164 ) ) ;
#36807=CARTESIAN_POINT ( 'NONE',  ( 4.257384923554907274, -46.87499999999997868, 32.69375250200203453 ) ) ;
#36820=CARTESIAN_POINT ( 'NONE',  ( 6.007384923554904610, -45.83333333333332149, 32.22484141524757462 ) ) ;
#36835=CARTESIAN_POINT ( 'NONE',  ( 4.257384923554909051, -47.92812500047795510, 25.37105061671875461 ) ) ;
#36838=CARTESIAN_POINT ( 'NONE',  ( 6.007384923554904610, -44.83333333333332149, 32.22484141524757462 ) ) ;
#36844=EDGE_CURVE ( 'NONE', #35115, #14568, #34979, .T. ) ;
#36845=CARTESIAN_POINT ( 'NONE',  ( 7.567941867304904591, -47.09895833381128938, 27.28240155936039812 ) ) ;
#36853=CARTESIAN_POINT ( 'NONE',  ( 0.7573849235549129366, -46.99999999999999289, 29.19375250200204164 ) ) ;
#36854=CARTESIAN_POINT ( 'NONE',  ( 7.567941867304904591, -49.64062500047794657, 29.19375250200204164 ) ) ;
#36855=ADVANCED_FACE ( 'NONE', ( #11417 ), #16153, .T. ) ;
#36867=CARTESIAN_POINT ( 'NONE',  ( 4.257384923554908163, -49.56875000095590877, 33.23520438632941421 ) ) ;
#36878=CARTESIAN_POINT ( 'NONE',  ( 3.598976344727616183, -44.80382840833893709, 25.75374530160593167 ) ) ;
#36893=CARTESIAN_POINT ( 'NONE',  ( 5.912663395429907709, -42.55729166714461087, 26.32672608803957459 ) ) ;
#36902=CARTESIAN_POINT ( 'NONE',  ( 6.007384923554904610, -44.86395833323773275, 32.22484141524757462 ) ) ;
#36909=CARTESIAN_POINT ( 'NONE',  ( 7.757384923554904610, -44.90208333428923737, 27.17302655983835180 ) ) ;
#36911=VERTEX_POINT ( 'NONE', #7610 ) ;
#36937=CARTESIAN_POINT ( 'NONE',  ( 7.504063396495882721, -50.91374635612697119, 27.88472468092318834 ) ) ;
#36944=ORIENTED_EDGE ( 'NONE', *, *, #41562, .T. ) ;
#36947=CARTESIAN_POINT ( 'NONE',  ( 2.602106451679911281, -42.38645833381128369, 26.32672608803957459 ) ) ;
#36952=B_SPLINE_CURVE_WITH_KNOTS ( 'NONE', 3,
 ( #9855, #38976, #38555, #19820, #16645, #19410, #25802, #29173, #32787, #256, #38767, #9637, #39171, #9422, #22387, #22600, #35577, #3656, #35365, #6227, #32175, #13240, #29603, #10051, #13439, #6441, #35981, #15815, #3039, #3245, #32383, #31959, #13031, #23015, #16232 ),
 .UNSPECIFIED., .F., .F.,
 ( 4, 2, 2, 2, 2, 2, 2, 2, 2, 1, 1, 2, 2, 2, 2, 1, 1, 1, 2, 4 ),
 ( 0.8520872187283060617, 0.8550808667847981104, 0.8580745148412901591, 0.8610681628977822077, 0.8640618109542742564, 0.8670554590107663051, 0.8685522830390123294, 0.8689264890460739466, 0.8690200405478392121, 0.8691135920496045886, 0.8693006950531353416, 0.8700491070672583538, 0.8730427551237501804, 0.8745395791519960937, 0.8752879911661189949, 0.8756621971731805010, 0.8758493001767112540, 0.8759428516784766305, 0.8759896274293593743, 0.8760364031802420071 ),
 .UNSPECIFIED. ) ;
#36956=CARTESIAN_POINT ( 'NONE',  ( 7.644361752814536892, -48.41895917869676680, 28.20315588869974377 ) ) ;
#36970=CARTESIAN_POINT ( 'NONE',  ( 6.007384923554904610, -49.02708333428924448, 32.22484141524757462 ) ) ;
#37000=AXIS2_PLACEMENT_3D ( 'NONE', #37918, #1204, #41323 ) ;
#37003=CARTESIAN_POINT ( 'NONE',  ( 4.715533841176139163, -49.82888893651767859, 25.69375250382983822 ) ) ;
#37011=FACE_OUTER_BOUND ( 'NONE', #41955, .T. ) ;
#37017=CARTESIAN_POINT ( 'NONE',  ( 2.602106451679911281, -46.38645833381128369, 26.32672608803957459 ) ) ;
#37019=VECTOR ( 'NONE', #6769, 1000.000000000000000 ) ;
#37047=CARTESIAN_POINT ( 'NONE',  ( 2.602106451679911281, -48.88645833381128369, 26.32672608803957459 ) ) ;
#37049=EDGE_CURVE ( 'NONE', #19251, #3545, #471, .T. ) ;
#37053=CARTESIAN_POINT ( 'NONE',  ( 4.257384923554908163, -45.37499999999999289, 33.23520438632941421 ) ) ;
#37054=VERTEX_POINT ( 'NONE', #5035 ) ;
#37056=CARTESIAN_POINT ( 'NONE',  ( 7.663548253397883592, -49.46377084265934343, 30.11951710663054982 ) ) ;
#37057=ADVANCED_FACE ( 'NONE', ( #24615 ), #5878, .T. ) ;
#37061=CARTESIAN_POINT ( 'NONE',  ( 4.257384923554909051, -46.62499999999999289, 25.69375250200204519 ) ) ;
#37063=CARTESIAN_POINT ( 'NONE',  ( 7.567941867304904591, -47.64062500047794657, 29.19375250200204164 ) ) ;
#37068=CARTESIAN_POINT ( 'NONE',  ( 2.507384923554911715, -46.58333333333332149, 26.16266358875650866 ) ) ;
#37069=CARTESIAN_POINT ( 'NONE',  ( 7.567941867304902814, -49.68229166714461087, 31.10510344464368870 ) ) ;
#37073=CARTESIAN_POINT ( 'NONE',  ( 1.592463123939933611, -43.13702115886177779, 31.46281179446486931 ) ) ;
#37081=CARTESIAN_POINT ( 'NONE',  ( 2.507384923554911715, -47.27708333428923737, 26.16266358875650866 ) ) ;
#37096=CARTESIAN_POINT ( 'NONE',  ( 0.7579344391105269363, -49.68420864725269581, 29.65642487570301000 ) ) ;
#37110=CARTESIAN_POINT ( 'NONE',  ( 0.9468279798049124008, -43.84895833381127517, 31.10510344464368515 ) ) ;
#37118=CARTESIAN_POINT ( 'NONE',  ( 4.257384923554908163, -44.90562499990439704, 33.23520438632941421 ) ) ;
#37124=CARTESIAN_POINT ( 'NONE',  ( 5.912663395429905044, -50.13645833381128369, 32.06077891596451224 ) ) ;
#37126=VERTEX_POINT ( 'NONE', #2052 ) ;
#37146=ADVANCED_FACE ( 'NONE', ( #28209 ), #5669, .T. ) ;
#37158=CARTESIAN_POINT ( 'NONE',  ( 5.912663395429907709, -50.05729166714461087, 26.32672608803957459 ) ) ;
#37168=ORIENTED_EDGE ( 'NONE', *, *, #29294, .T. ) ;
#37171=ORIENTED_EDGE ( 'NONE', *, *, #10638, .T. ) ;
#37175=CARTESIAN_POINT ( 'NONE',  ( 7.757384923554902834, -49.48541666762258018, 31.21447844416572792 ) ) ;
#37176=CARTESIAN_POINT ( 'NONE',  ( 0.9468279798049124008, -43.84895833381127517, 31.10510344464368515 ) ) ;
#37218=CARTESIAN_POINT ( 'NONE',  ( 2.602106451679909505, -45.21979166714461940, 32.06077891596451224 ) ) ;
#37221=ORIENTED_EDGE ( 'NONE', *, *, #2785, .F. ) ;
#37232=CARTESIAN_POINT ( 'NONE',  ( 1.705040971581427867, -46.13422715291972764, 31.62935232558720955 ) ) ;
#37249=CARTESIAN_POINT ( 'NONE',  ( 4.257384923554908163, -49.17812500047794799, 33.01645438728532866 ) ) ;
#37254=CARTESIAN_POINT ( 'NONE',  ( 7.757384923554902834, -43.79166666666665009, 31.21447844416572792 ) ) ;
#37256=CARTESIAN_POINT ( 'NONE',  ( 7.670865604470772148, -49.42604837679561314, 28.41195237612979696 ) ) ;
#37257=CARTESIAN_POINT ( 'NONE',  ( 0.7327791220173804909, -49.19879223554740122, 28.89884485772776301 ) ) ;
#37260=CARTESIAN_POINT ( 'NONE',  ( 5.912663395429907709, -46.05729166714461797, 26.32672608803957459 ) ) ;
#37261=CARTESIAN_POINT ( 'NONE',  ( 0.9468279798049117346, -47.26145833381128369, 31.10510344464368515 ) ) ;
#37264=CARTESIAN_POINT ( 'NONE',  ( 4.257384923554909051, 7.250000000000000000, 29.19375250200204164 ) ) ;
#37265=VECTOR ( 'NONE', #9591, 1000.000000000000000 ) ;
#37266=DIRECTION ( 'NONE',  ( 0.000000000000000000, 0.000000000000000000, -1.000000000000000000 ) ) ;
#37269=CARTESIAN_POINT ( 'NONE',  ( 4.257384923554909051, -46.12500000000000000, 25.15230061767466552 ) ) ;
#37270=CARTESIAN_POINT ( 'NONE',  ( 5.912663395429904156, -46.72395833381128227, 32.06077891596451224 ) ) ;
#37281=CARTESIAN_POINT ( 'NONE',  ( 6.007384923554907274, -47.86041666762257307, 26.16266358875650866 ) ) ;
#37296=CARTESIAN_POINT ( 'NONE',  ( 2.493484937676813118, -49.77792817957660532, 26.13615928864685145 ) ) ;
#37310=CARTESIAN_POINT ( 'NONE',  ( 4.717251901728550578, -50.55966189288677981, 32.69375261137668787 ) ) ;
#37317=CARTESIAN_POINT ( 'NONE',  ( 7.757384923554905498, -45.28062499990440415, 29.19375250200204164 ) ) ;
#37323=CARTESIAN_POINT ( 'NONE',  ( 7.567941867304905479, -51.01145833381128369, 27.28240155936039812 ) ) ;
#37324=CARTESIAN_POINT ( 'NONE',  ( 4.257384923554909051, -52.75000000000000000, 25.69375250200204519 ) ) ;
#37348=CARTESIAN_POINT ( 'NONE',  ( 2.507384923554909495, -49.41666666666665719, 32.22484141524756751 ) ) ;
#37355=CARTESIAN_POINT ( 'NONE',  ( 5.912663395429904156, -50.72395833381128227, 32.06077891596451224 ) ) ;
#37357=CARTESIAN_POINT ( 'NONE',  ( 6.007384923554907274, -47.66666666666665719, 26.16266358875650866 ) ) ;
#37368=CARTESIAN_POINT ( 'NONE',  ( 0.9366001913626449404, -50.16877627293516895, 30.30145963812845622 ) ) ;
#37374=CARTESIAN_POINT ( 'NONE',  ( 6.007384923554907274, -48.86041666762257307, 26.16266358875650866 ) ) ;
#37375=CARTESIAN_POINT ( 'NONE',  ( 5.912663395429904156, -43.22395833381127517, 32.06077891596451224 ) ) ;
#37392=B_SPLINE_CURVE_WITH_KNOTS ( 'NONE', 3,
 ( #28838, #41837, #25668, #31198, #15677, #38002, #8863, #22254, #24836, #28633, #21836, #6088, #35022, #41411, #41621, #15894, #5678, #38630, #21416, #34393, #12260, #5254, #25244, #18857, #18229, #18654, #38208, #31819, #2059, #9072, #15043, #28006, #18438, #22049, #5885 ),
 .UNSPECIFIED., .F., .F.,
 ( 4, 2, 1, 1, 1, 1, 2, 2, 2, 2, 2, 2, 2, 2, 1, 2, 2, 2, 2, 4 ),
 ( 0.5205426778099786489, 0.5205834770922372901, 0.5206242763744959312, 0.5207058749390133245, 0.5208690720680480002, 0.5211954663261172405, 0.5218482548422558320, 0.5231538318745330152, 0.5257649859390873814, 0.5283761400036417477, 0.5309872940681961140, 0.5316400825843347056, 0.5317216811488520989, 0.5318032797133693812, 0.5319664768424040568, 0.5322928711004732971, 0.5335984481327504803, 0.5362096021973048465, 0.5388207562618591018, 0.5414319103264134680 ),
 .UNSPECIFIED. ) ;
#37402=CARTESIAN_POINT ( 'NONE',  ( 3.801772089129318299, -47.80874391804899659, 25.71606448140684975 ) ) ;
#37422=AXIS2_PLACEMENT_3D ( 'NONE', #8435, #21412, #34389 ) ;
#37425=CARTESIAN_POINT ( 'NONE',  ( 0.9468279798049134000, -44.34479166714461940, 27.28240155936039457 ) ) ;
#37426=FACE_BOUND ( 'NONE', #27632, .T. ) ;
#37428=CARTESIAN_POINT ( 'NONE',  ( 7.757384923554905498, -44.74999999999999289, 29.19375250200204164 ) ) ;
#37432=B_SPLINE_CURVE_WITH_KNOTS ( 'NONE', 3,
 ( #38237, #34420, #5279, #28448, #9098, #5489, #18253, #12502, #18465, #31223, #22280, #35253, #31432, #2298, #28033, #6116, #41228, #12070, #6328, #16135, #22487, #3145, #41866, #19303, #12717, #25695, #35468, #38658, #32278, #9526, #20652, #37439, #30637, #37232, #21064, #1296, #40210, #4485, #11477, #8087 ),
 .UNSPECIFIED., .F., .F.,
 ( 4, 2, 1, 1, 1, 1, 2, 2, 2, 2, 2, 2, 1, 1, 2, 2, 1, 1, 2, 2, 2, 2, 2, 4 ),
 ( 0.5713273426949546652, 0.5713525279599025453, 0.5713777132248503143, 0.5714280837547460745, 0.5715288248145373728, 0.5717303069341200805, 0.5721332711732854959, 0.5729391996516162155, 0.5745510566082777659, 0.5777747705216008667, 0.5809984844349239674, 0.5842221983482470682, 0.5846251625874124835, 0.5846755331173081327, 0.5847007183822560128, 0.5847259036472038929, 0.5848266447069951912, 0.5850281268265778989, 0.5858340553049087296, 0.5874459122615703910, 0.5906696261748936028, 0.5938933400882168145, 0.5955051970448784759, 0.5971170540015400263 ),
 .UNSPECIFIED. ) ;
#37439=CARTESIAN_POINT ( 'NONE',  ( 1.014077279007118637, -46.16334402520043056, 30.55300818796811413 ) ) ;
#37455=CARTESIAN_POINT ( 'NONE',  ( 7.567941867304905479, -49.05312500047794799, 29.19375250200204164 ) ) ;
#37460=CARTESIAN_POINT ( 'NONE',  ( 6.007384923554904610, -45.33333333333332149, 32.22484141524757462 ) ) ;
#37462=CARTESIAN_POINT ( 'NONE',  ( 4.257384923554909051, 5.249999999999997335, 29.19375250200204164 ) ) ;
#37466=CARTESIAN_POINT ( 'NONE',  ( 2.602106451679912169, -47.47395833381128227, 26.32672608803957459 ) ) ;
#37467=CARTESIAN_POINT ( 'NONE',  ( 4.257384923554908163, -47.67812500047795510, 33.01645438728532866 ) ) ;
#37473=CARTESIAN_POINT ( 'NONE',  ( 4.257384923554909051, -44.62499999999999289, 25.15230061767466552 ) ) ;
#37474=CARTESIAN_POINT ( 'NONE',  ( 5.912663395429907709, -48.05729166714461087, 26.32672608803957459 ) ) ;
#37475=EDGE_CURVE ( 'NONE', #6697, #36237, #5659, .T. ) ;
#37486=CARTESIAN_POINT ( 'NONE',  ( 6.007384923554907274, -48.36041666762257307, 26.16266358875650866 ) ) ;
#37512=CARTESIAN_POINT ( 'NONE',  ( 7.567941867304902814, -43.68229166714461797, 31.10510344464368870 ) ) ;
#37519=CARTESIAN_POINT ( 'NONE',  ( 6.007384923554904610, -42.86395833323773275, 32.22484141524757462 ) ) ;
#37520=VECTOR ( 'NONE', #2096, 1000.000000000000000 ) ;
#37525=CARTESIAN_POINT ( 'NONE',  ( 7.567941867304905479, -51.51145833381127659, 27.28240155936039812 ) ) ;
#37542=CARTESIAN_POINT ( 'NONE',  ( 5.195207097063846646, -43.35267090063072715, 32.69375250200202743 ) ) ;
#37561=CARTESIAN_POINT ( 'NONE',  ( 5.912663395429904156, -50.22395833381128227, 32.06077891596451224 ) ) ;
#37562=CARTESIAN_POINT ( 'NONE',  ( 4.257384923554909051, -48.62499999999997868, 25.69375250200204519 ) ) ;
#37573=CARTESIAN_POINT ( 'NONE',  ( 0.7573849235549120484, -49.98895833323773985, 31.21447844416572792 ) ) ;
#37577=CARTESIAN_POINT ( 'NONE',  ( 4.257384923554915268, -50.12499999999997868, 25.69375250200204519 ) ) ;
#37579=CARTESIAN_POINT ( 'NONE',  ( 7.757384923554902834, -50.48541666762257307, 31.21447844416572792 ) ) ;
#37603=CARTESIAN_POINT ( 'NONE',  ( 4.257420362424698901, -42.81875084473693249, 25.69375250218146078 ) ) ;
#37607=CARTESIAN_POINT ( 'NONE',  ( 1.465971658858126192, -47.74661632627194052, 27.03306554874084711 ) ) ;
#37608=CARTESIAN_POINT ( 'NONE',  ( 4.257384923554909051, -45.62499999999999289, 25.69375250200204519 ) ) ;
#37611=CARTESIAN_POINT ( 'NONE',  ( 6.007384923554907274, -49.16666666666665719, 26.16266358875650866 ) ) ;
#37629=CARTESIAN_POINT ( 'NONE',  ( 4.257384923554908163, -42.67812500047794799, 33.01645438728532866 ) ) ;
#37630=PLANE ( 'NONE',  #27394 ) ;
#37645=CARTESIAN_POINT ( 'NONE',  ( 5.195207097063836876, -45.64732909936925864, 25.69375250200204519 ) ) ;
#37659=CARTESIAN_POINT ( 'NONE',  ( 2.602106451679911281, -45.88645833381128369, 26.32672608803957459 ) ) ;
#37664=CARTESIAN_POINT ( 'NONE',  ( 4.257384923554909051, -43.62499999999998579, 25.15230061767466552 ) ) ;
#37669=CARTESIAN_POINT ( 'NONE',  ( 0.9468279798049132889, -45.89062500047794657, 29.19375250200204164 ) ) ;
#37670=FACE_OUTER_BOUND ( 'NONE', #17461, .T. ) ;
#37671=CARTESIAN_POINT ( 'NONE',  ( 7.567941867304902814, -48.09479166714461229, 31.10510344464368870 ) ) ;
#37680=CARTESIAN_POINT ( 'NONE',  ( 4.257384923554909051, -45.12499999999998579, 25.15230061767466552 ) ) ;
#37681=CARTESIAN_POINT ( 'NONE',  ( 2.602106451679909505, -49.30729166714461087, 32.06077891596451224 ) ) ;
#37687=EDGE_CURVE ( 'NONE', #8274, #9278, #10010, .T. ) ;
#37688=VERTEX_POINT ( 'NONE', #3642 ) ;
#37693=CARTESIAN_POINT ( 'NONE',  ( 6.007384923554907274, -46.36041666762257307, 26.16266358875650866 ) ) ;
#37695=VECTOR ( 'NONE', #7159, 1000.000000000000114 ) ;
#37705=VECTOR ( 'NONE', #15943, 1000.000000000000000 ) ;
#37726=CARTESIAN_POINT ( 'NONE',  ( 5.176936075254148228, -50.54924767818420150, 32.60196377517807775 ) ) ;
#37729=CARTESIAN_POINT ( 'NONE',  ( 7.311929628570545958, -44.48665692690429552, 30.92825234318554450 ) ) ;
#37732=CARTESIAN_POINT ( 'NONE',  ( 4.257384923554908163, -42.90562499990439704, 33.23520438632941421 ) ) ;
#37738=PRODUCT ( '7 mm Screw', '7 mm Screw', '', ( #16093 ) ) ;
#37739=CARTESIAN_POINT ( 'NONE',  ( 7.567941867304905479, -52.01145833381127659, 27.28240155936039812 ) ) ;
#37761=DIRECTION ( 'NONE',  ( 0.8956692225370903593, 0.000000000000000000, 0.4447208605404113779 ) ) ;
#37764=LINE ( 'NONE', #41589, #694 ) ;
#37771=CARTESIAN_POINT ( 'NONE',  ( 7.567941867304904591, -49.59895833381128227, 27.28240155936039812 ) ) ;
#37774=CARTESIAN_POINT ( 'NONE',  ( 3.354820066221527064, -45.29862951391380221, 25.80446455651959425 ) ) ;
#37782=CARTESIAN_POINT ( 'NONE',  ( 6.007384923554907274, -49.69729166657106845, 26.16266358875650866 ) ) ;
#37789=CARTESIAN_POINT ( 'NONE',  ( 0.7573849235549138248, -47.23541666762257307, 27.17302655983835180 ) ) ;
#37815=CARTESIAN_POINT ( 'NONE',  ( 3.319562750045979005, -45.39732909936924443, 32.69375250200202743 ) ) ;
#37824=DIRECTION ( 'NONE',  ( 0.000000000000000000, 0.000000000000000000, -1.000000000000000000 ) ) ;
#37827=EDGE_CURVE ( 'NONE', #14935, #1417, #23034, .T. ) ;
#37833=ORIENTED_EDGE ( 'NONE', *, *, #42091, .F. ) ;
#37836=CARTESIAN_POINT ( 'NONE',  ( 2.602106451679909505, -43.71979166714461940, 32.06077891596451224 ) ) ;
#37871=CARTESIAN_POINT ( 'NONE',  ( 4.191183503178756098, -42.81717413520259186, 25.69428901987142666 ) ) ;
#37874=CARTESIAN_POINT ( 'NONE',  ( 5.912663395429904156, -42.72395833381127517, 32.06077891596451224 ) ) ;
#37875=CARTESIAN_POINT ( 'NONE',  ( 4.257384923554908163, -45.17812500047794799, 33.01645438728532866 ) ) ;
#37883=LINE ( 'NONE', #11718, #25824 ) ;
#37885=CARTESIAN_POINT ( 'NONE',  ( 2.507384923554911715, -46.08333333333332149, 26.16266358875650866 ) ) ;
#37886=CARTESIAN_POINT ( 'NONE',  ( 0.9468279798049124008, -49.34895833381128938, 31.10510344464368515 ) ) ;
#37887=ORIENTED_EDGE ( 'NONE', *, *, #41562, .F. ) ;
#37891=CARTESIAN_POINT ( 'NONE',  ( 7.567941867304905479, -52.05312500047794799, 29.19375250200204164 ) ) ;
#37898=CARTESIAN_POINT ( 'NONE',  ( 2.507384923554909495, -46.11041666762257307, 32.22484141524756751 ) ) ;
#37902=CARTESIAN_POINT ( 'NONE',  ( 7.757384923554904610, -51.20833333333332149, 27.17302655983835180 ) ) ;
#37918=CARTESIAN_POINT ( 'NONE',  ( 4.257384923554909051, -52.75000000000000000, 29.19375250200204164 ) ) ;
#37924=CARTESIAN_POINT ( 'NONE',  ( 4.257384923554909051, -48.62499999999999289, 25.15230061767466552 ) ) ;
#37930=CARTESIAN_POINT ( 'NONE',  ( 7.063756048411073074, -50.49637539346330328, 31.33519115690853951 ) ) ;
#37936=ORIENTED_EDGE ( 'NONE', *, *, #11821, .T. ) ;
#37938=CARTESIAN_POINT ( 'NONE',  ( 2.732834802411810315, -42.44192381231257372, 32.35500496349436617 ) ) ;
#37940=ORIENTED_EDGE ( 'NONE', *, *, #18856, .T. ) ;
#37942=CARTESIAN_POINT ( 'NONE',  ( 1.079328935762020603, -43.72736660417710652, 27.64954395361888473 ) ) ;
#37943=CARTESIAN_POINT ( 'NONE',  ( 7.757384923554902834, -43.79166666666665009, 31.21447844416572792 ) ) ;
#37944=CARTESIAN_POINT ( 'NONE',  ( 4.257384923554908163, -51.17812500047794799, 33.01645438728532866 ) ) ;
#37946=EDGE_CURVE ( 'NONE', #27430, #6697, #36087, .T. ) ;
#37977=CARTESIAN_POINT ( 'NONE',  ( 0.9468279798049132889, -49.39062500047794657, 29.19375250200204164 ) ) ;
#37980=CARTESIAN_POINT ( 'NONE',  ( 2.117302467936176935, -45.26771865233950365, 26.38651110529186639 ) ) ;
#37982=CARTESIAN_POINT ( 'NONE',  ( 7.757384923554904610, -46.20833333333332149, 27.17302655983835180 ) ) ;
#37984=VERTEX_POINT ( 'NONE', #5952 ) ;
#37988=CARTESIAN_POINT ( 'NONE',  ( 0.7573849235549120484, -51.48895833323773985, 31.21447844416572792 ) ) ;
#37996=CARTESIAN_POINT ( 'NONE',  ( 6.007384923554907274, -47.36041666762257307, 26.16266358875650866 ) ) ;
#37998=EDGE_CURVE ( 'NONE', #8545, #24350, #28385, .T. ) ;
#38000=DIRECTION ( 'NONE',  ( -0.000000000000000000, -1.000000000000000000, -0.000000000000000000 ) ) ;
#38002=CARTESIAN_POINT ( 'NONE',  ( 4.201952389638636376, -46.81743125086732249, 25.69412771569867360 ) ) ;
#38022=CARTESIAN_POINT ( 'NONE',  ( 1.017367647281261611, -48.22421303676531323, 27.86890235949422490 ) ) ;
#38042=EDGE_LOOP ( 'NONE', ( #39281, #7549, #9168, #17185 ) ) ;
#38044=CARTESIAN_POINT ( 'NONE',  ( 5.912663395429905044, -44.13645833381129080, 32.06077891596451224 ) ) ;
#38067=CARTESIAN_POINT ( 'NONE',  ( 5.913623004159759944, -45.52931091633293192, 32.27730627247832729 ) ) ;
#38068=B_SPLINE_CURVE_WITH_KNOTS ( 'NONE', 3,
 ( #17004, #840, #14033, #7864, #23606, #3596, #14237, #10833, #36567, #27216, #7432, #40179, #27005, #36784, #11049, #29545, #37003, #13386 ),
 .UNSPECIFIED., .F., .F.,
 ( 4, 2, 2, 2, 2, 2, 2, 2, 4 ),
 ( 0.1904640372305485552, 0.1936354618204662870, 0.1968068864103840188, 0.1999783110003017228, 0.2031497355902194546, 0.2063211601801371864, 0.2094925847700548904, 0.2126640093599726222, 0.2158354339498903540 ),
 .UNSPECIFIED. ) ;
#38079=CARTESIAN_POINT ( 'NONE',  ( 5.455283715586720206, -49.34750661867284549, 25.89662719505098210 ) ) ;
#38082=CARTESIAN_POINT ( 'NONE',  ( 4.257384923554931255, -44.87499999999998579, 32.69375250200203453 ) ) ;
#38084=CARTESIAN_POINT ( 'NONE',  ( 7.567941867304902814, -44.18229166714461797, 31.10510344464368870 ) ) ;
#38086=CARTESIAN_POINT ( 'NONE',  ( 5.912663395429905044, -45.63645833381128369, 32.06077891596451224 ) ) ;
#38096=CARTESIAN_POINT ( 'NONE',  ( 0.7573849235549120484, -44.95833333333332149, 31.21447844416572792 ) ) ;
#38097=CARTESIAN_POINT ( 'NONE',  ( 4.257384923554909051, -47.01562500047794657, 25.37105061671875106 ) ) ;
#38098=ORIENTED_EDGE ( 'NONE', *, *, #12693, .F. ) ;
#38109=CARTESIAN_POINT ( 'NONE',  ( 0.7573849235549120484, -45.65208333428923737, 31.21447844416572792 ) ) ;
#38116=CARTESIAN_POINT ( 'NONE',  ( 4.257384923554909939, 5.249999999999997335, 39.35503210563723542 ) ) ;
#38133=CARTESIAN_POINT ( 'NONE',  ( 2.507384923554909495, -48.91666666666665719, 32.22484141524756751 ) ) ;
#38138=CARTESIAN_POINT ( 'NONE',  ( 7.567941867304904591, -51.09895833381128227, 27.28240155936039812 ) ) ;
#38142=CARTESIAN_POINT ( 'NONE',  ( 2.787051468684293543, -51.10379658715133644, 32.36996391664733608 ) ) ;
#38143=VECTOR ( 'NONE', #15321, 1000.000000000000114 ) ;
#38147=CARTESIAN_POINT ( 'NONE',  ( 2.507384923554911715, -52.08333333333332149, 26.16266358875650866 ) ) ;
#38151=CARTESIAN_POINT ( 'NONE',  ( 3.950257109403993105, -43.81143971215364274, 25.70671177181144174 ) ) ;
#38153=CARTESIAN_POINT ( 'NONE',  ( 5.912663395429907709, -48.46979166714461229, 26.32672608803957459 ) ) ;
#38182=CARTESIAN_POINT ( 'NONE',  ( 5.912663395429904156, -48.72395833381128227, 32.06077891596451224 ) ) ;
#38186=AXIS2_PLACEMENT_3D ( 'NONE', #5290, #14044, #20630 ) ;
#38195=ORIENTED_EDGE ( 'NONE', *, *, #31748, .T. ) ;
#38196=CARTESIAN_POINT ( 'NONE',  ( 6.007384923554907274, -51.19729166657106845, 26.16266358875650866 ) ) ;
#38199=ORIENTED_EDGE ( 'NONE', *, *, #33223, .T. ) ;
#38202=CARTESIAN_POINT ( 'NONE',  ( 7.484069130855979246, -42.41320705223026977, 27.80601036129686676 ) ) ;
#38203=CARTESIAN_POINT ( 'NONE',  ( 7.757384923554905498, -47.44375000095590877, 29.19375250200204164 ) ) ;
#38208=CARTESIAN_POINT ( 'NONE',  ( 0.7448797157474323916, -46.69208217790951210, 29.24363994474119011 ) ) ;
#38209=VECTOR ( 'NONE', #31860, 1000.000000000000000 ) ;
#38213=MECHANICAL_DESIGN_GEOMETRIC_PRESENTATION_REPRESENTATION('',(#28011),#24625);
#38227=DIRECTION ( 'NONE',  ( 0.000000000000000000, 0.000000000000000000, 1.000000000000000000 ) ) ;
#38234=CARTESIAN_POINT ( 'NONE',  ( 2.060434183766105765, -48.12078017482809855, 31.97561774522484512 ) ) ;
#38237=CARTESIAN_POINT ( 'NONE',  ( 4.257461754300457812, -46.31875183025808695, 25.69375250284532441 ) ) ;
#38244=CARTESIAN_POINT ( 'NONE',  ( 5.596898847172711022, -48.03674032505659852, 32.43203318877733921 ) ) ;
#38252=EDGE_LOOP ( 'NONE', ( #23579, #24606, #3878, #8945 ) ) ;
#38254=CARTESIAN_POINT ( 'NONE',  ( 5.912663395429905044, -42.63645833381128369, 32.06077891596451224 ) ) ;
#38255=CARTESIAN_POINT ( 'NONE',  ( 4.257384923554909051, -42.31875000095590167, 25.15230061767466552 ) ) ;
#38272=CARTESIAN_POINT ( 'NONE',  ( 7.781339954851351770, -45.43513624620889146, 28.74636817037490744 ) ) ;
#38277=CARTESIAN_POINT ( 'NONE',  ( 2.507384923554909495, -50.91666666666665719, 32.22484141524756751 ) ) ;
#38287=ORIENTED_EDGE ( 'NONE', *, *, #8851, .F. ) ;
#38288=CARTESIAN_POINT ( 'NONE',  ( 5.912663395429907709, -43.55729166714461797, 26.32672608803957459 ) ) ;
#38289=CARTESIAN_POINT ( 'NONE',  ( 2.602106451679911281, -44.38645833381128369, 26.32672608803957459 ) ) ;
#38299=CARTESIAN_POINT ( 'NONE',  ( 7.685696144974102140, -46.96633562710411525, 30.11657914848785822 ) ) ;
#38300=CARTESIAN_POINT ( 'NONE',  ( 7.757384923554904610, -50.90208333428924448, 27.17302655983835180 ) ) ;
#38301=CARTESIAN_POINT ( 'NONE',  ( 0.9468279798049124008, -45.84895833381128227, 31.10510344464368515 ) ) ;
#38332=FACE_OUTER_BOUND ( 'NONE', #21401, .T. ) ;
#38341=CARTESIAN_POINT ( 'NONE',  ( 6.007384923554904610, -50.33333333333332860, 32.22484141524757462 ) ) ;
#38342=ORIENTED_EDGE ( 'NONE', *, *, #11821, .F. ) ;
#38348=CARTESIAN_POINT ( 'NONE',  ( 4.285912758476878359, -50.31936386396704108, 25.69386149159604571 ) ) ;
#38352=DIRECTION ( 'NONE',  ( -0.000000000000000000, -1.000000000000000000, -0.000000000000000000 ) ) ;
#38356=CARTESIAN_POINT ( 'NONE',  ( 4.257384923554909051, -43.65562499990439704, 25.15230061767466552 ) ) ;
#38358=VERTEX_POINT ( 'NONE', #1472 ) ;
#38360=CARTESIAN_POINT ( 'NONE',  ( 4.257384923554933032, -43.62499999999999289, 25.69375250200204519 ) ) ;
#38361=CARTESIAN_POINT ( 'NONE',  ( 0.9468279798049134000, -48.84479166714461229, 27.28240155936039457 ) ) ;
#38364=CARTESIAN_POINT ( 'NONE',  ( 2.494471097430898787, -48.77575838054858082, 26.13539043739497458 ) ) ;
#38366=FACE_OUTER_BOUND ( 'NONE', #39437, .T. ) ;
#38373=DIRECTION ( 'NONE',  ( 0.000000000000000000, 0.000000000000000000, -1.000000000000000000 ) ) ;
#38383=CARTESIAN_POINT ( 'NONE',  ( 0.7573849235549138248, -42.54166666666665719, 27.17302655983835180 ) ) ;
#38389=CARTESIAN_POINT ( 'NONE',  ( 4.257393643264853367, -45.06839824424229590, 32.69375250198117300 ) ) ;
#38398=CARTESIAN_POINT ( 'NONE',  ( 2.602106451679909505, -47.30729166714461087, 32.06077891596451224 ) ) ;
#38403=CARTESIAN_POINT ( 'NONE',  ( 7.567941867304905479, -52.05312500047794799, 29.19375250200204164 ) ) ;
#38410=CARTESIAN_POINT ( 'NONE',  ( 2.507384923554909495, -50.94729166657106845, 32.22484141524756751 ) ) ;
#38417=CARTESIAN_POINT ( 'NONE',  ( 0.7573849235549120484, -45.65208333428923737, 31.21447844416572792 ) ) ;
#38424=DIRECTION ( 'NONE',  ( 0.06269504844767277707, 0.000000000000000000, 0.9980327303751835855 ) ) ;
#38443=CARTESIAN_POINT ( 'NONE',  ( 5.195207097063836876, -42.64732909936925154, 25.69375250200204519 ) ) ;
#38450=VERTEX_POINT ( 'NONE', #8891 ) ;
#38453=CARTESIAN_POINT ( 'NONE',  ( 5.912663395429905044, -45.13645833381128369, 32.06077891596451224 ) ) ;
#38454=CARTESIAN_POINT ( 'NONE',  ( 4.257384923554909051, -52.75000000000000000, 29.19375250200204164 ) ) ;
#38460=CARTESIAN_POINT ( 'NONE',  ( 7.558579121486621588, -47.91722457245658973, 28.02108744175961519 ) ) ;
#38461=( BOUNDED_CURVE ( )  B_SPLINE_CURVE ( 2, ( #41557, #12410, #22193, #20259, #40034, #33444, #30037, #10903, #13879, #13448, #30252, #36200, #33865, #478, #30461, #23888, #7926, #14095, #909, #16653, #36424, #7072, #10478, #26645, #1332, #23232, #20051, #29825, #4306, #39388, #14303, #39604, #20892, #36637, #26858, #1124, #33014, #3882, #16863, #27282, #17289, #39828, #17072, #27069, #24100, #33225, #4517, #692, #13662, #23459, #20688, #20476, #7501, #7289, #40246, #11115, #10691, #4088, #23674, #37069, #36854, #26434, #7715, #33666, #17499, #29611, #10266, #37886, #37681, #12139, #21926, #8330, #34073, #40866, #30887, #11514, #27685, #2369, #8538, #2150, #28100, #5142, #24507, #18533, #15137, #5559, #17703, #1746, #11720, #34279, #8123, #1943, #21307, #4928, #21100, #14728, #40657, #17909, #37474, #15359, #14519, #18119, #31090, #14925, #41085, #21516, #27892, #11933, #24719, #1537, #34485, #5344, #24300, #18318, #31291, #8744, #24927, #31501, #21720, #34692, #28308, #41292, #25132, #38097, #8952, #4724, #30672, #27490, #40459, #11313, #37270, #41929, #5977, #12777, #32542, #15768, #26183, #25759, #2996, #6393, #41505, #28721, #18745, #38726, #25972, #15989, #35323, #35535, #213, #38515, #22769, #38301, #9167, #35113, #38934, #9596, #22555, #12357, #6605, #3408, #6185, #19370, #41714, #28517, #16193, #31707, #25341, #19161, #32341, #22142, #2575, #9812, #3208, #13194, #10013, #9380, #18952, #28932, #31916, #12569, #25555, #22345, #29344, #29135, #2787, #32130, #10, #19570, #12991, #35745, #16400, #39131, #34903, #5771, #15559, #11419, #4629, #11225, #24208, #37176, #36749, #7612, #39937, #34178, #33341, #27597, #20801, #33563, #8233, #14204, #14829, #30993, #4834, #14000, #37375, #7401, #1850, #17610, #4423, #17191, #21207, #5037, #30573, #40565, #26975, #27181, #27389, #35942, #14626, #30363, #20374, #10801, #23784, #27797, #40361, #8030, #24408, #33976, #30151 ),
 .UNSPECIFIED., .F., .T. ) 
 B_SPLINE_CURVE_WITH_KNOTS ( ( 3, 2, 2, 2, 2, 2, 2, 2, 2, 2, 2, 2, 2, 2, 2, 2, 2, 2, 2, 2, 2, 2, 2, 2, 2, 2, 2, 2, 2, 2, 2, 2, 2, 2, 2, 2, 2, 2, 2, 2, 2, 2, 2, 2, 2, 2, 2, 2, 2, 2, 2, 2, 2, 2, 2, 2, 2, 2, 2, 2, 2, 2, 2, 2, 2, 2, 2, 2, 2, 2, 2, 2, 2, 2, 2, 2, 2, 2, 2, 2, 2, 2, 2, 2, 2, 2, 2, 2, 2, 2, 2, 2, 2, 2, 2, 2, 2, 2, 2, 2, 2, 2, 2, 2, 2, 2, 2, 2, 2, 2, 2, 2, 2, 2, 2, 2, 2, 2, 2, 3 ),
 ( 0.000000000000000000, 0.008333333333333333218, 0.01666666666666666644, 0.02500000000000000139, 0.03333333333333333287, 0.04166666666666666435, 0.05000000000000000278, 0.05833333333333333426, 0.06666666666666666574, 0.07499999999999999722, 0.08333333333333332871, 0.09166666666666666019, 0.1000000000000000056, 0.1083333333333333370, 0.1166666666666666685, 0.1250000000000000000, 0.1333333333333333315, 0.1416666666666666630, 0.1499999999999999944, 0.1583333333333333259, 0.1666666666666666574, 0.1749999999999999889, 0.1833333333333333204, 0.1916666666666666796, 0.2000000000000000111, 0.2083333333333333426, 0.2166666666666666741, 0.2250000000000000056, 0.2333333333333333370, 0.2416666666666666685, 0.2500000000000000000, 0.2583333333333333592, 0.2666666666666666630, 0.2750000000000000222, 0.2833333333333333259, 0.2916666666666666297, 0.2999999999999999889, 0.3083333333333333481, 0.3166666666666666519, 0.3250000000000000111, 0.3333333333333333148, 0.3416666666666666741, 0.3499999999999999778, 0.3583333333333333370, 0.3666666666666666408, 0.3749999999999999445, 0.3833333333333333592, 0.3916666666666666630, 0.4000000000000000222, 0.4083333333333333259, 0.4166666666666666852, 0.4249999999999999889, 0.4333333333333333481, 0.4416666666666666519, 0.4500000000000000111, 0.4583333333333333703, 0.4666666666666666741, 0.4749999999999999778, 0.4833333333333333370, 0.4916666666666666408, 0.5000000000000000000, 0.5083333333333333037, 0.5166666666666667185, 0.5250000000000000222, 0.5333333333333333259, 0.5416666666666666297, 0.5500000000000000444, 0.5583333333333333481, 0.5666666666666666519, 0.5749999999999999556, 0.5833333333333332593, 0.5916666666666666741, 0.5999999999999999778, 0.6083333333333332815, 0.6166666666666666963, 0.6250000000000000000, 0.6333333333333333037, 0.6416666666666667185, 0.6500000000000000222, 0.6583333333333333259, 0.6666666666666666297, 0.6750000000000000444, 0.6833333333333333481, 0.6916666666666666519, 0.6999999999999999556, 0.7083333333333333703, 0.7166666666666666741, 0.7249999999999999778, 0.7333333333333332815, 0.7416666666666666963, 0.7499999999999998890, 0.7583333333333333037, 0.7666666666666667185, 0.7750000000000000222, 0.7833333333333333259, 0.7916666666666666297, 0.8000000000000000444, 0.8083333333333333481, 0.8166666666666666519, 0.8249999999999999556, 0.8333333333333333703, 0.8416666666666666741, 0.8499999999999999778, 0.8583333333333332815, 0.8666666666666666963, 0.8750000000000000000, 0.8833333333333333037, 0.8916666666666667185, 0.9000000000000000222, 0.9083333333333333259, 0.9166666666666667407, 0.9250000000000000444, 0.9333333333333333481, 0.9416666666666666519, 0.9499999999999999556, 0.9583333333333333703, 0.9666666666666666741, 0.9749999999999999778, 0.9833333333333332815, 0.9845488016436891865 ),
 .UNSPECIFIED. ) 
 CURVE ( )  GEOMETRIC_REPRESENTATION_ITEM ( )  RATIONAL_B_SPLINE_CURVE ( ( 1.000000000000000000, 0.8660254037844387076, 1.000000000000000000, 0.8660254037844387076, 1.000000000000000000, 0.8660254037844387076, 1.000000000000000000, 0.8660254037844387076, 1.000000000000000000, 0.8660254037844387076, 1.000000000000000000, 0.8660254037844387076, 1.000000000000000000, 0.8660254037844387076, 1.000000000000000000, 0.8660254037844387076, 1.000000000000000000, 0.8660254037844387076, 1.000000000000000000, 0.8660254037844387076, 1.000000000000000000, 0.8660254037844387076, 1.000000000000000000, 0.8660254037844387076, 1.000000000000000000, 0.8660254037844387076, 1.000000000000000000, 0.8660254037844387076, 1.000000000000000000, 0.8660254037844387076, 1.000000000000000000, 0.8660254037844387076, 1.000000000000000000, 0.8660254037844387076, 1.000000000000000000, 0.8660254037844387076, 1.000000000000000000, 0.8660254037844387076, 1.000000000000000000, 0.8660254037844387076, 1.000000000000000000, 0.8660254037844387076, 1.000000000000000000, 0.8660254037844387076, 1.000000000000000000, 0.8660254037844387076, 1.000000000000000000, 0.8660254037844387076, 1.000000000000000000, 0.8660254037844387076, 1.000000000000000000, 0.8660254037844387076, 1.000000000000000000, 0.8660254037844387076, 1.000000000000000000, 0.8660254037844387076, 1.000000000000000000, 0.8660254037844387076, 1.000000000000000000, 0.8660254037844387076, 1.000000000000000000, 0.8660254037844387076, 1.000000000000000000, 0.8660254037844387076, 1.000000000000000000, 0.8660254037844387076, 1.000000000000000000, 0.8660254037844387076, 1.000000000000000000, 0.8660254037844387076, 1.000000000000000000, 0.8660254037844387076, 1.000000000000000000, 0.8660254037844387076, 1.000000000000000000, 0.8660254037844387076, 1.000000000000000000, 0.8660254037844387076, 1.000000000000000000, 0.8660254037844387076, 1.000000000000000000, 0.8660254037844387076, 1.000000000000000000, 0.8660254037844387076, 1.000000000000000000, 0.8660254037844387076, 1.000000000000000000, 0.8660254037844387076, 1.000000000000000000, 0.8660254037844387076, 1.000000000000000000, 0.8660254037844387076, 1.000000000000000000, 0.8660254037844387076, 1.000000000000000000, 0.8660254037844387076, 1.000000000000000000, 0.8660254037844387076, 1.000000000000000000, 0.8660254037844387076, 1.000000000000000000, 0.8660254037844387076, 1.000000000000000000, 0.8660254037844387076, 1.000000000000000000, 0.8660254037844387076, 1.000000000000000000, 0.8660254037844387076, 1.000000000000000000, 0.8660254037844387076, 1.000000000000000000, 0.8660254037844387076, 1.000000000000000000, 0.8660254037844387076, 1.000000000000000000, 0.8660254037844387076, 1.000000000000000000, 0.8660254037844387076, 1.000000000000000000, 0.8660254037844387076, 1.000000000000000000, 0.8660254037844387076, 1.000000000000000000, 0.8660254037844387076, 1.000000000000000000, 0.8660254037844387076, 1.000000000000000000, 0.8660254037844387076, 1.000000000000000000, 0.8660254037844387076, 1.000000000000000000, 0.8660254037844387076, 1.000000000000000000, 0.8660254037844387076, 1.000000000000000000, 0.8660254037844387076, 1.000000000000000000, 0.8660254037844387076, 1.000000000000000000, 0.8660254037844387076, 1.000000000000000000, 0.8660254037844387076, 1.000000000000000000, 0.8660254037844387076, 1.000000000000000000, 0.8660254037844387076, 1.000000000000000000, 0.8660254037844387076, 1.000000000000000000, 0.8660254037844387076, 1.000000000000000000, 0.8660254037844387076, 1.000000000000000000, 0.8660254037844387076, 1.000000000000000000, 0.8660254037844387076, 1.000000000000000000, 0.8660254037844387076, 1.000000000000000000, 0.8660254037844387076, 1.000000000000000000, 0.8660254037844387076, 1.000000000000000000, 0.8660254037844387076, 1.000000000000000000, 0.8660254037844387076, 1.000000000000000000, 0.8660254037844387076, 1.000000000000000000, 0.8660254037844387076, 1.000000000000000000, 0.8660254037844387076, 1.000000000000000000, 0.8660254037844387076, 1.000000000000000000, 0.8660254037844387076, 1.000000000000000000, 0.8660254037844387076, 1.000000000000000000, 0.8660254037844387076, 1.000000000000000000, 0.8660254037844387076, 1.000000000000000000, 0.8660254037844387076, 1.000000000000000000, 0.8660254037844387076, 1.000000000000000000, 0.8660254037844387076, 1.000000000000000000, 0.8660254037844387076, 1.000000000000000000, 0.8660254037844387076, 1.000000000000000000, 0.8660254037844387076, 1.000000000000000000, 0.8660254037844387076, 1.000000000000000000, 0.8660254037844387076, 1.000000000000000000, 0.8660254037844387076, 1.000000000000000000, 0.8660254037844387076, 1.000000000000000000, 0.8660254037844387076, 1.000000000000000000, 0.8660254037844387076, 1.000000000000000000, 0.8660254037844387076, 1.000000000000000000, 0.8660254037844387076, 1.000000000000000000, 0.8660254037844387076, 1.000000000000000000, 0.8660254037844387076, 1.000000000000000000, 0.8660254037844387076, 1.000000000000000000, 0.8660254037844387076, 1.000000000000000000, 0.8660254037844387076, 1.000000000000000000, 0.8660254037844387076, 1.000000000000000000, 0.8660254037844387076, 1.000000000000000000, 0.8660254037844387076, 1.000000000000000000, 0.8660254037844387076, 1.000000000000000000, 0.8660254037844387076, 1.000000000000000000, 0.8660254037844387076, 1.000000000000000000, 0.8660254037844387076, 1.000000000000000000, 0.8660254037844387076, 1.000000000000000000, 0.9804589748688710138, 0.9666183089694433406 ) ) 
 REPRESENTATION_ITEM ( '' )  );
#38465=CARTESIAN_POINT ( 'NONE',  ( 4.257384923554909051, -52.75000000000000000, 32.69375250200203453 ) ) ;
#38492=CARTESIAN_POINT ( 'NONE',  ( 7.503825773792312859, -45.41357286515077618, 27.87647185644111758 ) ) ;
#38495=CARTESIAN_POINT ( 'NONE',  ( 2.192254113573406382, -45.76691396922733901, 26.33483905265823566 ) ) ;
#38498=DIRECTION ( 'NONE',  ( 8.659560562354904508E-17, 0.7071067811865500152, -0.7071067811865451302 ) ) ;
#38503=CARTESIAN_POINT ( 'NONE',  ( 1.021904544718179819, -42.72425390798291289, 27.80503422411961623 ) ) ;
#38505=CARTESIAN_POINT ( 'NONE',  ( 0.9468279798049124008, -44.34895833381128227, 31.10510344464368515 ) ) ;
#38506=CARTESIAN_POINT ( 'NONE',  ( 0.9468279798049117346, -43.76145833381129080, 31.10510344464368515 ) ) ;
#38514=CARTESIAN_POINT ( 'NONE',  ( 2.507384923554911715, -42.58333333333332149, 26.16266358875650866 ) ) ;
#38515=CARTESIAN_POINT ( 'NONE',  ( 0.9468279798049143992, -45.93229166714461087, 27.28240155936039457 ) ) ;
#38516=VERTEX_POINT ( 'NONE', #18466 ) ;
#38523=EDGE_CURVE ( 'NONE', #34704, #40134, #41229, .T. ) ;
#38528=EDGE_CURVE ( 'NONE', #8428, #11963, #22080, .T. ) ;
#38548=CARTESIAN_POINT ( 'NONE',  ( 4.257384923554909051, -52.75000000000000000, 25.69375250200204519 ) ) ;
#38549=DIRECTION ( 'NONE',  ( 0.000000000000000000, 0.000000000000000000, -1.000000000000000000 ) ) ;
#38550=CARTESIAN_POINT ( 'NONE',  ( 2.507384923554911715, -49.58333333333332860, 26.16266358875650866 ) ) ;
#38555=CARTESIAN_POINT ( 'NONE',  ( 4.972289058208029466, -43.55447854781107253, 32.64208317214530553 ) ) ;
#38556=CARTESIAN_POINT ( 'NONE',  ( 0.9468279798049132889, -51.39062500047794657, 29.19375250200204164 ) ) ;
#38559=CARTESIAN_POINT ( 'NONE',  ( 2.139658747706474351, -51.26608739425359573, 26.37102499356486973 ) ) ;
#38562=CARTESIAN_POINT ( 'NONE',  ( 6.007384923554907274, -49.66666666666665719, 26.16266358875650866 ) ) ;
#38565=ORIENTED_EDGE ( 'NONE', *, *, #37998, .F. ) ;
#38566=CARTESIAN_POINT ( 'NONE',  ( 4.257384923554909051, -41.90485061181026083, 29.19375250200204164 ) ) ;
#38568=CARTESIAN_POINT ( 'NONE',  ( 0.9468279798049125118, -48.30312500047795510, 29.19375250200204164 ) ) ;
#38572=CARTESIAN_POINT ( 'NONE',  ( 1.448194491253642857, -48.74407861578495016, 27.05509188727943837 ) ) ;
#38605=CARTESIAN_POINT ( 'NONE',  ( 0.9468279798049132889, -47.39062500047794657, 29.19375250200204164 ) ) ;
#38606=CARTESIAN_POINT ( 'NONE',  ( 4.257384923554909939, -42.40485061181025372, 23.69375250200204519 ) ) ;
#38611=CARTESIAN_POINT ( 'NONE',  ( 7.567941867304905479, -49.05312500047794799, 29.19375250200204164 ) ) ;
#38617=CARTESIAN_POINT ( 'NONE',  ( 7.757384923554905498, -49.28062499990439704, 29.19375250200204164 ) ) ;
#38625=CARTESIAN_POINT ( 'NONE',  ( 6.007384923554907274, -47.86041666762257307, 26.16266358875650866 ) ) ;
#38627=EDGE_LOOP ( 'NONE', ( #8032, #3711, #41321, #11002 ) ) ;
#38628=CARTESIAN_POINT ( 'NONE',  ( 4.257384923554909051, -52.75000000000000000, 29.19375250200204164 ) ) ;
#38630=CARTESIAN_POINT ( 'NONE',  ( 0.8808784705192040931, -46.71430397141623558, 28.26421586738624114 ) ) ;
#38640=CARTESIAN_POINT ( 'NONE',  ( 1.765687707437911369, -51.75448822846161789, 26.69348292462718675 ) ) ;
#38654=CYLINDRICAL_SURFACE ( 'NONE', #25128, 3.499999999999996003 ) ;
#38655=CARTESIAN_POINT ( 'NONE',  ( 1.132196512511900233, -48.15678375161897407, 30.77036606214074510 ) ) ;
#38658=CARTESIAN_POINT ( 'NONE',  ( 0.7811651842903489795, -46.18493214757014442, 29.60796884365009518 ) ) ;
#38660=CARTESIAN_POINT ( 'NONE',  ( 0.9468279798049115126, -45.76145833381128369, 31.10510344464368515 ) ) ;
#38662=DIRECTION ( 'NONE',  ( -0.000000000000000000, -1.000000000000000000, -0.000000000000000000 ) ) ;
#38663=CARTESIAN_POINT ( 'NONE',  ( 4.257384923554913492, -49.87499999999998579, 32.69375250200203453 ) ) ;
#38668=CARTESIAN_POINT ( 'NONE',  ( 7.503822152569706638, -47.91357263177820158, 27.87646259706157892 ) ) ;
#38670=ORIENTED_EDGE ( 'NONE', *, *, #7384, .F. ) ;
#38698=( BOUNDED_CURVE ( )  B_SPLINE_CURVE ( 2, ( #31738, #25792, #8780, #21961, #34935, #41326, #5376, #6220, #18354 ),
 .UNSPECIFIED., .F., .T. ) 
 B_SPLINE_CURVE_WITH_KNOTS ( ( 3, 2, 2, 2, 3 ),
 ( 0.1624999999999999778, 0.1666666666666666574, 0.1749999999999999889, 0.1833333333333333204, 0.1875000000000000000 ),
 .UNSPECIFIED. ) 
 CURVE ( )  GEOMETRIC_REPRESENTATION_ITEM ( )  RATIONAL_B_SPLINE_CURVE ( ( 0.9330127018922194093, 0.9330127018922191873, 1.000000000000000000, 0.8660254037844387076, 1.000000000000000000, 0.8660254037844387076, 1.000000000000000000, 0.9330127018922194093, 0.9330127018922194093 ) ) 
 REPRESENTATION_ITEM ( '' )  );
#38700=CYLINDRICAL_SURFACE ( 'NONE', #22608, 3.499999999999996003 ) ;
#38704=CARTESIAN_POINT ( 'NONE',  ( 3.319562750045980337, -51.10267090063073425, 25.69375250200204519 ) ) ;
#38705=CARTESIAN_POINT ( 'NONE',  ( 9.216391464164017222, 7.250000000000000000, 25.89968016835878828 ) ) ;
#38713=CARTESIAN_POINT ( 'NONE',  ( 1.765637743271347038, -42.63301343970476154, 31.69397149145243731 ) ) ;
#38715=CARTESIAN_POINT ( 'NONE',  ( 7.567941867304904591, -43.64062500047794657, 29.19375250200204164 ) ) ;
#38717=CARTESIAN_POINT ( 'NONE',  ( 0.9468279798049134000, -44.84479166714461940, 27.28240155936039102 ) ) ;
#38720=CARTESIAN_POINT ( 'NONE',  ( 4.257384923554909051, -52.75000000000000000, 25.69375250200204519 ) ) ;
#38725=CARTESIAN_POINT ( 'NONE',  ( 6.745679961556507287, -47.00793802605274152, 31.67521643054201874 ) ) ;
#38726=CARTESIAN_POINT ( 'NONE',  ( 7.567941867304902814, -46.18229166714461797, 31.10510344464368870 ) ) ;
#38731=ORIENTED_EDGE ( 'NONE', *, *, #34208, .T. ) ;
#38750=LINE ( 'NONE', #28745, #23473 ) ;
#38758=CARTESIAN_POINT ( 'NONE',  ( 7.567941867304905479, -50.55312500047794799, 29.19375250200204164 ) ) ;
#38762=CARTESIAN_POINT ( 'NONE',  ( 2.507384923554911715, -48.58333333333332860, 26.16266358875650866 ) ) ;
#38766=CARTESIAN_POINT ( 'NONE',  ( 7.757384923554904610, -51.20833333333332149, 27.17302655983835180 ) ) ;
#38767=CARTESIAN_POINT ( 'NONE',  ( 7.714925209453245891, -43.42662810561786557, 28.40897263654498772 ) ) ;
#38768=CARTESIAN_POINT ( 'NONE',  ( 2.602106451679912169, -50.97395833381128227, 26.32672608803957459 ) ) ;
#38772=CARTESIAN_POINT ( 'NONE',  ( 1.380005750912540075, -51.14648319177504732, 31.23700828352463787 ) ) ;
#38776=CARTESIAN_POINT ( 'NONE',  ( 0.7573849235549120484, -49.45833333333332860, 31.21447844416572792 ) ) ;
#38780=CARTESIAN_POINT ( 'NONE',  ( 0.9468279798049125118, -49.30312500047794799, 29.19375250200204164 ) ) ;
#38788=CARTESIAN_POINT ( 'NONE',  ( 4.257384923554908163, -51.37499999999999289, 33.23520438632941421 ) ) ;
#38798=CARTESIAN_POINT ( 'NONE',  ( 0.7833427284552760828, -44.20303821867119609, 28.75667872767649769 ) ) ;
#38801=CARTESIAN_POINT ( 'NONE',  ( 4.257384923554909051, -46.62499999999999289, 25.69375250200204519 ) ) ;
#38815=CARTESIAN_POINT ( 'NONE',  ( 2.602106451679909505, -46.80729166714461087, 32.06077891596451224 ) ) ;
#38820=CARTESIAN_POINT ( 'NONE',  ( 7.567941867304905479, -50.01145833381128369, 27.28240155936039457 ) ) ;
#38823=ORIENTED_EDGE ( 'NONE', *, *, #10718, .F. ) ;
#38825=ORIENTED_EDGE ( 'NONE', *, *, #33733, .F. ) ;
#38826=CARTESIAN_POINT ( 'NONE',  ( 0.7573849235549138248, -49.57229166657106845, 27.17302655983835180 ) ) ;
#38833=CARTESIAN_POINT ( 'NONE',  ( 7.757384923554905498, -43.94375000095590877, 29.19375250200204164 ) ) ;
#38835=EDGE_LOOP ( 'NONE', ( #18899, #4137, #38825, #13931, #963 ) ) ;
#38869=CARTESIAN_POINT ( 'NONE',  ( 2.602106451679911281, -45.38645833381128369, 26.32672608803957459 ) ) ;
#38872=CARTESIAN_POINT ( 'NONE',  ( 4.257384923554909051, -48.62499999999997868, 25.69375250200204519 ) ) ;
#38878=CARTESIAN_POINT ( 'NONE',  ( 7.598587240175194601, -47.97255824994331874, 30.36080446354949913 ) ) ;
#38882=DIRECTION ( 'NONE',  ( 0.000000000000000000, 0.000000000000000000, -1.000000000000000000 ) ) ;
#38886=EDGE_CURVE ( 'NONE', #35642, #2889, #29871, .T. ) ;
#38889=AXIS2_PLACEMENT_3D ( 'NONE', #38566, #6240, #36426 ) ;
#38902=EDGE_CURVE ( 'NONE', #37984, #38516, #15445, .T. ) ;
#38914=CARTESIAN_POINT ( 'NONE',  ( 0.9136055911694869192, -45.67044313664037247, 30.23500233154295103 ) ) ;
#38926=CARTESIAN_POINT ( 'NONE',  ( 2.602106451679912169, -42.47395833381127517, 26.32672608803957459 ) ) ;
#38934=CARTESIAN_POINT ( 'NONE',  ( 5.912663395429904156, -45.72395833381128227, 32.06077891596451224 ) ) ;
#38944=ORIENTED_EDGE ( 'NONE', *, *, #6870, .F. ) ;
#38966=CARTESIAN_POINT ( 'NONE',  ( 5.912663395429905044, -51.63645833381128369, 32.06077891596451224 ) ) ;
#38969=FACE_OUTER_BOUND ( 'NONE', #5984, .T. ) ;
#38970=CARTESIAN_POINT ( 'NONE',  ( 7.757384923554904610, -48.20833333333332149, 27.17302655983835180 ) ) ;
#38976=CARTESIAN_POINT ( 'NONE',  ( 4.603315378677745429, -43.56273844970385056, 32.69375263004300791 ) ) ;
#38977=CARTESIAN_POINT ( 'NONE',  ( 5.912663395429904156, -49.72395833381128227, 32.06077891596451224 ) ) ;
#38983=CARTESIAN_POINT ( 'NONE',  ( 0.7573849235549138248, -50.04166666666666430, 27.17302655983835180 ) ) ;
#38984=CARTESIAN_POINT ( 'NONE',  ( 5.195207097063836876, -45.14732909936925154, 25.69375250200204519 ) ) ;
#38986=CARTESIAN_POINT ( 'NONE',  ( 5.238511374674988730, -46.34208369659737059, 25.82314355930084915 ) ) ;
#38990=CARTESIAN_POINT ( 'NONE',  ( 0.7593310934756882791, -48.69106711361769868, 29.32456282660584890 ) ) ;
#39018=CARTESIAN_POINT ( 'NONE',  ( 0.9468279798049124008, -47.84895833381128227, 31.10510344464368515 ) ) ;
#39022=CARTESIAN_POINT ( 'NONE',  ( 4.257384923554908163, -49.17812500047794799, 33.01645438728532866 ) ) ;
#39029=CARTESIAN_POINT ( 'NONE',  ( 0.7573849235549138248, -48.57229166657106845, 27.17302655983835180 ) ) ;
#39032=ORIENTED_EDGE ( 'NONE', *, *, #30560, .T. ) ;
#39036=CARTESIAN_POINT ( 'NONE',  ( 6.007384923554907274, -44.86041666762257307, 26.16266358875650866 ) ) ;
#39039=EDGE_LOOP ( 'NONE', ( #35279, #14291, #28086, #39142 ) ) ;
#39040=CYLINDRICAL_SURFACE ( 'NONE', #39834, 3.499999999999996003 ) ;
#39050=DIRECTION ( 'NONE',  ( -0.000000000000000000, -1.000000000000000000, -0.000000000000000000 ) ) ;
#39052=UNCERTAINTY_MEASURE_WITH_UNIT (LENGTH_MEASURE( 1.000000000000000082E-05 ), #26884, 'distance_accuracy_value', 'NONE');
#39074=CARTESIAN_POINT ( 'NONE',  ( 7.567941867304905479, -46.01145833381127659, 27.28240155936039812 ) ) ;
#39077=CARTESIAN_POINT ( 'NONE',  ( 6.995232616280920190, -43.89111165166269757, 26.97769823792731714 ) ) ;
#39090=CARTESIAN_POINT ( 'NONE',  ( 0.9870038947435508803, -50.66231609540762548, 30.52759166177329675 ) ) ;
#39091=ADVANCED_FACE ( 'NONE', ( #15019 ), #5438, .T. ) ;
#39100=DIRECTION ( 'NONE',  ( 0.000000000000000000, 0.000000000000000000, -1.000000000000000000 ) ) ;
#39111=CARTESIAN_POINT ( 'NONE',  ( 7.417243718325343238, -45.40866587835354551, 27.68864479613948149 ) ) ;
#39120=DIRECTION ( 'NONE',  ( -0.000000000000000000, -1.000000000000000000, -0.000000000000000000 ) ) ;
#39122=CARTESIAN_POINT ( 'NONE',  ( 0.7980520403560245057, -42.70747941762135724, 28.53809425231622399 ) ) ;
#39125=CARTESIAN_POINT ( 'NONE',  ( 0.9468279798049134000, -42.84479166714461940, 27.28240155936039102 ) ) ;
#39127=ORIENTED_EDGE ( 'NONE', *, *, #33663, .T. ) ;
#39131=CARTESIAN_POINT ( 'NONE',  ( 7.567941867304902814, -44.18229166714461797, 31.10510344464368870 ) ) ;
#39139=CARTESIAN_POINT ( 'NONE',  ( 4.910170338596717698, -46.05320690417175911, 32.63238856155484058 ) ) ;
#39142=ORIENTED_EDGE ( 'NONE', *, *, #31967, .F. ) ;
#39147=DIRECTION ( 'NONE',  ( -0.000000000000000000, -1.000000000000000000, -0.000000000000000000 ) ) ;
#39160=CARTESIAN_POINT ( 'NONE',  ( 4.257384923554908163, -51.17812500047794799, 33.01645438728532866 ) ) ;
#39161=CARTESIAN_POINT ( 'NONE',  ( 1.424348344509744235, -47.14417379375343131, 31.29540821818305218 ) ) ;
#39164=CARTESIAN_POINT ( 'NONE',  ( 6.007384923554904610, -47.83333333333332149, 32.22484141524757462 ) ) ;
#39171=CARTESIAN_POINT ( 'NONE',  ( 7.257119946227015284, -43.40002460845716570, 27.36671699846773009 ) ) ;
#39173=CARTESIAN_POINT ( 'NONE',  ( 2.602106451679912169, -48.97395833381128227, 26.32672608803957459 ) ) ;
#39179=CARTESIAN_POINT ( 'NONE',  ( 4.257384923554909051, -49.12499999999997868, 25.15230061767466552 ) ) ;
#39181=CARTESIAN_POINT ( 'NONE',  ( 4.257384923554907274, -45.37499999999999289, 32.69375250200203453 ) ) ;
#39183=CARTESIAN_POINT ( 'NONE',  ( 5.603086445853804776, -46.53864453555991787, 32.44234740926479788 ) ) ;
#39192=CARTESIAN_POINT ( 'NONE',  ( 0.7573849235549138248, -48.73541666762257307, 27.17302655983835180 ) ) ;
#39201=CARTESIAN_POINT ( 'NONE',  ( 0.9220331012640999857, -44.16572571656928403, 30.40542051012231539 ) ) ;
#39206=CARTESIAN_POINT ( 'NONE',  ( 7.757384923554904610, -42.90208333428923737, 27.17302655983835180 ) ) ;
#39211=DIRECTION ( 'NONE',  ( 0.000000000000000000, 1.000000000000000000, 0.000000000000000000 ) ) ;
#39218=CARTESIAN_POINT ( 'NONE',  ( 5.912663395429907709, -44.55729166714461797, 26.32672608803957459 ) ) ;
#39221=CARTESIAN_POINT ( 'NONE',  ( 5.912663395429905044, -50.13645833381128369, 32.06077891596451224 ) ) ;
#39228=CARTESIAN_POINT ( 'NONE',  ( 6.007384923554904610, -47.36395833323773275, 32.22484141524757462 ) ) ;
#39235=CARTESIAN_POINT ( 'NONE',  ( 4.257384923554908163, -44.06875000095590877, 33.23520438632941421 ) ) ;
#39236=CARTESIAN_POINT ( 'NONE',  ( 7.757384923554904610, -43.40208333428924448, 27.17302655983835180 ) ) ;
#39255=CARTESIAN_POINT ( 'NONE',  ( 4.257384923554909051, -52.75000000000000000, 32.69375250200203453 ) ) ;
#39268=ORIENTED_EDGE ( 'NONE', *, *, #10282, .T. ) ;
#39271=CARTESIAN_POINT ( 'NONE',  ( 7.567941867304904591, -52.14062500047794657, 29.19375250200204164 ) ) ;
#39280=CARTESIAN_POINT ( 'NONE',  ( 7.768069823941834429, -48.44960502302508587, 29.55150272548278778 ) ) ;
#39281=ORIENTED_EDGE ( 'NONE', *, *, #41216, .F. ) ;
#39288=ORIENTED_EDGE ( 'NONE', *, *, #8077, .T. ) ;
#39290=CARTESIAN_POINT ( 'NONE',  ( 6.955504822719134950, -42.31075905001993220, 34.01771537441437943 ) ) ;
#39293=CARTESIAN_POINT ( 'NONE',  ( 4.257384923554909051, -42.40485061181025372, 29.19375250200204164 ) ) ;
#39313=CARTESIAN_POINT ( 'NONE',  ( 7.339647754402778723, -45.40455638939489802, 27.53362591471264764 ) ) ;
#39325=CARTESIAN_POINT ( 'NONE',  ( 2.142675753277913486, -42.76592205225234977, 26.35435275062776128 ) ) ;
#39328=CARTESIAN_POINT ( 'NONE',  ( 0.9468279798049117346, -43.26145833381128369, 31.10510344464368515 ) ) ;
#39336=VECTOR ( 'NONE', #20534, 1000.000000000000000 ) ;
#39340=CARTESIAN_POINT ( 'NONE',  ( 3.319562750045979005, -46.89732909936925864, 32.69375250200202743 ) ) ;
#39358=CARTESIAN_POINT ( 'NONE',  ( 4.257384923554896616, -47.62499999999999289, 25.69375250200204519 ) ) ;
#39366=CARTESIAN_POINT ( 'NONE',  ( 4.257384923554908163, -50.67812500047794799, 33.01645438728532866 ) ) ;
#39367=CARTESIAN_POINT ( 'NONE',  ( 4.024745076659226761, -47.31350275550386897, 25.70038837312468161 ) ) ;
#39371=B_SPLINE_CURVE_WITH_KNOTS ( 'NONE', 3,
 ( #23907, #20710, #27088, #36658, #14324, #20912, #33885, #40054, #33686, #17516, #30482, #17093, #30693, #24321, #17723, #20279, #7945, #4326 ),
 .UNSPECIFIED., .F., .F.,
 ( 4, 2, 2, 2, 2, 2, 2, 2, 4 ),
 ( 0.6983096216405908496, 0.7014811667581976051, 0.7046527118758044717, 0.7078242569934112272, 0.7109958021110180937, 0.7141673472286248492, 0.7173388923462316047, 0.7205104374638384712, 0.7236819825814452267 ),
 .UNSPECIFIED. ) ;
#39372=CARTESIAN_POINT ( 'NONE',  ( 2.507384923554911715, -47.08333333333332149, 26.16266358875650866 ) ) ;
#39381=CARTESIAN_POINT ( 'NONE',  ( 0.9468279798049143992, -47.93229166714461797, 27.28240155936039812 ) ) ;
#39387=CARTESIAN_POINT ( 'NONE',  ( 6.007384923554907274, -51.16666666666665719, 26.16266358875650866 ) ) ;
#39388=CARTESIAN_POINT ( 'NONE',  ( 0.9468279798049143992, -50.93229166714461797, 27.28240155936039457 ) ) ;
#39398=CARTESIAN_POINT ( 'NONE',  ( 7.757384923554902834, -48.48541666762256597, 31.21447844416572792 ) ) ;
#39412=CARTESIAN_POINT ( 'NONE',  ( 1.424350047630230431, -44.64417359024929510, 31.29541048859400121 ) ) ;
#39428=CARTESIAN_POINT ( 'NONE',  ( 4.257384923554908163, -46.26562500047795368, 33.01645438728532866 ) ) ;
#39432=CARTESIAN_POINT ( 'NONE',  ( 4.257384923554908163, -49.67812500047794799, 33.01645438728532866 ) ) ;
#39437=EDGE_LOOP ( 'NONE', ( #33751, #17405, #26552, #5026, #21208, #9606, #5875, #24152, #26693, #22046, #35932, #15509, #8835, #34745, #21413, #14552, #39549, #20781, #38565, #8207, #30709, #2626, #32125, #8172, #1978, #15026, #26802, #31494, #2144, #34023, #21319, #12600, #29559, #31188, #38944, #13395, #26279, #17920, #18266, #16804, #12473, #22543, #34539, #14979 ) ) ;
#39441=CARTESIAN_POINT ( 'NONE',  ( 4.257384923554909051, -47.65562499990439704, 25.15230061767466552 ) ) ;
#39447=CARTESIAN_POINT ( 'NONE',  ( 6.007384923554907274, -43.36041666762257307, 26.16266358875650866 ) ) ;
#39448=CARTESIAN_POINT ( 'NONE',  ( 2.507384923554911715, -43.27708333428924448, 26.16266358875650866 ) ) ;
#39450=ORIENTED_EDGE ( 'NONE', *, *, #24931, .F. ) ;
#39489=CARTESIAN_POINT ( 'NONE',  ( 2.602106451679911281, -43.38645833381128369, 26.32672608803957459 ) ) ;
#39498=CARTESIAN_POINT ( 'NONE',  ( 5.158093851143114250, -48.33854257795462672, 25.78177109524803967 ) ) ;
#39505=ORIENTED_EDGE ( 'NONE', *, *, #26230, .T. ) ;
#39508=CARTESIAN_POINT ( 'NONE',  ( 6.007384923554907274, -42.66666666666665719, 26.16266358875650866 ) ) ;
#39512=CARTESIAN_POINT ( 'NONE',  ( 0.7573849235549129366, -51.99999999999999289, 29.19375250200204164 ) ) ;
#39546=CARTESIAN_POINT ( 'NONE',  ( 4.257384923554908163, -42.67812500047794799, 33.01645438728532866 ) ) ;
#39549=ORIENTED_EDGE ( 'NONE', *, *, #21287, .F. ) ;
#39552=CARTESIAN_POINT ( 'NONE',  ( 2.602106451679911281, -48.38645833381128369, 26.32672608803957459 ) ) ;
#39557=CARTESIAN_POINT ( 'NONE',  ( 5.158096795874895335, -45.83854262196766172, 25.78177182199053519 ) ) ;
#39567=B_SPLINE_CURVE_WITH_KNOTS ( 'NONE', 3,
 ( #20355, #16546, #40494, #26534, #14554, #27528, #33109, #36518, #33321, #32900, #29712, #17738, #14765, #13546, #39077, #8160, #1577, #3974, #11352, #10154, #24336, #17946 ),
 .UNSPECIFIED., .F., .F.,
 ( 4, 2, 2, 2, 2, 2, 2, 2, 2, 2, 4 ),
 ( 0.7953550928917824114, 0.7972236050084329229, 0.7990921171250835453, 0.8009606292417340567, 0.8028291413583845682, 0.8065661655916857020, 0.8103031898249867249, 0.8140402140582878587, 0.8177772382915889926, 0.8215142625248900154, 0.8252512867581911493 ),
 .UNSPECIFIED. ) ;
#39585=CARTESIAN_POINT ( 'NONE',  ( 2.602106451679911281, -50.38645833381128369, 26.32672608803957459 ) ) ;
#39589=CARTESIAN_POINT ( 'NONE',  ( 6.007384923554907274, -47.66666666666665719, 26.16266358875650866 ) ) ;
#39596=CARTESIAN_POINT ( 'NONE',  ( 5.912663395429904156, -49.22395833381128227, 32.06077891596451224 ) ) ;
#39602=CARTESIAN_POINT ( 'NONE',  ( 7.757384923554905498, -48.24999999999998579, 29.19375250200204164 ) ) ;
#39604=CARTESIAN_POINT ( 'NONE',  ( 0.9468279798049124008, -50.84895833381128227, 31.10510344464368515 ) ) ;
#39608=CARTESIAN_POINT ( 'NONE',  ( 0.7573849235549138248, -43.54166666666665719, 27.17302655983835180 ) ) ;
#39615=CARTESIAN_POINT ( 'NONE',  ( 6.007384923554907274, -49.36041666762257307, 26.16266358875650866 ) ) ;
#39628=CARTESIAN_POINT ( 'NONE',  ( 3.728821824152880104, -44.80679457882185091, 25.73137165454332020 ) ) ;
#39646=CARTESIAN_POINT ( 'NONE',  ( 7.567941867304904591, -46.59895833381128227, 27.28240155936039812 ) ) ;
#39650=CARTESIAN_POINT ( 'NONE',  ( 4.257384923554909051, -47.42812500047796220, 25.37105061671875106 ) ) ;
#39656=CARTESIAN_POINT ( 'NONE',  ( 6.007384923554904610, -45.86395833323773275, 32.22484141524757462 ) ) ;
#39661=CARTESIAN_POINT ( 'NONE',  ( 7.757384923554902834, -50.79166666666665719, 31.21447844416572792 ) ) ;
#39662=CARTESIAN_POINT ( 'NONE',  ( 2.507384923554909495, -44.61041666762257307, 32.22484141524756751 ) ) ;
#39663=TOROIDAL_SURFACE ( 'NONE', #13868, 8.161279603635192004, 2.000000000000000000 ) ;
#39669=ADVANCED_FACE ( 'NONE', ( #26734 ), #26520, .T. ) ;
#39671=EDGE_CURVE ( 'NONE', #28152, #20255, #353, .T. ) ;
#39674=EDGE_CURVE ( 'NONE', #40028, #27384, #9853, .T. ) ;
#39705=CARTESIAN_POINT ( 'NONE',  ( 2.602106451679909505, -44.21979166714461940, 32.06077891596451224 ) ) ;
#39708=LINE ( 'NONE', #10366, #10174 ) ;
#39715=CARTESIAN_POINT ( 'NONE',  ( 2.466134985911174304, -42.40449753004583755, 26.18386436545577922 ) ) ;
#39726=CARTESIAN_POINT ( 'NONE',  ( 4.257384923554909051, -43.12499999999999289, 25.15230061767466552 ) ) ;
#39730=CARTESIAN_POINT ( 'NONE',  ( 3.319562750045980337, -52.10267090063072715, 25.69375250200204519 ) ) ;
#39732=AXIS2_PLACEMENT_3D ( 'NONE', #22313, #12320, #34868 ) ;
#39756=CARTESIAN_POINT ( 'NONE',  ( 5.221911385353703139, -45.34002536942892192, 25.79487343363435770 ) ) ;
#39770=CARTESIAN_POINT ( 'NONE',  ( 7.567941867304905479, -42.55312500047794799, 29.19375250200204164 ) ) ;
#39777=EDGE_CURVE ( 'NONE', #22238, #32591, #22696, .T. ) ;
#39778=CARTESIAN_POINT ( 'NONE',  ( 7.567941867304904591, -46.59479166714461229, 31.10510344464368870 ) ) ;
#39782=CARTESIAN_POINT ( 'NONE',  ( 7.744254439903421883, -45.92914486373499727, 28.65094957864718239 ) ) ;
#39810=CARTESIAN_POINT ( 'NONE',  ( 7.567941867304905479, -47.51145833381127659, 27.28240155936039812 ) ) ;
#39814=CARTESIAN_POINT ( 'NONE',  ( 6.007384923554907274, -48.16666666666665719, 26.16266358875650866 ) ) ;
#39820=CARTESIAN_POINT ( 'NONE',  ( 0.9468279798049124008, -49.84895833381128227, 31.10510344464368515 ) ) ;
#39824=CARTESIAN_POINT ( 'NONE',  ( 4.257397009801616505, -51.06825406007883572, 32.69375250196129912 ) ) ;
#39827=CARTESIAN_POINT ( 'NONE',  ( 7.757384923554904610, -48.20833333333332149, 27.17302655983835180 ) ) ;
#39828=CARTESIAN_POINT ( 'NONE',  ( 0.9468279798049143992, -50.43229166714461797, 27.28240155936039457 ) ) ;
#39832=CARTESIAN_POINT ( 'NONE',  ( 1.565627383209468482, -43.13800020507162003, 31.43083490771288169 ) ) ;
#39834=AXIS2_PLACEMENT_3D ( 'NONE', #38628, #35848, #32863 ) ;
#39839=CARTESIAN_POINT ( 'NONE',  ( 4.257384923554909051, -49.81875000095590167, 25.15230061767466552 ) ) ;
#39850=CARTESIAN_POINT ( 'NONE',  ( 4.228262762087923399, -44.81809345912770937, 25.69385632335355041 ) ) ;
#39859=VERTEX_POINT ( 'NONE', #16736 ) ;
#39861=CARTESIAN_POINT ( 'NONE',  ( 5.912663395429907709, -45.55729166714461797, 26.32672608803957459 ) ) ;
#39866=CARTESIAN_POINT ( 'NONE',  ( 2.602106451679909505, -47.21979166714461229, 32.06077891596451224 ) ) ;
#39872=CARTESIAN_POINT ( 'NONE',  ( 0.7573849235549120484, -46.48895833323773275, 31.21447844416572792 ) ) ;
#39878=CARTESIAN_POINT ( 'NONE',  ( 2.507384923554909495, -43.11041666762257307, 32.22484141524756751 ) ) ;
#39880=EDGE_LOOP ( 'NONE', ( #16133, #10601, #41193, #7750 ) ) ;
#39905=CARTESIAN_POINT ( 'NONE',  ( 6.440082037525358238, -50.87102193237520709, 26.41833544997166783 ) ) ;
#39906=ADVANCED_FACE ( 'NONE', ( #23751 ), #13965, .T. ) ;
#39916=CARTESIAN_POINT ( 'NONE',  ( 7.567941867304905479, -43.01145833381129080, 27.28240155936039812 ) ) ;
#39924=EDGE_CURVE ( 'NONE', #5921, #35115, #6292, .T. ) ;
#39925=CARTESIAN_POINT ( 'NONE',  ( 4.866654878311854837, -48.55424356578008371, 32.64031840814624275 ) ) ;
#39929=CARTESIAN_POINT ( 'NONE',  ( 0.8500331308301141142, -44.21153070892416537, 28.38400101020632249 ) ) ;
#39930=CARTESIAN_POINT ( 'NONE',  ( 1.196014987747854308, -50.15239607024638957, 30.95119510937487206 ) ) ;
#39936=CARTESIAN_POINT ( 'NONE',  ( 0.7573849235549138248, -49.73541666762256597, 27.17302655983835180 ) ) ;
#39937=CARTESIAN_POINT ( 'NONE',  ( 5.912663395429904156, -43.72395833381127517, 32.06077891596451224 ) ) ;
#39947=CARTESIAN_POINT ( 'NONE',  ( 4.257388422463325384, -49.06861128833901375, 32.69375250199872340 ) ) ;
#39955=CARTESIAN_POINT ( 'NONE',  ( 7.754954177366758294, -42.94811813129728506, 29.41241712777807749 ) ) ;
#39962=EDGE_LOOP ( 'NONE', ( #20094, #26021, #25394, #6447 ) ) ;
#39964=LINE ( 'NONE', #20404, #7678 ) ;
#39973=CARTESIAN_POINT ( 'NONE',  ( 4.257384923554909939, 5.249999999999997335, 21.03247289836684786 ) ) ;
#39974=ORIENTED_EDGE ( 'NONE', *, *, #5340, .T. ) ;
#39984=CARTESIAN_POINT ( 'NONE',  ( 0.9468279798049125118, -45.30312500047794799, 29.19375250200204164 ) ) ;
#39988=CARTESIAN_POINT ( 'NONE',  ( 4.986173583452949920, -46.05139289515954459, 32.61764335583990970 ) ) ;
#39992=ORIENTED_EDGE ( 'NONE', *, *, #39777, .T. ) ;
#40015=CARTESIAN_POINT ( 'NONE',  ( 2.602106451679911281, -48.38645833381128369, 26.32672608803957459 ) ) ;
#40020=CARTESIAN_POINT ( 'NONE',  ( 7.757384923554902834, -43.29166666666666430, 31.21447844416572792 ) ) ;
#40022=DIRECTION ( 'NONE',  ( -0.000000000000000000, -1.000000000000000000, -0.000000000000000000 ) ) ;
#40026=CARTESIAN_POINT ( 'NONE',  ( 0.9468279798049143992, -45.43229166714461797, 27.28240155936039812 ) ) ;
#40028=VERTEX_POINT ( 'NONE', #12805 ) ;
#40033=CARTESIAN_POINT ( 'NONE',  ( 0.7573849235549138248, -47.54166666666666430, 27.17302655983835180 ) ) ;
#40034=CARTESIAN_POINT ( 'NONE',  ( 2.602106451679912169, -51.97395833381127517, 26.32672608803957459 ) ) ;
#40037=CARTESIAN_POINT ( 'NONE',  ( 1.528394789216473315, -43.13937915656339328, 31.38532619635940435 ) ) ;
#40044=CARTESIAN_POINT ( 'NONE',  ( 7.757384923554905498, -49.44375000095590167, 29.19375250200204164 ) ) ;
#40046=AXIS2_PLACEMENT_3D ( 'NONE', #30561, #1427, #14400 ) ;
#40054=CARTESIAN_POINT ( 'NONE',  ( 7.666287247524001813, -44.96382799930678686, 30.10987731412011215 ) ) ;
#40073=CARTESIAN_POINT ( 'NONE',  ( 5.912663395429907709, -43.05729166714461797, 26.32672608803957459 ) ) ;
#40082=CARTESIAN_POINT ( 'NONE',  ( 2.507384923554909495, -45.94729166657106845, 32.22484141524756751 ) ) ;
#40088=CARTESIAN_POINT ( 'NONE',  ( 7.757384923554905498, -50.74999999999999289, 29.19375250200204164 ) ) ;
#40089=CARTESIAN_POINT ( 'NONE',  ( 6.007384923554904610, -45.02708333428923737, 32.22484141524757462 ) ) ;
#40094=CARTESIAN_POINT ( 'NONE',  ( 4.257384923554909051, 7.250000000000000000, 29.19375250200204164 ) ) ;
#40103=CARTESIAN_POINT ( 'NONE',  ( 4.257384918501243121, -51.56875000107599760, 32.69375250200203453 ) ) ;
#40114=CARTESIAN_POINT ( 'NONE',  ( 5.177855991107565004, -51.04659951482094726, 32.59344845590745621 ) ) ;
#40122=VECTOR ( 'NONE', #7553, 1000.000000000000000 ) ;
#40125=CARTESIAN_POINT ( 'NONE',  ( 4.257384923554909051, -42.42812500047794799, 25.37105061671875461 ) ) ;
#40127=CARTESIAN_POINT ( 'NONE',  ( 6.007384923554904610, -47.83333333333332149, 32.22484141524757462 ) ) ;
#40133=CARTESIAN_POINT ( 'NONE',  ( 7.691985863281998625, -48.45987965223148564, 30.00394388495349318 ) ) ;
#40134=VERTEX_POINT ( 'NONE', #39 ) ;
#40146=CARTESIAN_POINT ( 'NONE',  ( 0.7573849235549138248, -48.23541666762256597, 27.17302655983835180 ) ) ;
#40161=CARTESIAN_POINT ( 'NONE',  ( 0.7573849235549120484, -43.95833333333332149, 31.21447844416572792 ) ) ;
#40171=CARTESIAN_POINT ( 'NONE',  ( 4.257384923554913492, -50.87499999999999289, 32.69375250200203453 ) ) ;
#40179=CARTESIAN_POINT ( 'NONE',  ( 7.315637186035080397, -49.90041940074508631, 27.43108590933141144 ) ) ;
#40195=CARTESIAN_POINT ( 'NONE',  ( 2.602106451679909505, -46.71979166714461229, 32.06077891596451224 ) ) ;
#40196=CARTESIAN_POINT ( 'NONE',  ( 4.257406270103921919, -48.06789733593042513, 32.69375250187820114 ) ) ;
#40198=CARTESIAN_POINT ( 'NONE',  ( 7.757384923554902834, -44.79166666666665719, 31.21447844416572792 ) ) ;
#40201=ORIENTED_EDGE ( 'NONE', *, *, #3138, .T. ) ;
#40210=CARTESIAN_POINT ( 'NONE',  ( 3.048166101253366733, -46.09728155433570151, 32.49173244127049998 ) ) ;
#40223=CARTESIAN_POINT ( 'NONE',  ( 3.319562750045980337, -51.60267090063072715, 25.69375250200204519 ) ) ;
#40227=CARTESIAN_POINT ( 'NONE',  ( 0.9468279798049125118, -48.30312500047795510, 29.19375250200204164 ) ) ;
#40232=CARTESIAN_POINT ( 'NONE',  ( 7.757384923554904610, -44.20833333333332149, 27.17302655983835180 ) ) ;
#40234=DIRECTION ( 'NONE',  ( 0.000000000000000000, 0.000000000000000000, -1.000000000000000000 ) ) ;
#40238=CARTESIAN_POINT ( 'NONE',  ( 7.567941867304902814, -46.18229166714461087, 31.10510344464368870 ) ) ;
#40245=CARTESIAN_POINT ( 'NONE',  ( 2.507384923554909495, -46.41666666666666430, 32.22484141524756751 ) ) ;
#40246=CARTESIAN_POINT ( 'NONE',  ( 0.9468279798049132889, -49.89062500047794657, 29.19375250200204164 ) ) ;
#40247=ORIENTED_EDGE ( 'NONE', *, *, #25705, .F. ) ;
#40259=CARTESIAN_POINT ( 'NONE',  ( 7.757384923554905498, -47.44375000095590877, 29.19375250200204164 ) ) ;
#40272=CARTESIAN_POINT ( 'NONE',  ( 2.969867941416742152, -44.78911512457433020, 25.92902140427570146 ) ) ;
#40285=CARTESIAN_POINT ( 'NONE',  ( 7.567941867304904591, -43.09895833381128227, 27.28240155936039812 ) ) ;
#40290=B_SPLINE_CURVE_WITH_KNOTS ( 'NONE', 3,
 ( #28085, #41064, #11916, #24910 ),
 .UNSPECIFIED., .F., .F.,
 ( 4, 4 ),
 ( 0.000000000000000000, 7.737219110625801963E-05 ),
 .UNSPECIFIED. ) ;
#40295=CARTESIAN_POINT ( 'NONE',  ( 6.007384923554907274, -45.19729166657106845, 26.16266358875650866 ) ) ;
#40302=CARTESIAN_POINT ( 'NONE',  ( 2.602106451679909505, -50.21979166714461940, 32.06077891596451224 ) ) ;
#40310=CARTESIAN_POINT ( 'NONE',  ( 2.507384923554909495, -51.41666666666665719, 32.22484141524756751 ) ) ;
#40311=AXIS2_PLACEMENT_3D ( 'NONE', #25168, #35776, #18987 ) ;
#40320=CARTESIAN_POINT ( 'NONE',  ( 5.408115636292230022, -51.34643313192503200, 25.87604258886805297 ) ) ;
#40323=CARTESIAN_POINT ( 'NONE',  ( 6.007384923554904610, -48.33333333333332860, 32.22484141524757462 ) ) ;
#40333=CARTESIAN_POINT ( 'NONE',  ( 6.927642430100137361, -50.88721722400683234, 26.91910934872551664 ) ) ;
#40342=CARTESIAN_POINT ( 'NONE',  ( 4.257384923554908163, -51.76562500047794657, 33.01645438728532866 ) ) ;
#40360=CARTESIAN_POINT ( 'NONE',  ( 0.7573849235549120484, -49.65208333428923737, 31.21447844416572792 ) ) ;
#40361=CARTESIAN_POINT ( 'NONE',  ( 0.9468279798049132889, -42.39062500047794657, 29.19375250200204164 ) ) ;
#40367=CARTESIAN_POINT ( 'NONE',  ( 4.257384923554909051, -52.75000000000000000, 29.19375250200204164 ) ) ;
#40378=B_SPLINE_CURVE_WITH_KNOTS ( 'NONE', 3,
 ( #27072, #10907, #7719, #20691, #23235, #13882, #33017, #1335, #7292, #33868, #11119, #23677, #33669, #26861, #7076, #40037, #1127, #39832, #20895, #30040, #3885, #13451, #37073, #14307, #30465, #20262, #17075, #4728, #26437, #7929, #13666 ),
 .UNSPECIFIED., .F., .F.,
 ( 4, 2, 2, 2, 2, 2, 2, 2, 1, 2, 2, 1, 1, 2, 2, 2, 4 ),
 ( 0.8760364031802420071, 0.8794105722678615678, 0.8827847413554812395, 0.8861589104431008002, 0.8895330795307203609, 0.8929072486183400326, 0.8937507908902448950, 0.8941725620261973262, 0.8942780048101854895, 0.8943307262021795712, 0.8943439065501780361, 0.8943570868981765010, 0.8943834475941735418, 0.8945943331621503125, 0.8962814177059641452, 0.8996555867935920325, 0.9030297558812198089 ),
 .UNSPECIFIED. ) ;
#40381=CARTESIAN_POINT ( 'NONE',  ( 7.739515353988964286, -42.95214612222731176, 29.59185003268196468 ) ) ;
#40393=CARTESIAN_POINT ( 'NONE',  ( 6.523534992973405444, -49.01344472851528167, 31.86129379394605365 ) ) ;
#40402=ORIENTED_EDGE ( 'NONE', *, *, #22277, .F. ) ;
#40405=CARTESIAN_POINT ( 'NONE',  ( 5.912663395429905044, -45.63645833381128369, 32.06077891596451224 ) ) ;
#40409=LINE ( 'NONE', #5724, #37705 ) ;
#40415=EDGE_CURVE ( 'NONE', #3034, #29243, #11856, .T. ) ;
#40435=CARTESIAN_POINT ( 'NONE',  ( 5.912663395429905044, -48.13645833381128369, 32.06077891596451224 ) ) ;
#40438=DIRECTION ( 'NONE',  ( -0.000000000000000000, -1.000000000000000000, -0.000000000000000000 ) ) ;
#40440=CARTESIAN_POINT ( 'NONE',  ( 2.507384923554911715, -44.58333333333332149, 26.16266358875650866 ) ) ;
#40442=AXIS2_PLACEMENT_3D ( 'NONE', #11131, #24112, #36650 ) ;
#40443=CARTESIAN_POINT ( 'NONE',  ( 7.594402521559315389, -49.41981346090616967, 28.13659641155990698 ) ) ;
#40445=CARTESIAN_POINT ( 'NONE',  ( 1.132663516193878950, -49.23063060117946321, 27.55179856133426952 ) ) ;
#40450=CARTESIAN_POINT ( 'NONE',  ( 0.9468279798049124008, -46.84895833381128227, 31.10510344464368515 ) ) ;
#40453=B_SPLINE_CURVE_WITH_KNOTS ( 'NONE', 3,
 ( #24898, #15327, #8716, #31263, #18720, #38067, #8926, #2548, #31679, #21897, #2126, #9138, #15109, #34876, #28486, #41479, #38272, #15743, #38492, #9354, #22320, #35297, #39111, #16791, #13589, #39313, #26573, #35920, #9788, #10192, #32521, #39756, #16378, #25947 ),
 .UNSPECIFIED., .F., .F.,
 ( 4, 2, 2, 2, 2, 2, 2, 2, 2, 2, 2, 2, 1, 1, 2, 2, 2, 4 ),
 ( 0.6462026339712469980, 0.6495394992190089978, 0.6512079318428900532, 0.6516250399988602338, 0.6520421481548305254, 0.6528763644667711086, 0.6562132297145334414, 0.6595500949622956632, 0.6628869602100579961, 0.6637211765219985793, 0.6637733150414948380, 0.6638254535609910967, 0.6639297305999837251, 0.6641382846779688709, 0.6645553928339391625, 0.6662238254578205510, 0.6695606907055833279, 0.6728975559533459938 ),
 .UNSPECIFIED. ) ;
#40458=CARTESIAN_POINT ( 'NONE',  ( 7.757384923554902834, -47.79166666666665719, 31.21447844416572792 ) ) ;
#40459=CARTESIAN_POINT ( 'NONE',  ( 2.602106451679909505, -46.80729166714461087, 32.06077891596451224 ) ) ;
#40470=CARTESIAN_POINT ( 'NONE',  ( 0.7573849235549129366, -46.19375000095590877, 29.19375250200204164 ) ) ;
#40494=CARTESIAN_POINT ( 'NONE',  ( 4.956495632475545143, -44.05388999312047105, 32.63984233408726254 ) ) ;
#40497=CARTESIAN_POINT ( 'NONE',  ( 2.602106451679912169, -43.97395833381127517, 26.32672608803957459 ) ) ;
#40501=CARTESIAN_POINT ( 'NONE',  ( 4.658274936810717470, -44.32822776703420686, 25.70768716362445261 ) ) ;
#40506=CARTESIAN_POINT ( 'NONE',  ( 7.757384923554905498, -46.78062499990440415, 29.19375250200204164 ) ) ;
#40512=CARTESIAN_POINT ( 'NONE',  ( 0.9468279798049134000, -51.84479166714461229, 27.28240155936039457 ) ) ;
#40519=AXIS2_PLACEMENT_3D ( 'NONE', #3195, #39120, #36137 ) ;
#40545=CARTESIAN_POINT ( 'NONE',  ( 2.602106451679909505, -51.80729166714461797, 32.06077891596451224 ) ) ;
#40563=DIRECTION ( 'NONE',  ( 0.000000000000000000, 1.000000000000000000, 0.000000000000000000 ) ) ;
#40564=CARTESIAN_POINT ( 'NONE',  ( 0.7573849235549138248, -48.73541666762257307, 27.17302655983835180 ) ) ;
#40565=CARTESIAN_POINT ( 'NONE',  ( 0.9468279798049124008, -42.84895833381127517, 31.10510344464368515 ) ) ;
#40595=CARTESIAN_POINT ( 'NONE',  ( 4.873229714572088866, -48.83333297527259731, 25.73192528989814321 ) ) ;
#40600=ORIENTED_EDGE ( 'NONE', *, *, #9560, .T. ) ;
#40607=CARTESIAN_POINT ( 'NONE',  ( 0.9468279798049125118, -42.30312500047794799, 29.19375250200204164 ) ) ;
#40636=CARTESIAN_POINT ( 'NONE',  ( 2.602106451679909505, -49.21979166714461940, 32.06077891596451224 ) ) ;
#40641=CARTESIAN_POINT ( 'NONE',  ( 7.757384923554902834, -45.79166666666666430, 31.21447844416572792 ) ) ;
#40646=CARTESIAN_POINT ( 'NONE',  ( 7.567941867304904591, -47.59895833381127517, 27.28240155936039812 ) ) ;
#40647=CARTESIAN_POINT ( 'NONE',  ( 7.567941867304905479, -48.55312500047794799, 29.19375250200204164 ) ) ;
#40656=CARTESIAN_POINT ( 'NONE',  ( 7.757384923554905498, -44.74999999999999289, 29.19375250200204164 ) ) ;
#40657=CARTESIAN_POINT ( 'NONE',  ( 7.567941867304904591, -48.14062500047794657, 29.19375250200204164 ) ) ;
#40660=CARTESIAN_POINT ( 'NONE',  ( 4.257384923554909051, -52.75000000000000000, 32.69375250200203453 ) ) ;
#40667=CARTESIAN_POINT ( 'NONE',  ( 6.007384923554907274, -47.36041666762257307, 26.16266358875650866 ) ) ;
#40673=EDGE_CURVE ( 'NONE', #22457, #16800, #1019, .T. ) ;
#40692=ORIENTED_EDGE ( 'NONE', *, *, #34173, .F. ) ;
#40697=CARTESIAN_POINT ( 'NONE',  ( 7.567941867304904591, -43.64062500047794657, 29.19375250200204164 ) ) ;
#40704=CARTESIAN_POINT ( 'NONE',  ( 2.507384923554909495, -43.94729166657106845, 32.22484141524756751 ) ) ;
#40709=CARTESIAN_POINT ( 'NONE',  ( 0.9701386403401061065, -43.66210072765234429, 30.48733976708923166 ) ) ;
#40711=CARTESIAN_POINT ( 'NONE',  ( 0.9468279798049115126, -51.76145833381127659, 31.10510344464368515 ) ) ;
#40712=DIRECTION ( 'NONE',  ( 0.000000000000000000, 1.000000000000000000, 0.000000000000000000 ) ) ;
#40746=CARTESIAN_POINT ( 'NONE',  ( 4.257384923554909051, -50.01562500047793947, 25.37105061671875461 ) ) ;
#40751=CARTESIAN_POINT ( 'NONE',  ( 4.257384923554909051, -52.75000000000000000, 32.69375250200203453 ) ) ;
#40756=ORIENTED_EDGE ( 'NONE', *, *, #16057, .T. ) ;
#40767=CARTESIAN_POINT ( 'NONE',  ( 0.7573849235549129366, -48.69375000095590167, 29.19375250200204164 ) ) ;
#40787=DIRECTION ( 'NONE',  ( -0.000000000000000000, -1.000000000000000000, -0.000000000000000000 ) ) ;
#40819=CARTESIAN_POINT ( 'NONE',  ( 5.912663395429907709, -43.96979166714461940, 26.32672608803957459 ) ) ;
#40846=CARTESIAN_POINT ( 'NONE',  ( 5.912663395429907709, -44.96979166714461940, 26.32672608803957459 ) ) ;
#40851=CARTESIAN_POINT ( 'NONE',  ( 6.007384923554907274, -43.66666666666665719, 26.16266358875650866 ) ) ;
#40856=CARTESIAN_POINT ( 'NONE',  ( 4.257384923554908163, -45.76562500047795368, 33.01645438728532866 ) ) ;
#40857=CARTESIAN_POINT ( 'NONE',  ( 0.9468279798049134000, -47.84479166714461229, 27.28240155936039102 ) ) ;
#40865=CARTESIAN_POINT ( 'NONE',  ( 6.007384923554907274, -45.16666666666665719, 26.16266358875650866 ) ) ;
#40866=CARTESIAN_POINT ( 'NONE',  ( 7.567941867304902814, -49.09895833381128227, 27.28240155936039457 ) ) ;
#40871=DIRECTION ( 'NONE',  ( -0.000000000000000000, -1.000000000000000000, -0.000000000000000000 ) ) ;
#40879=CARTESIAN_POINT ( 'NONE',  ( 7.757384923554905498, -46.44375000095590877, 29.19375250200204164 ) ) ;
#40910=CARTESIAN_POINT ( 'NONE',  ( 4.981705856419682554, -44.55394497124888886, 32.63577228912052419 ) ) ;
#40915=CARTESIAN_POINT ( 'NONE',  ( 0.7573849235549129366, -43.03062499990439704, 29.19375250200204164 ) ) ;
#40918=EDGE_CURVE ( 'NONE', #13147, #631, #26845, .T. ) ;
#40924=CARTESIAN_POINT ( 'NONE',  ( 7.567941867304905479, -52.05312500047794799, 29.19375250200204164 ) ) ;
#40959=VERTEX_POINT ( 'NONE', #15367 ) ;
#40961=CARTESIAN_POINT ( 'NONE',  ( 7.567941867304904591, -50.14062500047794657, 29.19375250200204164 ) ) ;
#40964=DIRECTION ( 'NONE',  ( -0.000000000000000000, -1.000000000000000000, -0.000000000000000000 ) ) ;
#40968=CARTESIAN_POINT ( 'NONE',  ( 4.257384923554907274, -47.37499999999997868, 32.69375250200203453 ) ) ;
#40970=VERTEX_POINT ( 'NONE', #14526 ) ;
#40973=CARTESIAN_POINT ( 'NONE',  ( 0.7573849235549129366, -52.03062499990439704, 29.19375250200204164 ) ) ;
#40981=EDGE_CURVE ( 'NONE', #21757, #18585, #5766, .T. ) ;
#40982=CARTESIAN_POINT ( 'NONE',  ( 4.257384923554909051, -47.81875000095592299, 25.15230061767466552 ) ) ;
#41017=CARTESIAN_POINT ( 'NONE',  ( 4.257443491160582738, -48.81875139542229647, 25.69375250249206744 ) ) ;
#41032=CARTESIAN_POINT ( 'NONE',  ( 4.257384923554909051, -43.92812500047795510, 25.37105061671875461 ) ) ;
#41038=ORIENTED_EDGE ( 'NONE', *, *, #25063, .F. ) ;
#41064=CARTESIAN_POINT ( 'NONE',  ( 7.318519326147631787, -42.40485061181025372, 27.50104830306472081 ) ) ;
#41066=CARTESIAN_POINT ( 'NONE',  ( 4.224336222578468636, -42.81796322358007245, 25.69388605220731847 ) ) ;
#41071=CARTESIAN_POINT ( 'NONE',  ( 2.602106451679909505, -42.80729166714461797, 32.06077891596451224 ) ) ;
#41074=CARTESIAN_POINT ( 'NONE',  ( 2.602106451679909505, -48.71979166714461229, 32.06077891596451224 ) ) ;
#41084=CARTESIAN_POINT ( 'NONE',  ( 2.507384923554909495, -44.91666666666665719, 32.22484141524756751 ) ) ;
#41085=CARTESIAN_POINT ( 'NONE',  ( 2.602106451679909505, -47.80729166714461087, 32.06077891596451224 ) ) ;
#41088=CARTESIAN_POINT ( 'NONE',  ( 4.257384923554907274, -47.87499999999998579, 32.69375250200203453 ) ) ;
#41096=CARTESIAN_POINT ( 'NONE',  ( 7.757384923554902834, -47.48541666762257307, 31.21447844416572792 ) ) ;
#41115=CARTESIAN_POINT ( 'NONE',  ( 0.8497169545472491592, -49.67363851611187897, 30.11463166423736126 ) ) ;
#41117=CARTESIAN_POINT ( 'NONE',  ( 7.708706269020556334, -50.96287277223758849, 29.95749870462118736 ) ) ;
#41123=CARTESIAN_POINT ( 'NONE',  ( 4.257384923554908163, -50.37499999999998579, 33.23520438632941421 ) ) ;
#41129=CARTESIAN_POINT ( 'NONE',  ( 5.912663395429904156, -50.72395833381128227, 32.06077891596451224 ) ) ;
#41131=EDGE_CURVE ( 'NONE', #36320, #34895, #2165, .T. ) ;
#41134=CARTESIAN_POINT ( 'NONE',  ( 2.831140700720844894, -51.10262509025741906, 32.39001997092292839 ) ) ;
#41137=CARTESIAN_POINT ( 'NONE',  ( 2.507384923554909495, -42.44729166657106845, 32.22484141524756751 ) ) ;
#41144=CARTESIAN_POINT ( 'NONE',  ( 2.507384923554909495, -42.11041666762257307, 32.22484141524756751 ) ) ;
#41178=CARTESIAN_POINT ( 'NONE',  ( 7.567941867304902814, -49.68229166714461797, 31.10510344464368870 ) ) ;
#41190=CARTESIAN_POINT ( 'NONE',  ( 6.007384923554907274, -51.69729166657106845, 26.16266358875650866 ) ) ;
#41193=ORIENTED_EDGE ( 'NONE', *, *, #18124, .T. ) ;
#41194=EDGE_CURVE ( 'NONE', #27540, #8545, #4175, .T. ) ;
#41197=CARTESIAN_POINT ( 'NONE',  ( 4.257384923554909051, -52.75000000000000000, 29.19375250200204164 ) ) ;
#41199=CARTESIAN_POINT ( 'NONE',  ( 4.257384923554908163, -46.56875000095590877, 33.23520438632941421 ) ) ;
#41216=EDGE_CURVE ( 'NONE', #24255, #27786, #23929, .T. ) ;
#41226=ADVANCED_FACE ( 'NONE', ( #34440 ), #1896, .T. ) ;
#41228=CARTESIAN_POINT ( 'NONE',  ( 1.185812148657462206, -46.23362346307683168, 27.45166453608769075 ) ) ;
#41229=LINE ( 'NONE', #15496, #28800 ) ;
#41244=CARTESIAN_POINT ( 'NONE',  ( 5.912663395429907709, -42.96979166714461940, 26.32672608803957459 ) ) ;
#41270=CARTESIAN_POINT ( 'NONE',  ( 3.817979627562230860, -45.80888858003611830, 25.71969949286686585 ) ) ;
#41276=CARTESIAN_POINT ( 'NONE',  ( 2.507384923554911715, -43.08333333333332149, 26.16266358875650866 ) ) ;
#41278=CARTESIAN_POINT ( 'NONE',  ( 4.870262998413927846, -49.33333905041367018, 25.74569417592035236 ) ) ;
#41281=CARTESIAN_POINT ( 'NONE',  ( 2.602106451679909505, -43.80729166714461797, 32.06077891596451224 ) ) ;
#41282=CARTESIAN_POINT ( 'NONE',  ( 4.257384923554908163, -45.67812500047794799, 33.01645438728532866 ) ) ;
#41285=VERTEX_POINT ( 'NONE', #18273 ) ;
#41291=CARTESIAN_POINT ( 'NONE',  ( 0.7573849235549138248, -44.04166666666665719, 27.17302655983835180 ) ) ;
#41292=CARTESIAN_POINT ( 'NONE',  ( 7.567941867304902814, -47.09895833381128227, 27.28240155936039457 ) ) ;
#41299=EDGE_CURVE ( 'NONE', #42017, #6132, #24459, .T. ) ;
#41300=ORIENTED_EDGE ( 'NONE', *, *, #24145, .T. ) ;
#41305=CARTESIAN_POINT ( 'NONE',  ( 0.7573849235549138248, -45.73541666762256597, 27.17302655983835180 ) ) ;
#41321=ORIENTED_EDGE ( 'NONE', *, *, #17639, .T. ) ;
#41323=DIRECTION ( 'NONE',  ( 0.000000000000000000, 0.000000000000000000, -1.000000000000000000 ) ) ;
#41326=CARTESIAN_POINT ( 'NONE',  ( 0.7573849235549120484, -50.45833333333332860, 31.21447844416572792 ) ) ;
#41329=CARTESIAN_POINT ( 'NONE',  ( 0.7573849235549129366, -50.99999999999999289, 29.19375250200204164 ) ) ;
#41333=FACE_OUTER_BOUND ( 'NONE', #435, .T. ) ;
#41334=CARTESIAN_POINT ( 'NONE',  ( 6.007384923554907274, -51.16666666666665719, 26.16266358875650866 ) ) ;
#41336=CARTESIAN_POINT ( 'NONE',  ( 6.014906377723012731, -50.35863679631177092, 26.13275671584835536 ) ) ;
#41340=LINE ( 'NONE', #28766, #41356 ) ;
#41344=CARTESIAN_POINT ( 'NONE',  ( 4.257384923554908163, -51.87499999999998579, 33.23520438632941421 ) ) ;
#41350=CARTESIAN_POINT ( 'NONE',  ( 0.9468279798049134000, -47.84479166714461229, 27.28240155936039457 ) ) ;
#41354=CARTESIAN_POINT ( 'NONE',  ( 6.007384923554907274, -51.36041666762257307, 26.16266358875650866 ) ) ;
#41356=VECTOR ( 'NONE', #38352, 1000.000000000000000 ) ;
#41368=CARTESIAN_POINT ( 'NONE',  ( 4.257384923554909051, -43.12499999999999289, 25.69375250200204519 ) ) ;
#41384=CARTESIAN_POINT ( 'NONE',  ( 0.9468279798049143992, -48.43229166714461087, 27.28240155936039812 ) ) ;
#41390=EDGE_CURVE ( 'NONE', #24255, #13392, #40409, .T. ) ;
#41394=AXIS2_PLACEMENT_3D ( 'NONE', #34633, #25072, #2093 ) ;
#41399=CARTESIAN_POINT ( 'NONE',  ( 0.7573849235549138248, -51.07229166657106845, 27.17302655983835180 ) ) ;
#41401=ORIENTED_EDGE ( 'NONE', *, *, #32098, .F. ) ;
#41405=CARTESIAN_POINT ( 'NONE',  ( 7.581482109886807486, -42.41933560691557403, 28.06786826585468120 ) ) ;
#41406=CARTESIAN_POINT ( 'NONE',  ( 7.757384923554902834, -46.48541666762257307, 31.21447844416572792 ) ) ;
#41408=VERTEX_POINT ( 'NONE', #2323 ) ;
#41409=DIRECTION ( 'NONE',  ( 0.000000000000000000, 0.000000000000000000, -1.000000000000000000 ) ) ;
#41411=CARTESIAN_POINT ( 'NONE',  ( 2.160769449054563918, -46.76683909755764290, 26.36694297485869498 ) ) ;
#41427=CARTESIAN_POINT ( 'NONE',  ( 5.195207097063835988, -42.85267090063073425, 32.69375250200204164 ) ) ;
#41432=CARTESIAN_POINT ( 'NONE',  ( 1.090861531830362940, -48.15903358148088387, 30.68489001010549089 ) ) ;
#41445=CARTESIAN_POINT ( 'NONE',  ( 2.722885376285983483, -42.40452717880835110, 32.34230368909746289 ) ) ;
#41455=CARTESIAN_POINT ( 'NONE',  ( 0.9468279798049134000, -42.84479166714461940, 27.28240155936039457 ) ) ;
#41456=CARTESIAN_POINT ( 'NONE',  ( 6.007384923554907274, -42.36041666762257307, 26.16266358875650866 ) ) ;
#41479=CARTESIAN_POINT ( 'NONE',  ( 7.793954214201344044, -45.44835223390516177, 29.32909286842892982 ) ) ;
#41483=CARTESIAN_POINT ( 'NONE',  ( 1.318557518874711398, -45.64744183096181729, 31.11822447732679109 ) ) ;
#41489=CARTESIAN_POINT ( 'NONE',  ( 0.7573849235549120484, -42.45833333333332860, 31.21447844416572792 ) ) ;
#41494=CARTESIAN_POINT ( 'NONE',  ( 5.912663395429904156, -44.72395833381127517, 32.06077891596451224 ) ) ;
#41495=CARTESIAN_POINT ( 'NONE',  ( 0.9468279798049125118, -45.30312500047794799, 29.19375250200204164 ) ) ;
#41503=CARTESIAN_POINT ( 'NONE',  ( 7.726943934575421835, -46.92952120584362774, 28.49386773333143097 ) ) ;
#41504=CARTESIAN_POINT ( 'NONE',  ( 2.507384923554909495, -43.91666666666665719, 32.22484141524756751 ) ) ;
#41505=CARTESIAN_POINT ( 'NONE',  ( 2.602106451679909505, -46.30729166714461797, 32.06077891596451224 ) ) ;
#41542=CARTESIAN_POINT ( 'NONE',  ( 7.757384923554905498, -50.74999999999999289, 29.19375250200204164 ) ) ;
#41549=CARTESIAN_POINT ( 'NONE',  ( 4.457108023815643527, -50.32305449969910427, 25.69863942513239863 ) ) ;
#41552=CARTESIAN_POINT ( 'NONE',  ( 2.523426821904034334, -51.27645931062548357, 26.12032704423936735 ) ) ;
#41555=CARTESIAN_POINT ( 'NONE',  ( 0.7573849235549120484, -43.98895833323772564, 31.21447844416572792 ) ) ;
#41557=CARTESIAN_POINT ( 'NONE',  ( 7.567941867304904591, -52.14062500047794657, 29.19375250200204164 ) ) ;
#41562=EDGE_CURVE ( 'NONE', #9278, #5298, #36328, .T. ) ;
#41563=CARTESIAN_POINT ( 'NONE',  ( 7.567941867304905479, -47.55312500047795510, 29.19375250200204164 ) ) ;
#41565=CARTESIAN_POINT ( 'NONE',  ( 2.783286337577825176, -48.60390859220163406, 32.37987436702933053 ) ) ;
#41580=CARTESIAN_POINT ( 'NONE',  ( 4.257384923554909051, -52.75000000000000000, 32.69375250200203453 ) ) ;
#41589=CARTESIAN_POINT ( 'NONE',  ( 4.257384923554909051, -52.75000000000000000, 25.69375250200204519 ) ) ;
#41593=EDGE_LOOP ( 'NONE', ( #16436, #23721, #13555, #37887 ) ) ;
#41595=CARTESIAN_POINT ( 'NONE',  ( 2.602106451679912169, -47.97395833381128227, 26.32672608803957459 ) ) ;
#41602=CARTESIAN_POINT ( 'NONE',  ( 7.567941867304905479, -52.01145833381129080, 27.28240155936039457 ) ) ;
#41604=DIRECTION ( 'NONE',  ( -1.000000000000000000, 0.000000000000000000, 0.000000000000000000 ) ) ;
#41609=CARTESIAN_POINT ( 'NONE',  ( 2.507384923554909495, -51.94729166657106845, 32.22484141524756751 ) ) ;
#41615=CARTESIAN_POINT ( 'NONE',  ( 7.419819297308113626, -42.47768670061491036, 30.71893562847657932 ) ) ;
#41616=CARTESIAN_POINT ( 'NONE',  ( 0.7573849235549138248, -45.73541666762256597, 27.17302655983835180 ) ) ;
#41618=ORIENTED_EDGE ( 'NONE', *, *, #35649, .F. ) ;
#41621=CARTESIAN_POINT ( 'NONE',  ( 1.845678898593310580, -46.75774494461840902, 26.62135694635153627 ) ) ;
#41634=CARTESIAN_POINT ( 'NONE',  ( 4.257372105343447011, -50.31874971046479317, 25.69375250202551797 ) ) ;
#41636=EDGE_CURVE ( 'NONE', #321, #24255, #41821, .T. ) ;
#41639=( BOUNDED_CURVE ( )  B_SPLINE_CURVE ( 1, ( #4561, #34532 ),
 .UNSPECIFIED., .F., .F. ) 
 B_SPLINE_CURVE_WITH_KNOTS ( ( 2, 2 ),
 ( 0.000000000000000000, 1.000000000000000000 ),
 .UNSPECIFIED. ) 
 CURVE ( )  GEOMETRIC_REPRESENTATION_ITEM ( )  RATIONAL_B_SPLINE_CURVE ( ( 0.9666183089694433406, 0.9666183089694433406 ) ) 
 REPRESENTATION_ITEM ( '' )  );
#41646=CARTESIAN_POINT ( 'NONE',  ( 3.384420263264186879, -48.29861120262528118, 25.79722196747504981 ) ) ;
#41650=CARTESIAN_POINT ( 'NONE',  ( 5.912663395429905044, -46.13645833381128369, 32.06077891596451224 ) ) ;
#41656=CARTESIAN_POINT ( 'NONE',  ( 6.891116391645906170, -48.00330039333458387, 31.54103961699432190 ) ) ;
#41691=CARTESIAN_POINT ( 'NONE',  ( 3.708862610918322922, -45.80635049771240119, 25.73524927127315109 ) ) ;
#41703=CARTESIAN_POINT ( 'NONE',  ( 4.257384923554909051, -43.51562500047794657, 25.37105061671875461 ) ) ;
#41704=CARTESIAN_POINT ( 'NONE',  ( 0.9468279798049134000, -45.84479166714461229, 27.28240155936039102 ) ) ;
#41710=CIRCLE ( 'NONE', #32197, 5.000000000000004441 ) ;
#41713=CARTESIAN_POINT ( 'NONE',  ( 2.507384923554909495, -42.41666666666665719, 32.22484141524756751 ) ) ;
#41714=CARTESIAN_POINT ( 'NONE',  ( 0.9468279798049132889, -45.39062500047794657, 29.19375250200204164 ) ) ;
#41752=CARTESIAN_POINT ( 'NONE',  ( 0.7573849235549129366, -48.99999999999998579, 29.19375250200204164 ) ) ;
#41759=CARTESIAN_POINT ( 'NONE',  ( 4.257384923554909939, 0.8500000000000035305, 34.69375250200203453 ) ) ;
#41760=CARTESIAN_POINT ( 'NONE',  ( 7.670955751635855080, -50.46401105366427942, 30.09320378183186051 ) ) ;
#41763=CARTESIAN_POINT ( 'NONE',  ( 3.807290611962736104, -51.30803347542620685, 25.69375680867332079 ) ) ;
#41766=CARTESIAN_POINT ( 'NONE',  ( 0.7573849235549120484, -51.45833333333332860, 31.21447844416572792 ) ) ;
#41769=CARTESIAN_POINT ( 'NONE',  ( 7.254877732733446827, -46.48887622534604702, 31.02403140709775897 ) ) ;
#41771=CARTESIAN_POINT ( 'NONE',  ( 5.912663395429907709, -47.96979166714461229, 26.32672608803957459 ) ) ;
#41777=CARTESIAN_POINT ( 'NONE',  ( 4.257384923554909051, -42.40485061181025372, 32.69375250200203453 ) ) ;
#41778=CARTESIAN_POINT ( 'NONE',  ( 7.757384923554905498, -52.75000000000000000, 29.19375250200204164 ) ) ;
#41805=CARTESIAN_POINT ( 'NONE',  ( 4.257384923554909051, -51.12499999999999289, 25.69375250200204519 ) ) ;
#41813=CARTESIAN_POINT ( 'NONE',  ( 2.602106451679912169, -48.97395833381128227, 26.32672608803957459 ) ) ;
#41814=PLANE ( 'NONE',  #32654 ) ;
#41818=CARTESIAN_POINT ( 'NONE',  ( 2.602106451679909505, -49.21979166714461940, 32.06077891596451224 ) ) ;
#41821=( BOUNDED_CURVE ( )  B_SPLINE_CURVE ( 2, ( #11788, #24008, #27398, #28166, #5835, #15418, #2434, #31766, #25198 ),
 .UNSPECIFIED., .F., .F. ) 
 B_SPLINE_CURVE_WITH_KNOTS ( ( 3, 2, 2, 2, 3 ),
 ( 0.7125000000000000222, 0.7166666666666666741, 0.7249999999999999778, 0.7333333333333332815, 0.7375000000000000444 ),
 .UNSPECIFIED. ) 
 CURVE ( )  GEOMETRIC_REPRESENTATION_ITEM ( )  RATIONAL_B_SPLINE_CURVE ( ( 0.9330127018922194093, 0.9330127018922194093, 1.000000000000000000, 0.8660254037844387076, 1.000000000000000000, 0.8660254037844387076, 1.000000000000000000, 0.9330127018922185211, 0.9330127018922194093 ) ) 
 REPRESENTATION_ITEM ( '' )  );
#41822=ORIENTED_EDGE ( 'NONE', *, *, #31967, .T. ) ;
#41826=CARTESIAN_POINT ( 'NONE',  ( 0.7573849235549138248, -51.57229166657107555, 27.17302655983835180 ) ) ;
#41832=CARTESIAN_POINT ( 'NONE',  ( 7.757384923554902834, -45.48541666762258018, 31.21447844416572792 ) ) ;
#41837=CARTESIAN_POINT ( 'NONE',  ( 4.255650924630306697, -46.81870871537116585, 25.69375247392593664 ) ) ;
#41840=EDGE_CURVE ( 'NONE', #34895, #10524, #11021, .T. ) ;
#41860=DIRECTION ( 'NONE',  ( 0.000000000000000000, 1.000000000000000000, 0.000000000000000000 ) ) ;
#41863=CARTESIAN_POINT ( 'NONE',  ( 2.510907566537041280, -48.10860061040995816, 32.26504720916054936 ) ) ;
#41866=CARTESIAN_POINT ( 'NONE',  ( 0.7684673811017630474, -46.18787926659695842, 29.47208334557828024 ) ) ;
#41867=CARTESIAN_POINT ( 'NONE',  ( 4.257384923554909051, -46.42812500047794799, 25.37105061671875461 ) ) ;
#41883=CARTESIAN_POINT ( 'NONE',  ( 3.458056246848340454, -50.58802889386231527, 32.60320010129223078 ) ) ;
#41890=B_SPLINE_CURVE_WITH_KNOTS ( 'NONE', 3,
 ( #19811, #35358, #19598, #32167, #28754, #6431, #458, #39367, #22803, #19402, #6635, #6221, #16023, #32571, #35974, #3438, #3030, #10245, #3646, #16635, #29594, #39161, #6838, #13228, #15806, #16430, #6009, #28965 ),
 .UNSPECIFIED., .F., .F.,
 ( 4, 2, 1, 1, 1, 1, 2, 2, 2, 2, 2, 2, 2, 2, 2, 4 ),
 ( 0.4697586089320929248, 0.4697756252119271725, 0.4697926414917614202, 0.4698266740514299156, 0.4698947391707669619, 0.4700308694094409434, 0.4703031298867890175, 0.4708476508414850548, 0.4719366927508771847, 0.4741147765696614447, 0.4762928603884457046, 0.4784709442072299646, 0.4806490280260142245, 0.4828271118447984844, 0.4850051956635827444, 0.4871832794823670043 ),
 .UNSPECIFIED. ) ;
#41910=CARTESIAN_POINT ( 'NONE',  ( 1.048089749400655579, -45.66146103540702939, 30.59184582071224767 ) ) ;
#41921=CARTESIAN_POINT ( 'NONE',  ( 2.602106451679912169, -44.47395833381127517, 26.32672608803957459 ) ) ;
#41922=CARTESIAN_POINT ( 'NONE',  ( 4.257384923554909051, -44.92812500047794799, 25.37105061671875106 ) ) ;
#41928=CARTESIAN_POINT ( 'NONE',  ( 7.166792211719248407, -46.89730324316374066, 27.19494096043778342 ) ) ;
#41929=CARTESIAN_POINT ( 'NONE',  ( 7.567941867304902814, -46.68229166714461087, 31.10510344464368870 ) ) ;
#41955=EDGE_LOOP ( 'NONE', ( #41401, #21550, #2055, #1018 ) ) ;
#41961=CARTESIAN_POINT ( 'NONE',  ( 7.757383757921477496, -47.45343320964042277, 29.65190956378627263 ) ) ;
#41965=CARTESIAN_POINT ( 'NONE',  ( 4.257384923554909051, -49.62499999999998579, 25.15230061767466552 ) ) ;
#41972=CARTESIAN_POINT ( 'NONE',  ( 7.567941867304904591, -51.64062500047794657, 29.19375250200204164 ) ) ;
#41978=CARTESIAN_POINT ( 'NONE',  ( 0.7573849235549120484, -49.95833333333332860, 31.21447844416572792 ) ) ;
#41981=CARTESIAN_POINT ( 'NONE',  ( 5.529148135610982173, -46.34911474184233526, 25.91596308222525380 ) ) ;
#41983=CARTESIAN_POINT ( 'NONE',  ( 0.9468279798049134000, -49.84479166714461940, 27.28240155936039457 ) ) ;
#41986=CARTESIAN_POINT ( 'NONE',  ( 0.7484315261398766239, -48.70256682825286276, 28.79284084005871236 ) ) ;
#41991=LINE ( 'NONE', #20061, #25799 ) ;
#42017=VERTEX_POINT ( 'NONE', #35602 ) ;
#42021=CARTESIAN_POINT ( 'NONE',  ( 0.9468279798049132889, -46.89062500047794657, 29.19375250200204164 ) ) ;
#42026=CARTESIAN_POINT ( 'NONE',  ( 4.257384923554909051, -51.42812500047794799, 25.37105061671875106 ) ) ;
#42032=CARTESIAN_POINT ( 'NONE',  ( 4.257384923554909051, -49.15562499990438994, 25.15230061767466552 ) ) ;
#42038=CARTESIAN_POINT ( 'NONE',  ( 0.7573849235549138248, -45.23541666762257307, 27.17302655983835180 ) ) ;
#42052=DIRECTION ( 'NONE',  ( 0.4447208605404111559, 0.000000000000000000, -0.8956692225370905813 ) ) ;
#42054=CARTESIAN_POINT ( 'NONE',  ( 2.142585429583778289, -51.62158056362617486, 32.03308208067690543 ) ) ;
#42056=DIRECTION ( 'NONE',  ( -0.000000000000000000, -1.000000000000000000, -0.000000000000000000 ) ) ;
#42067=FACE_OUTER_BOUND ( 'NONE', #12301, .T. ) ;
#42071=CARTESIAN_POINT ( 'NONE',  ( 2.602106451679909505, -44.71979166714461940, 32.06077891596451224 ) ) ;
#42074=CARTESIAN_POINT ( 'NONE',  ( 0.7573849235549138248, -50.04166666666665719, 27.17302655983835180 ) ) ;
#42081=CONICAL_SURFACE ( 'NONE', #14232, 5.000000000000004441, 0.7853981633974447263 ) ;
#42085=LINE ( 'NONE', #38465, #38209 ) ;
#42091=EDGE_CURVE ( 'NONE', #31605, #21912, #1136, .T. ) ;
#42112=CARTESIAN_POINT ( 'NONE',  ( 4.257384923554907274, -47.37499999999997868, 32.69375250200203453 ) ) ;
#42115=CARTESIAN_POINT ( 'NONE',  ( 4.257384923554913492, -50.87499999999999289, 32.69375250200203453 ) ) ;
#42153=COLOUR_RGB('Black',0.12,0.14,0.17);
#42154=FILL_AREA_STYLE_COLOUR('',#42153);
#42155=FILL_AREA_STYLE('',(#42154));
#42156=SURFACE_STYLE_FILL_AREA(#42155);
#42157=SURFACE_SIDE_STYLE('',(#42156));
#42158=SURFACE_STYLE_USAGE(.BOTH.,#42157);
#42159=PRESENTATION_STYLE_ASSIGNMENT((#42158));
ENDSEC;
END-ISO-10303-21;
